ISO-10303-21;
HEADER;
FILE_DESCRIPTION (('STEP AP214'),
    '1' );
FILE_NAME ('base.step',
    '2026-10-05T20:10:51',
    ( '' ),
    ( '' ),
    'SwSTEP 2.0',
    'SolidWorks 2020',
    '' );
FILE_SCHEMA (( 'AUTOMOTIVE_DESIGN' ));
ENDSEC;

DATA;
#32=ADVANCED_FACE ( 'NONE', ( #8553 ), #60499, .T. ) ;
#41=CARTESIAN_POINT ( 'NONE',  ( 1.642778471875001811, -1.742708332855374298, 2.845375778867859751 ) ) ;
#121=CARTESIAN_POINT ( 'NONE',  ( -2.324088772396477673E-16, -1.093749999044084653, -3.475000000000000089 ) ) ;
#174=CARTESIAN_POINT ( 'NONE',  ( 1.467871227757891193E-11, -3.138498625356828775, -3.379301813585260383 ) ) ;
#200=CARTESIAN_POINT ( 'NONE',  ( 3.475000000000000533, -2.945833333333332416, -2.006292185433951047 ) ) ;
#291=CARTESIAN_POINT ( 'NONE',  ( 1.001543065824772753E-15, -3.762499999999999289, 4.012584370867899430 ) ) ;
#302=CARTESIAN_POINT ( 'NONE',  ( -3.285556943750000514, -0.5760416661887087786, -1.896917185911906500 ) ) ;
#359=CARTESIAN_POINT ( 'NONE',  ( 3.475000000000000533, -3.631249999044082966, 0.000000000000000000 ) ) ;
#385=AXIS2_PLACEMENT_3D ( 'NONE', #162717, #16422, #146480 ) ;
#416=DIRECTION ( 'NONE',  ( 0.000000000000000000, -1.000000000000000000, 0.000000000000000000 ) ) ;
#449=CARTESIAN_POINT ( 'NONE',  ( 3.285556943750000070, -1.684374999522043836, 0.000000000000000000 ) ) ;
#473=AXIS2_PLACEMENT_3D ( 'NONE', #86071, #54636, #69791 ) ;
#575=CYLINDRICAL_SURFACE ( 'NONE', #7911, 3.475000000000000089 ) ;
#652=CARTESIAN_POINT ( 'NONE',  ( 3.285556943749998737, -3.755208332855373587, -1.896917185911906500 ) ) ;
#655=ORIENTED_EDGE ( 'NONE', *, *, #150659, .T. ) ;
#800=CARTESIAN_POINT ( 'NONE',  ( 0.000000000000000000, -0.08749999999999961975, -4.012584370867899430 ) ) ;
#834=B_SPLINE_CURVE_WITH_KNOTS ( 'NONE', 3,
 ( #91115, #202684, #5534, #157174, #88976, #21785, #39148 ),
 .UNSPECIFIED., .F., .F.,
 ( 4, 3, 4 ),
 ( 0.002201685690204611880, 0.002395020826490580276, 0.002952547457960625829 ),
 .UNSPECIFIED. ) ;
#847=CARTESIAN_POINT ( 'NONE',  ( -3.475000000000000533, -3.849999999999999201, 0.000000000000000000 ) ) ;
#849=CARTESIAN_POINT ( 'NONE',  ( -1.642778471874998480, -3.288541666188707246, 2.845375778867863303 ) ) ;
#881=ORIENTED_EDGE ( 'NONE', *, *, #139074, .T. ) ;
#897=VERTEX_POINT ( 'NONE', #202354 ) ;
#916=CARTESIAN_POINT ( 'NONE',  ( -1.642778471875000035, -1.655208332855377051, -2.845375778867859751 ) ) ;
#1083=CARTESIAN_POINT ( 'NONE',  ( -3.277990255609289694, -0.8976961690679158279, 0.3594898028441471105 ) ) ;
#1114=CARTESIAN_POINT ( 'NONE',  ( -1.642778471875000035, -3.317708332855374476, -2.845375778867859751 ) ) ;
#1142=VERTEX_POINT ( 'NONE', #84590 ) ;
#1250=CARTESIAN_POINT ( 'NONE',  ( 2.691539545140940959, -3.171237134043524808, -1.997224515217858487 ) ) ;
#1269=DIRECTION ( 'NONE',  ( -3.491481338843133750E-15, -0.000000000000000000, -1.000000000000000000 ) ) ;
#1276=CARTESIAN_POINT ( 'NONE',  ( -3.285556943750000070, -0.1112512837626866702, -0.04025571921194345121 ) ) ;
#1277=CARTESIAN_POINT ( 'NONE',  ( 3.475000000000000533, -3.645833333333333037, -2.006292185433951047 ) ) ;
#1365=CARTESIAN_POINT ( 'NONE',  ( 3.475000000000000533, -3.675000000000001155, 0.000000000000000000 ) ) ;
#1401=CARTESIAN_POINT ( 'NONE',  ( -3.285556943750000070, -1.859374999522041882, 0.000000000000000000 ) ) ;
#1435=CARTESIAN_POINT ( 'NONE',  ( -1.737500000000000266, -2.814583332377419644, -3.009438278150923907 ) ) ;
#1522=CARTESIAN_POINT ( 'NONE',  ( 3.285556943750000070, -0.9843749995220412163, 0.000000000000000000 ) ) ;
#1639=AXIS2_PLACEMENT_3D ( 'NONE', #182712, #2874, #135066 ) ;
#1653=VECTOR ( 'NONE', #11849, 1000.000000000000000 ) ;
#1729=CARTESIAN_POINT ( 'NONE',  ( 1.001543065824772753E-15, -3.521874999522041083, 3.793834371823811669 ) ) ;
#1735=DIRECTION ( 'NONE',  ( 0.000000000000000000, 1.000000000000000000, 0.000000000000000000 ) ) ;
#1875=DIRECTION ( 'NONE',  ( -0.000000000000000000, 1.000000000000000000, -0.000000000000000000 ) ) ;
#1877=CARTESIAN_POINT ( 'NONE',  ( 3.285556943750000514, -3.813541666188710710, 1.896917185911906500 ) ) ;
#1921=CARTESIAN_POINT ( 'NONE',  ( -3.475000000000000533, -3.879166666666665986, -2.006292185433948827 ) ) ;
#1924=CARTESIAN_POINT ( 'NONE',  ( 1.642778471875001811, -1.392708332855374653, 2.845375778867859751 ) ) ;
#1983=CARTESIAN_POINT ( 'NONE',  ( 1.642778471875001811, -1.130208332855375808, 2.845375778867859751 ) ) ;
#1991=ORIENTED_EDGE ( 'NONE', *, *, #214118, .F. ) ;
#2058=EDGE_CURVE ( 'NONE', #144530, #7256, #60351, .T. ) ;
#2067=VECTOR ( 'NONE', #106947, 1000.000000000000114 ) ;
#2141=CARTESIAN_POINT ( 'NONE',  ( -3.367283612523017666, -0.9434115528611304313, 0.1057662437326452737 ) ) ;
#2168=CARTESIAN_POINT ( 'NONE',  ( 1.642778471875000035, -2.676041666188708756, -2.845375778867859751 ) ) ;
#2302=EDGE_CURVE ( 'NONE', #64997, #36604, #30885, .T. ) ;
#2303=DIRECTION ( 'NONE',  ( -0.6483454320283789096, 0.000000000000000000, 0.7613463080411795314 ) ) ;
#2337=CARTESIAN_POINT ( 'NONE',  ( 3.130865642711470276, -4.000192543527539613, -1.507748429708645199 ) ) ;
#2363=CARTESIAN_POINT ( 'NONE',  ( -1.499999999999963141, 7.750000000000000000, 10.86128356754324820 ) ) ;
#2402=DIRECTION ( 'NONE',  ( 0.000000000000000000, -1.000000000000000000, -0.000000000000000000 ) ) ;
#2463=CARTESIAN_POINT ( 'NONE',  ( -3.285556943750000070, -2.209374999522041527, 0.000000000000000000 ) ) ;
#2501=CARTESIAN_POINT ( 'NONE',  ( -1.642778471875000035, -0.6052083328553746755, -2.845375778867859751 ) ) ;
#2526=AXIS2_PLACEMENT_3D ( 'NONE', #145885, #98183, #29972 ) ;
#2552=EDGE_LOOP ( 'NONE', ( #164602, #2842, #180087, #82500 ) ) ;
#2593=CARTESIAN_POINT ( 'NONE',  ( 3.285556943750000070, -2.734374999522042771, 0.000000000000000000 ) ) ;
#2725=FACE_OUTER_BOUND ( 'NONE', #33291, .T. ) ;
#2794=CARTESIAN_POINT ( 'NONE',  ( -1.642778471875000035, -3.317708332855374476, -2.845375778867859751 ) ) ;
#2803=EDGE_LOOP ( 'NONE', ( #93624, #58508, #129338, #132929, #183373, #210468, #60869 ) ) ;
#2818=B_SPLINE_CURVE_WITH_KNOTS ( 'NONE', 3,
 ( #18413, #150579, #1083, #68218, #17337, #180927, #164686, #117058, #84488, #197176, #201414, #133282, #19477, #33611, #67147, #16269, #2141, #135392, #53053, #166820, #52002, #82354, #168939, #118128, #36796, #48812 ),
 .UNSPECIFIED., .F., .F.,
 ( 4, 2, 2, 2, 2, 2, 2, 2, 2, 2, 2, 2, 4 ),
 ( 8.741117365843410899E-19, 0.0002250267552868354852, 0.0003375401329302527942, 0.0003937968217519613131, 0.0004219251661628155726, 0.0004500535105736698321, 0.0004641176827790974768, 0.0004781818549845251215, 0.0005063101993953802483, 0.0005625668882170907189, 0.0006750802658605122020, 0.0009001070211473549514, 0.001800214042294726599 ),
 .UNSPECIFIED. ) ;
#2842=ORIENTED_EDGE ( 'NONE', *, *, #188328, .T. ) ;
#2874=DIRECTION ( 'NONE',  ( -1.000000000000000000, 0.000000000000000000, 3.491481338843133355E-15 ) ) ;
#2945=CARTESIAN_POINT ( 'NONE',  ( 3.285556943749998737, -3.755208332855373587, -1.896917185911906500 ) ) ;
#2992=CARTESIAN_POINT ( 'NONE',  ( -1.642778471874998480, -0.7510416661887092671, 2.845375778867863303 ) ) ;
#3014=CIRCLE ( 'NONE', #44663, 9.999999999999996447 ) ;
#3052=CARTESIAN_POINT ( 'NONE',  ( 3.285556943750000070, -2.121874999522044281, 0.000000000000000000 ) ) ;
#3115=COLOUR_RGB ( '', 0.40784314, 0.44705882, 0.49803922) ;
#3140=EDGE_CURVE ( 'NONE', #7595, #204603, #137712, .T. ) ;
#3232=EDGE_CURVE ( 'NONE', #63041, #179285, #73016, .T. ) ;
#3243=CARTESIAN_POINT ( 'NONE',  ( -3.285556943749998737, -2.180208332855376518, 1.896917185911908499 ) ) ;
#3433=CARTESIAN_POINT ( 'NONE',  ( -4.124095526617549778E-13, -0.9769569599453676867, 3.449959810851647823 ) ) ;
#3512=DIRECTION ( 'NONE',  ( 0.000000000000000000, 0.000000000000000000, 1.000000000000000000 ) ) ;
#3531=CARTESIAN_POINT ( 'NONE',  ( 1.001543065824772753E-15, -2.471874999522041705, 3.793834371823810780 ) ) ;
#3566=CARTESIAN_POINT ( 'NONE',  ( 2.665787623643367521, -4.288499431575266918, -2.473491168755026948 ) ) ;
#3588=CARTESIAN_POINT ( 'NONE',  ( 7.204675194429079505E-15, -1.487500000000000044, -3.475000000000000089 ) ) ;
#3607=ORIENTED_EDGE ( 'NONE', *, *, #5122, .F. ) ;
#3615=CARTESIAN_POINT ( 'NONE',  ( 1.347111479062088405E-15, 0.000000000000000000, 11.00000000000000000 ) ) ;
#3619=CARTESIAN_POINT ( 'NONE',  ( 0.000000000000000000, -1.399999999999998579, 0.000000000000000000 ) ) ;
#3652=CARTESIAN_POINT ( 'NONE',  ( -1.642778471874998480, -3.551041666188709645, 2.845375778867863303 ) ) ;
#3675=ORIENTED_EDGE ( 'NONE', *, *, #198470, .F. ) ;
#3680=EDGE_CURVE ( 'NONE', #71477, #169163, #189478, .T. ) ;
#3761=CARTESIAN_POINT ( 'NONE',  ( 0.000000000000000000, 2.999999999999999112, 10.25000000000000000 ) ) ;
#3838=CARTESIAN_POINT ( 'NONE',  ( 0.000000000000000000, 12.31951671548121219, 10.25000000000000000 ) ) ;
#3844=CARTESIAN_POINT ( 'NONE',  ( -3.287551290890295519, -0.1090402198146262214, -0.08054459095556501524 ) ) ;
#3853=PLANE ( 'NONE',  #118770 ) ;
#3868=PLANE ( 'NONE',  #156537 ) ;
#3878=CARTESIAN_POINT ( 'NONE',  ( 0.9311234436981545848, -1.459380368602566369, -3.474999999999999201 ) ) ;
#3985=VERTEX_POINT ( 'NONE', #80756 ) ;
#3989=CARTESIAN_POINT ( 'NONE',  ( 3.285556943749998737, -1.742708332855374076, -1.896917185911906722 ) ) ;
#4012=CARTESIAN_POINT ( 'NONE',  ( 1.642778471875001811, -3.842708332855375275, 2.845375778867859751 ) ) ;
#4044=DIRECTION ( 'NONE',  ( 0.000000000000000000, 0.000000000000000000, 1.000000000000000000 ) ) ;
#4055=CARTESIAN_POINT ( 'NONE',  ( -3.285556943749998737, -0.7802083328553744979, 1.896917185911908499 ) ) ;
#4088=EDGE_LOOP ( 'NONE', ( #114985, #53281, #184745, #68979 ) ) ;
#4118=CARTESIAN_POINT ( 'NONE',  ( -1.642778471875000035, -2.355208332855376341, -2.845375778867859751 ) ) ;
#4119=ORIENTED_EDGE ( 'NONE', *, *, #170395, .F. ) ;
#4203=CARTESIAN_POINT ( 'NONE',  ( 1.489652919843037271, -0.9674398443463784192, 3.089271823530293393 ) ) ;
#4262=ORIENTED_EDGE ( 'NONE', *, *, #73605, .F. ) ;
#4268=DIRECTION ( 'NONE',  ( 0.000000000000000000, 0.000000000000000000, -1.000000000000000000 ) ) ;
#4303=CARTESIAN_POINT ( 'NONE',  ( 1.642778471875000035, -1.976041666188709689, -2.845375778867859751 ) ) ;
#4309=B_SPLINE_CURVE_WITH_KNOTS ( 'NONE', 3,
 ( #211172, #199174, #116946, #212239, #98511, #197065, #196018, #82243, #114817, #50820, #62797, #133174, #128959, #112694, #63872, #214334, #148334, #12975 ),
 .UNSPECIFIED., .F., .F.,
 ( 4, 2, 2, 2, 2, 2, 2, 2, 4 ),
 ( 0.000000000000000000, 0.0006562923895199564888, 0.001312584779039912978, 0.001968877168559869575, 0.002625169558079825955, 0.003281461947599781902, 0.003937754337119737415, 0.004594046726639694662, 0.005250339116159651043 ),
 .UNSPECIFIED. ) ;
#4339=CARTESIAN_POINT ( 'NONE',  ( -3.475000000000000533, -2.450000000000000622, 0.000000000000000000 ) ) ;
#4346=CARTESIAN_POINT ( 'NONE',  ( -6.042630808230841359E-15, -1.968749999044084875, 3.474999999999999645 ) ) ;
#4431=FACE_OUTER_BOUND ( 'NONE', #192626, .T. ) ;
#4455=CARTESIAN_POINT ( 'NONE',  ( -3.419783357106924715, -0.02451629128698711024, -0.3994745426820112688 ) ) ;
#4595=CARTESIAN_POINT ( 'NONE',  ( 1.642778471875000035, -1.276041666188710400, -2.845375778867859751 ) ) ;
#4623=CARTESIAN_POINT ( 'NONE',  ( 0.000000000000000000, 0.5000000000000004441, 0.000000000000000000 ) ) ;
#4625=ORIENTED_EDGE ( 'NONE', *, *, #139916, .T. ) ;
#4628=CARTESIAN_POINT ( 'NONE',  ( -3.285556943750000070, -1.246874999522043392, 0.000000000000000000 ) ) ;
#4653=DIRECTION ( 'NONE',  ( -0.6483454320283800199, 0.000000000000000000, 0.7613463080411786432 ) ) ;
#4714=CARTESIAN_POINT ( 'NONE',  ( 0.000000000000000000, 2.499999999999998668, -4.500000000000000000 ) ) ;
#4716=CARTESIAN_POINT ( 'NONE',  ( 0.000000000000000000, -3.696874999522040017, -3.793834371823813001 ) ) ;
#4926=ORIENTED_EDGE ( 'NONE', *, *, #204566, .F. ) ;
#4968=FACE_OUTER_BOUND ( 'NONE', #66297, .T. ) ;
#4976=DIRECTION ( 'NONE',  ( 0.000000000000000000, 1.000000000000000000, 0.000000000000000000 ) ) ;
#5051=CARTESIAN_POINT ( 'NONE',  ( 1.642778471875000035, -1.013541666188708223, -2.845375778867859751 ) ) ;
#5106=AXIS2_PLACEMENT_3D ( 'NONE', #189443, #41086, #77818 ) ;
#5116=CARTESIAN_POINT ( 'NONE',  ( 1.001543065824772753E-15, -2.121874999522043836, 3.793834371823811669 ) ) ;
#5122=EDGE_CURVE ( 'NONE', #118628, #193157, #4309, .T. ) ;
#5177=CYLINDRICAL_SURFACE ( 'NONE', #54262, 9.999999999999998224 ) ;
#5181=CARTESIAN_POINT ( 'NONE',  ( 3.285556943749998737, -2.792708332855373676, -1.896917185911906500 ) ) ;
#5262=CARTESIAN_POINT ( 'NONE',  ( -4.124095526617549778E-13, -0.9769569599453676867, 3.449959810851647823 ) ) ;
#5365=CARTESIAN_POINT ( 'NONE',  ( -1.737500000000000266, -0.7583333333333330817, -3.009438278150923907 ) ) ;
#5520=CARTESIAN_POINT ( 'NONE',  ( -3.419492857000915986, -0.02754147205532485668, -0.3393126727284642152 ) ) ;
#5534=CARTESIAN_POINT ( 'NONE',  ( -1.500000000000039524, 7.128742170989512239, -10.89107411574799045 ) ) ;
#5559=VERTEX_POINT ( 'NONE', #210403 ) ;
#5586=AXIS2_PLACEMENT_3D ( 'NONE', #127407, #77494, #94839 ) ;
#5635=CARTESIAN_POINT ( 'NONE',  ( 1.642778471875001811, -2.530208332855374387, 2.845375778867859751 ) ) ;
#5655=ORIENTED_EDGE ( 'NONE', *, *, #51928, .T. ) ;
#5660=CARTESIAN_POINT ( 'NONE',  ( 1.642778471875000035, -1.626041666188710044, -2.845375778867859751 ) ) ;
#5682=ORIENTED_EDGE ( 'NONE', *, *, #30234, .F. ) ;
#5696=CARTESIAN_POINT ( 'NONE',  ( 0.000000000000000000, -0.2843749995220433702, -3.793834371823813001 ) ) ;
#5754=VERTEX_POINT ( 'NONE', #139730 ) ;
#5784=CARTESIAN_POINT ( 'NONE',  ( 3.285556943750000514, -3.813541666188710710, 1.896917185911906500 ) ) ;
#5817=AXIS2_PLACEMENT_3D ( 'NONE', #186095, #38795, #87549 ) ;
#5828=EDGE_LOOP ( 'NONE', ( #152679, #100768, #3675, #154947 ) ) ;
#5855=DIRECTION ( 'NONE',  ( -0.000000000000000000, 1.000000000000000000, -0.000000000000000000 ) ) ;
#5917=AXIS2_PLACEMENT_3D ( 'NONE', #126327, #75364, #27672 ) ;
#5925=CARTESIAN_POINT ( 'NONE',  ( -3.380278471875000523, -0.05468749976102194044, 0.000000000000000000 ) ) ;
#5998=VERTEX_POINT ( 'NONE', #211450 ) ;
#6066=DIRECTION ( 'NONE',  ( 0.000000000000000000, 0.000000000000000000, 1.000000000000000000 ) ) ;
#6077=ORIENTED_EDGE ( 'NONE', *, *, #64021, .T. ) ;
#6091=EDGE_CURVE ( 'NONE', #92865, #210464, #15508, .T. ) ;
#6103=EDGE_LOOP ( 'NONE', ( #150005, #196660 ) ) ;
#6195=CARTESIAN_POINT ( 'NONE',  ( 3.285556943749998737, -1.655208332855374609, -1.896917185911906500 ) ) ;
#6228=VERTEX_POINT ( 'NONE', #168049 ) ;
#6258=CARTESIAN_POINT ( 'NONE',  ( -3.285556943750000514, -3.026041666188709733, -1.896917185911906500 ) ) ;
#6336=EDGE_LOOP ( 'NONE', ( #159596, #69246, #49544, #120406, #150047, #16458 ) ) ;
#6344=CARTESIAN_POINT ( 'NONE',  ( 3.187124369784331002, -0.9488429814887938685, 1.145676217959502585 ) ) ;
#6421=AXIS2_PLACEMENT_3D ( 'NONE', #180734, #16076, #32361 ) ;
#6447=CARTESIAN_POINT ( 'NONE',  ( 1.642778471875000035, -3.376041666188708046, -2.845375778867859751 ) ) ;
#6526=ORIENTED_EDGE ( 'NONE', *, *, #214167, .T. ) ;
#6568=CARTESIAN_POINT ( 'NONE',  ( 0.000000000000000000, 0.06547992991065912372, 0.000000000000000000 ) ) ;
#6603=ORIENTED_EDGE ( 'NONE', *, *, #84346, .T. ) ;
#6684=DIRECTION ( 'NONE',  ( -0.000000000000000000, 0.000000000000000000, -1.000000000000000000 ) ) ;
#6701=CARTESIAN_POINT ( 'NONE',  ( 1.737499999999999378, -2.216666666666665453, -3.009438278150925683 ) ) ;
#6719=CARTESIAN_POINT ( 'NONE',  ( 3.285556943749998737, -1.042708332855377451, -1.896917185911906500 ) ) ;
#6770=DIRECTION ( 'NONE',  ( 0.000000000000000000, -1.000000000000000000, 0.000000000000000000 ) ) ;
#6774=DIRECTION ( 'NONE',  ( -0.000000000000000000, -1.000000000000000000, -0.000000000000000000 ) ) ;
#6775=CARTESIAN_POINT ( 'NONE',  ( 0.000000000000000000, -3.893749999044084031, -4.012584370867899430 ) ) ;
#6830=DIRECTION ( 'NONE',  ( 0.000000000000000000, -1.000000000000000000, 0.000000000000000000 ) ) ;
#6840=LINE ( 'NONE', #71840, #63138 ) ;
#6862=CARTESIAN_POINT ( 'NONE',  ( 1.642778471875001811, -2.792708332855376785, 2.845375778867859751 ) ) ;
#6897=DIRECTION ( 'NONE',  ( 0.000000000000000000, -1.000000000000000000, 0.000000000000000000 ) ) ;
#7000=EDGE_CURVE ( 'NONE', #24990, #89074, #8831, .T. ) ;
#7011=( BOUNDED_CURVE ( )  B_SPLINE_CURVE ( 2, ( #43130, #109246, #92943, #158988, #208779, #60409, #126570, #192530, #44184 ),
 .UNSPECIFIED., .F., .T. ) 
 B_SPLINE_CURVE_WITH_KNOTS ( ( 3, 2, 2, 2, 3 ),
 ( 0.3125000000000000000, 0.3194444444444444198, 0.3333333333333333148, 0.3472222222222222099, 0.3541666666666666852 ),
 .UNSPECIFIED. ) 
 CURVE ( )  GEOMETRIC_REPRESENTATION_ITEM ( )  RATIONAL_B_SPLINE_CURVE ( ( 0.9330127018922194093, 0.9330127018922194093, 1.000000000000000000, 0.8660254037844387076, 1.000000000000000000, 0.8660254037844387076, 1.000000000000000000, 0.9330127018922190762, 0.9330127018922194093 ) ) 
 REPRESENTATION_ITEM ( '' )  );
#7126=DIRECTION ( 'NONE',  ( -0.000000000000000000, -1.000000000000000000, -0.000000000000000000 ) ) ;
#7196=DIRECTION ( 'NONE',  ( -0.6483454320283799088, 0.000000000000000000, 0.7613463080411786432 ) ) ;
#7199=CARTESIAN_POINT ( 'NONE',  ( -1.642778471874998480, -1.888541666188708890, 2.845375778867863303 ) ) ;
#7256=VERTEX_POINT ( 'NONE', #165749 ) ;
#7263=CARTESIAN_POINT ( 'NONE',  ( 1.001543065824772753E-15, -3.171874999522042327, 3.793834371823811669 ) ) ;
#7325=VERTEX_POINT ( 'NONE', #118126 ) ;
#7328=CARTESIAN_POINT ( 'NONE',  ( 1.001543065824772753E-15, -3.609374999522044547, 3.793834371823811669 ) ) ;
#7408=ORIENTED_EDGE ( 'NONE', *, *, #41018, .F. ) ;
#7448=CIRCLE ( 'NONE', #159615, 3.432849766368862632 ) ;
#7483=CARTESIAN_POINT ( 'NONE',  ( 1.642778471875000035, -0.5760416661887077794, -2.845375778867859751 ) ) ;
#7518=CARTESIAN_POINT ( 'NONE',  ( 0.000000000000000000, -3.696874999522040017, -3.793834371823813001 ) ) ;
#7554=CARTESIAN_POINT ( 'NONE',  ( 0.000000000000000000, 6.999999999999999112, -11.00000000000000000 ) ) ;
#7595=VERTEX_POINT ( 'NONE', #117056 ) ;
#7661=CARTESIAN_POINT ( 'NONE',  ( 0.3967682513765422581, -3.073437234850263433, 3.444363204092072195 ) ) ;
#7790=CARTESIAN_POINT ( 'NONE',  ( -3.285556943750000514, -1.276041666188709511, -1.896917185911906500 ) ) ;
#7851=CARTESIAN_POINT ( 'NONE',  ( 1.642778471875000035, -2.063541666188710266, -2.845375778867859751 ) ) ;
#7876=EDGE_CURVE ( 'NONE', #94296, #212297, #196117, .T. ) ;
#7902=CARTESIAN_POINT ( 'NONE',  ( 0.000000000000000000, 5.000000000000000888, -11.00000000000000000 ) ) ;
#7911=AXIS2_PLACEMENT_3D ( 'NONE', #110446, #85061, #176448 ) ;
#7941=CARTESIAN_POINT ( 'NONE',  ( 3.285556943750000514, -3.463541666188707957, 1.896917185911906500 ) ) ;
#7976=CARTESIAN_POINT ( 'NONE',  ( -1.177606547106018198, -3.137449485356257561, 3.183006684848862733 ) ) ;
#8029=CARTESIAN_POINT ( 'NONE',  ( 3.475000000000000533, -1.254166666666665098, 2.006292185433948827 ) ) ;
#8103=PRODUCT_CONTEXT ( 'NONE', #141817, 'mechanical' ) ;
#8111=CARTESIAN_POINT ( 'NONE',  ( -3.475000000000000533, -0.6854166657107528815, -2.006292185433948827 ) ) ;
#8279=CARTESIAN_POINT ( 'NONE',  ( 3.475000000000000533, -2.202083332377416713, -2.006292185433951047 ) ) ;
#8347=CARTESIAN_POINT ( 'NONE',  ( 3.285556943750000514, -3.813541666188710710, 1.896917185911906500 ) ) ;
#8406=CARTESIAN_POINT ( 'NONE',  ( -3.285556943750000514, -3.376041666188708490, -1.896917185911906500 ) ) ;
#8434=DIRECTION ( 'NONE',  ( 0.000000000000000000, 0.000000000000000000, 1.000000000000000000 ) ) ;
#8491=CARTESIAN_POINT ( 'NONE',  ( 0.4437927792854980402, -0.8979896776215845478, -3.297249098415093282 ) ) ;
#8500=ADVANCED_FACE ( 'NONE', ( #44395 ), #96127, .F. ) ;
#8503=FACE_OUTER_BOUND ( 'NONE', #85978, .T. ) ;
#8553=FACE_OUTER_BOUND ( 'NONE', #10677, .T. ) ;
#8560=CARTESIAN_POINT ( 'NONE',  ( -1.642778471874998480, -0.7510416661887092671, 2.845375778867863303 ) ) ;
#8595=CARTESIAN_POINT ( 'NONE',  ( 2.960183410750786059, -4.109567543049581495, -1.425552035297093623 ) ) ;
#8596=CARTESIAN_POINT ( 'NONE',  ( -6.042630808230841359E-15, -1.662500000000000533, 3.474999999999999645 ) ) ;
#8722=CARTESIAN_POINT ( 'NONE',  ( -1.499999999999960476, 6.999999999999999112, 10.89724735885168982 ) ) ;
#8809=CARTESIAN_POINT ( 'NONE',  ( 1.737500000000001155, -2.639583332377418046, 3.009438278150922130 ) ) ;
#8831=LINE ( 'NONE', #74908, #60216 ) ;
#8869=CARTESIAN_POINT ( 'NONE',  ( 1.001543065824772753E-15, -1.159374999522043481, 3.793834371823811669 ) ) ;
#8877=CARTESIAN_POINT ( 'NONE',  ( 1.500000000000035971, 7.750000000000000000, 10.86128356754324109 ) ) ;
#8903=ORIENTED_EDGE ( 'NONE', *, *, #141806, .F. ) ;
#8926=CARTESIAN_POINT ( 'NONE',  ( -1.642778471874998480, -2.588541666188707957, 2.845375778867863303 ) ) ;
#8941=CARTESIAN_POINT ( 'NONE',  ( 1.737500000000001155, -3.033333333333332327, 3.009438278150922130 ) ) ;
#8952=CARTESIAN_POINT ( 'NONE',  ( -1.020158943445720556, -3.232243495192077987, 3.126638183162731899 ) ) ;
#8995=CARTESIAN_POINT ( 'NONE',  ( 0.000000000000000000, 0.5000000000000004441, 0.000000000000000000 ) ) ;
#9022=CARTESIAN_POINT ( 'NONE',  ( 3.475000000000000533, -2.304166666666668473, 2.006292185433948827 ) ) ;
#9059=CARTESIAN_POINT ( 'NONE',  ( -2.200353596358113339, -3.182436278638796523, 2.524625639462166671 ) ) ;
#9111=CARTESIAN_POINT ( 'NONE',  ( -3.475000000000000533, -1.779166666666666785, -2.006292185433948827 ) ) ;
#9157=CARTESIAN_POINT ( 'NONE',  ( 0.000000000000000000, 0.5000000000000004441, 0.000000000000000000 ) ) ;
#9187=CARTESIAN_POINT ( 'NONE',  ( 0.000000000000000000, -0.3937499990440834763, -4.012584370867899430 ) ) ;
#9195=CARTESIAN_POINT ( 'NONE',  ( 1.499999999999959588, 6.999999999999999112, -10.89724735885168805 ) ) ;
#9209=EDGE_CURVE ( 'NONE', #142998, #75662, #83746, .T. ) ;
#9345=CARTESIAN_POINT ( 'NONE',  ( 0.000000000000000000, 6.999999999999999112, 0.000000000000000000 ) ) ;
#9421=CARTESIAN_POINT ( 'NONE',  ( 0.000000000000000000, -2.296874999522042327, -3.793834371823813001 ) ) ;
#9483=CARTESIAN_POINT ( 'NONE',  ( 3.285556943750000514, -3.901041666188710177, 1.896917185911906500 ) ) ;
#9505=DIRECTION ( 'NONE',  ( 0.7613463080411785322, -0.000000000000000000, 0.6483454320283801309 ) ) ;
#9564=CARTESIAN_POINT ( 'NONE',  ( 2.055513515747692921, -0.9138922176956919552, -2.615695235488095349 ) ) ;
#9586=ORIENTED_EDGE ( 'NONE', *, *, #71473, .T. ) ;
#9640=DIRECTION ( 'NONE',  ( 0.000000000000000000, -1.000000000000000000, 0.000000000000000000 ) ) ;
#9664=CARTESIAN_POINT ( 'NONE',  ( -3.285556943750000514, -3.988541666188710089, -1.896917185911906500 ) ) ;
#9763=CARTESIAN_POINT ( 'NONE',  ( 2.550000000000000266, 2.499999999999998668, 1.849324200890695824 ) ) ;
#9768=EDGE_CURVE ( 'NONE', #193157, #142998, #159977, .T. ) ;
#9776=ADVANCED_FACE ( 'NONE', ( #174025 ), #151965, .F. ) ;
#9847=DIRECTION ( 'NONE',  ( 1.224646799147353454E-16, 0.000000000000000000, -1.000000000000000000 ) ) ;
#9937=CARTESIAN_POINT ( 'NONE',  ( 0.000000000000000000, -2.384374999522042238, -3.793834371823813001 ) ) ;
#9969=VERTEX_POINT ( 'NONE', #191225 ) ;
#9988=ORIENTED_EDGE ( 'NONE', *, *, #175486, .T. ) ;
#9991=CARTESIAN_POINT ( 'NONE',  ( 1.642778471875001811, -2.880208332855377584, 2.845375778867859751 ) ) ;
#10041=CARTESIAN_POINT ( 'NONE',  ( 4.163088478618747692E-16, 0.06547992991065912372, 3.399419719642636561 ) ) ;
#10083=CARTESIAN_POINT ( 'NONE',  ( -1.737499999999997824, -0.9916666666666684726, 3.009438278150925683 ) ) ;
#10119=ORIENTED_EDGE ( 'NONE', *, *, #97268, .F. ) ;
#10154=DIRECTION ( 'NONE',  ( -0.000000000000000000, 1.000000000000000000, -0.000000000000000000 ) ) ;
#10173=CARTESIAN_POINT ( 'NONE',  ( 3.475000000000000533, -1.604166666666667629, 2.006292185433948827 ) ) ;
#10219=LINE ( 'NONE', #155410, #99204 ) ;
#10245=CARTESIAN_POINT ( 'NONE',  ( 3.475000000000000533, -1.181249999044085897, 0.000000000000000000 ) ) ;
#10280=EDGE_CURVE ( 'NONE', #187973, #85130, #834, .T. ) ;
#10286=ORIENTED_EDGE ( 'NONE', *, *, #171577, .T. ) ;
#10409=CARTESIAN_POINT ( 'NONE',  ( 3.475000000000000533, -1.924999999999999600, 0.000000000000000000 ) ) ;
#10412=CARTESIAN_POINT ( 'NONE',  ( -1.642778471874998480, -2.938541666188707602, 2.845375778867863303 ) ) ;
#10473=CARTESIAN_POINT ( 'NONE',  ( -1.642778471874998480, -3.551041666188709645, 2.845375778867863303 ) ) ;
#10537=CARTESIAN_POINT ( 'NONE',  ( 3.285556943750000070, -0.6343749995220415716, 0.000000000000000000 ) ) ;
#10677=EDGE_LOOP ( 'NONE', ( #9586, #187528, #32539, #130158 ) ) ;
#10723=CARTESIAN_POINT ( 'NONE',  ( 3.475000000000000533, -2.654166666666666785, 2.006292185433948827 ) ) ;
#10735=B_SPLINE_CURVE_WITH_KNOTS ( 'NONE', 3,
 ( #114074, #1276, #195249, #49005 ),
 .UNSPECIFIED., .F., .F.,
 ( 4, 4 ),
 ( 0.000000000000000000, 0.0001207671576358290770 ),
 .UNSPECIFIED. ) ;
#10760=LINE ( 'NONE', #76834, #202916 ) ;
#10807=VERTEX_POINT ( 'NONE', #90850 ) ;
#10817=ADVANCED_FACE ( 'NONE', ( #8503 ), #110742, .T. ) ;
#10841=PLANE ( 'NONE',  #30498 ) ;
#10843=CARTESIAN_POINT ( 'NONE',  ( 1.249999999999964695, 8.500000000000000000, -9.921567416492218072 ) ) ;
#10920=CARTESIAN_POINT ( 'NONE',  ( -1.416652131158683492, 8.000043606524068096, -10.86080395187256187 ) ) ;
#10959=LINE ( 'NONE', #77034, #67322 ) ;
#10978=CARTESIAN_POINT ( 'NONE',  ( 1.001543065824772753E-15, -1.421874999522042327, 3.793834371823811669 ) ) ;
#10991=CARTESIAN_POINT ( 'NONE',  ( -1.642778471874998480, -2.938541666188707602, 2.845375778867863303 ) ) ;
#11047=CARTESIAN_POINT ( 'NONE',  ( 3.285556943750000070, -3.171874999522043215, 0.000000000000000000 ) ) ;
#11054=AXIS2_PLACEMENT_3D ( 'NONE', #125554, #122371, #73513 ) ;
#11079=ORIENTED_EDGE ( 'NONE', *, *, #66779, .T. ) ;
#11098=DIRECTION ( 'NONE',  ( 1.000000000000000000, 0.000000000000000000, -1.224646799147353207E-16 ) ) ;
#11140=CARTESIAN_POINT ( 'NONE',  ( -1.737500000000000266, -0.7583333333333330817, -3.009438278150923907 ) ) ;
#11163=EDGE_LOOP ( 'NONE', ( #117885, #9988 ) ) ;
#11192=EDGE_LOOP ( 'NONE', ( #61149, #16527, #181946, #91125, #63396, #130380, #156162, #137227, #149617, #195284 ) ) ;
#11202=ORIENTED_EDGE ( 'NONE', *, *, #86135, .F. ) ;
#11235=CARTESIAN_POINT ( 'NONE',  ( 1.001543065824772753E-15, -2.362500000000001155, 4.012584370867899430 ) ) ;
#11272=LINE ( 'NONE', #176992, #139528 ) ;
#11307=CARTESIAN_POINT ( 'NONE',  ( -1.737499999999997824, -1.297916665710750150, 3.009438278150925683 ) ) ;
#11366=DIRECTION ( 'NONE',  ( -0.000000000000000000, -1.000000000000000000, -0.000000000000000000 ) ) ;
#11394=CARTESIAN_POINT ( 'NONE',  ( -3.285556943750000070, -0.4593749995220435256, 0.000000000000000000 ) ) ;
#11401=DIRECTION ( 'NONE',  ( -0.000000000000000000, -1.000000000000000000, -0.000000000000000000 ) ) ;
#11448=( BOUNDED_CURVE ( )  B_SPLINE_CURVE ( 3, ( #45548, #44480, #144145, #190693 ),
 .UNSPECIFIED., .F., .T. ) 
 B_SPLINE_CURVE_WITH_KNOTS ( ( 4, 4 ),
 ( 4.837716811552755125, 4.862957253161376059 ),
 .UNSPECIFIED. ) 
 CURVE ( )  GEOMETRIC_REPRESENTATION_ITEM ( )  RATIONAL_B_SPLINE_CURVE ( ( 1.000000000000000000, 0.9999469107135832147, 0.9999469107135832147, 1.000000000000000000 ) ) 
 REPRESENTATION_ITEM ( '' )  );
#11547=CARTESIAN_POINT ( 'NONE',  ( -1.642778471875000035, -3.667708332855373676, -2.845375778867859751 ) ) ;
#11606=CARTESIAN_POINT ( 'NONE',  ( -1.642778471874998480, -0.7510416661887092671, 2.845375778867863303 ) ) ;
#11629=FACE_OUTER_BOUND ( 'NONE', #2552, .T. ) ;
#11752=CARTESIAN_POINT ( 'NONE',  ( -3.285556943750000070, -1.509374999522042238, 0.000000000000000000 ) ) ;
#11768=CARTESIAN_POINT ( 'NONE',  ( 0.000000000000000000, 8.500000000000000000, 0.000000000000000000 ) ) ;
#11790=CARTESIAN_POINT ( 'NONE',  ( -3.475000000000000533, -2.479166666666667851, -2.006292185433948827 ) ) ;
#11849=DIRECTION ( 'NONE',  ( 0.000000000000000000, -1.000000000000000000, 0.000000000000000000 ) ) ;
#11945=CARTESIAN_POINT ( 'NONE',  ( -1.393942678861017415, 1.000000000000001332, 1.636894562288534694 ) ) ;
#12055=CARTESIAN_POINT ( 'NONE',  ( 1.642778471875001811, -1.392708332855374653, 2.845375778867859751 ) ) ;
#12122=CARTESIAN_POINT ( 'NONE',  ( 1.001543065824772753E-15, -2.559374999522041172, 3.793834371823811669 ) ) ;
#12134=VERTEX_POINT ( 'NONE', #206297 ) ;
#12174=DIRECTION ( 'NONE',  ( -0.000000000000000000, -1.000000000000000000, -0.000000000000000000 ) ) ;
#12214=CARTESIAN_POINT ( 'NONE',  ( 3.475000000000000533, -1.924999999999999600, 0.000000000000000000 ) ) ;
#12230=FACE_OUTER_BOUND ( 'NONE', #214105, .T. ) ;
#12234=VERTEX_POINT ( 'NONE', #124087 ) ;
#12281=CARTESIAN_POINT ( 'NONE',  ( 3.285556943750000514, -3.113541666188709645, 1.896917185911906722 ) ) ;
#12298=CARTESIAN_POINT ( 'NONE',  ( 3.475000000000000533, -0.8750000000000007772, 0.000000000000000000 ) ) ;
#12372=CARTESIAN_POINT ( 'NONE',  ( -1.737500000000000266, -1.764583332377417380, -3.009438278150923907 ) ) ;
#12413=VERTEX_POINT ( 'NONE', #155185 ) ;
#12527=EDGE_CURVE ( 'NONE', #89074, #55892, #134968, .T. ) ;
#12539=CYLINDRICAL_SURFACE ( 'NONE', #100355, 2.750000000000000444 ) ;
#12541=DIRECTION ( 'NONE',  ( 0.000000000000000000, 1.000000000000000000, 0.000000000000000000 ) ) ;
#12603=FACE_OUTER_BOUND ( 'NONE', #6103, .T. ) ;
#12666=CARTESIAN_POINT ( 'NONE',  ( 0.000000000000000000, -1.246874999522042948, -3.793834371823813001 ) ) ;
#12809=CARTESIAN_POINT ( 'NONE',  ( 3.285556943750000514, -2.763541666188707335, 1.896917185911906500 ) ) ;
#12842=VERTEX_POINT ( 'NONE', #209226 ) ;
#12847=CARTESIAN_POINT ( 'NONE',  ( 3.475000000000000533, -1.574999999999999956, 0.000000000000000000 ) ) ;
#12852=PRESENTATION_STYLE_ASSIGNMENT (( #49640 ) ) ;
#12890=CARTESIAN_POINT ( 'NONE',  ( 4.255647627037052709E-16, 0.5000000000000004441, 3.475000000000000089 ) ) ;
#12913=CARTESIAN_POINT ( 'NONE',  ( 1.642778471875000035, -1.013541666188708223, -2.845375778867859751 ) ) ;
#12914=CARTESIAN_POINT ( 'NONE',  ( -2.306635926208834508, -3.112620303657281262, -2.512400949369866687 ) ) ;
#12975=CARTESIAN_POINT ( 'NONE',  ( -3.246376473470825363, -0.8887487162375362626, 0.5058895364790267912 ) ) ;
#13091=DIRECTION ( 'NONE',  ( 0.000000000000000000, 1.000000000000000000, 0.000000000000000000 ) ) ;
#13117=CARTESIAN_POINT ( 'NONE',  ( -3.285556943750000070, -0.8093749995220431703, 0.000000000000000000 ) ) ;
#13166=VERTEX_POINT ( 'NONE', #175703 ) ;
#13172=B_SPLINE_CURVE_WITH_KNOTS ( 'NONE', 3,
 ( #80272, #145323, #146370, #48851 ),
 .UNSPECIFIED., .F., .F.,
 ( 4, 4 ),
 ( 0.01196238986099508982, 0.01242187503699302212 ),
 .UNSPECIFIED. ) ;
#13188=DIRECTION ( 'NONE',  ( 0.000000000000000000, 0.000000000000000000, 1.000000000000000000 ) ) ;
#13192=CARTESIAN_POINT ( 'NONE',  ( 3.285556943749998737, -3.492708332855374742, -1.896917185911906500 ) ) ;
#13210=ORIENTED_EDGE ( 'NONE', *, *, #102718, .T. ) ;
#13231=EDGE_CURVE ( 'NONE', #71477, #92865, #179495, .T. ) ;
#13290=CARTESIAN_POINT ( 'NONE',  ( 1.737500000000001155, -0.9333333333333346804, 3.009438278150922130 ) ) ;
#13310=ORIENTED_EDGE ( 'NONE', *, *, #98482, .T. ) ;
#13316=AXIS2_PLACEMENT_3D ( 'NONE', #40178, #150741, #2303 ) ;
#13336=ORIENTED_EDGE ( 'NONE', *, *, #133615, .T. ) ;
#13358=CARTESIAN_POINT ( 'NONE',  ( 3.285556943749998737, -3.055208332855376518, -1.896917185911906722 ) ) ;
#13375=CARTESIAN_POINT ( 'NONE',  ( 0.000000000000000000, -3.237499999999997602, -4.012584370867899430 ) ) ;
#13447=CARTESIAN_POINT ( 'NONE',  ( 0.000000000000000000, -2.143749999044084031, -4.012584370867899430 ) ) ;
#13474=EDGE_CURVE ( 'NONE', #153164, #85478, #13570, .T. ) ;
#13481=CARTESIAN_POINT ( 'NONE',  ( -1.250000000000001110, 8.500000000000000000, 3.469446951953614189E-15 ) ) ;
#13487=ORIENTED_EDGE ( 'NONE', *, *, #16746, .T. ) ;
#13492=EDGE_LOOP ( 'NONE', ( #27564, #4625 ) ) ;
#13506=CARTESIAN_POINT ( 'NONE',  ( -1.347971487989957070E-14, -2.712500000000000355, 3.475000000000000089 ) ) ;
#13570=CIRCLE ( 'NONE', #169119, 9.999999999999998224 ) ;
#13611=FACE_OUTER_BOUND ( 'NONE', #35884, .T. ) ;
#13632=EDGE_LOOP ( 'NONE', ( #203770, #51156, #134911, #86054 ) ) ;
#13653=( GEOMETRIC_REPRESENTATION_CONTEXT ( 3 ) GLOBAL_UNCERTAINTY_ASSIGNED_CONTEXT ( ( #115795 ) ) GLOBAL_UNIT_ASSIGNED_CONTEXT ( ( #164460, #179652, #78927 ) ) REPRESENTATION_CONTEXT ( 'NONE', 'WORKASPACE' ) );
#13655=LINE ( 'NONE', #80805, #79084 ) ;
#13726=CARTESIAN_POINT ( 'NONE',  ( -3.475000000000000533, -2.785416665710751527, -2.006292185433948827 ) ) ;
#13734=ORIENTED_EDGE ( 'NONE', *, *, #174269, .T. ) ;
#13737=CARTESIAN_POINT ( 'NONE',  ( -1.642778471875000035, -1.917708332855375897, -2.845375778867859751 ) ) ;
#13765=CIRCLE ( 'NONE', #172896, 9.999999999999996447 ) ;
#13784=FACE_OUTER_BOUND ( 'NONE', #171293, .T. ) ;
#13791=CARTESIAN_POINT ( 'NONE',  ( -1.782949938078045138, -1.600000000000000755, 2.093702347113242102 ) ) ;
#13834=DIRECTION ( 'NONE',  ( 0.000000000000000000, 1.000000000000000000, 0.000000000000000000 ) ) ;
#13877=CARTESIAN_POINT ( 'NONE',  ( 3.285556943750000070, -1.684374999522043836, 0.000000000000000000 ) ) ;
#13913=CARTESIAN_POINT ( 'NONE',  ( 0.000000000000000000, -1.837499999999999911, -4.012584370867899430 ) ) ;
#13976=CARTESIAN_POINT ( 'NONE',  ( 3.285556943749998737, -0.3427083328553764408, -1.896917185911906500 ) ) ;
#13979=CARTESIAN_POINT ( 'NONE',  ( -1.250000000000039302, 8.500000000000000000, -10.85702537530423228 ) ) ;
#13983=DIRECTION ( 'NONE',  ( 0.000000000000000000, 0.000000000000000000, 1.000000000000000000 ) ) ;
#14112=FACE_OUTER_BOUND ( 'NONE', #195776, .T. ) ;
#14166=CARTESIAN_POINT ( 'NONE',  ( 3.285556943750000514, -0.6635416661887083567, 1.896917185911906500 ) ) ;
#14241=ORIENTED_EDGE ( 'NONE', *, *, #65049, .T. ) ;
#14248=ORIENTED_EDGE ( 'NONE', *, *, #40321, .F. ) ;
#14253=AXIS2_PLACEMENT_3D ( 'NONE', #57190, #58255, #123350 ) ;
#14289=FACE_OUTER_BOUND ( 'NONE', #11192, .T. ) ;
#14295=CARTESIAN_POINT ( 'NONE',  ( -3.475000000000000533, -1.750000000000001554, 0.000000000000000000 ) ) ;
#14307=CARTESIAN_POINT ( 'NONE',  ( 1.258396710555287346, -3.152325552749383863, -3.126779214646796756 ) ) ;
#14328=DIRECTION ( 'NONE',  ( -0.9486832980505139901, -0.3162277660168373861, 3.312310031615527941E-15 ) ) ;
#14340=CARTESIAN_POINT ( 'NONE',  ( 1.737500000000001155, -3.383333333333331971, 3.009438278150922130 ) ) ;
#14358=LINE ( 'NONE', #111955, #147339 ) ;
#14410=CARTESIAN_POINT ( 'NONE',  ( 3.475000000000000533, -2.931249999044084120, 0.000000000000000000 ) ) ;
#14427=CARTESIAN_POINT ( 'NONE',  ( -1.737500000000000266, -3.908333333333333215, -3.009438278150923907 ) ) ;
#14431=ADVANCED_FACE ( 'NONE', ( #97757 ), #196305, .T. ) ;
#14501=CARTESIAN_POINT ( 'NONE',  ( 1.001543065824772753E-15, -3.368749999044086341, 4.012584370867899430 ) ) ;
#14538=EDGE_CURVE ( 'NONE', #108029, #12234, #23454, .T. ) ;
#14589=CARTESIAN_POINT ( 'NONE',  ( 1.001543065824772753E-15, -0.7218749995220414828, 3.793834371823811669 ) ) ;
#14797=CARTESIAN_POINT ( 'NONE',  ( 1.642778471875000035, -2.326041666188709112, -2.845375778867859751 ) ) ;
#14807=CARTESIAN_POINT ( 'NONE',  ( 3.796405077356793438E-16, -0.5000000000000005551, -3.099999999999999201 ) ) ;
#14870=CARTESIAN_POINT ( 'NONE',  ( -1.249999999999946487, 8.500000000000000000, 15.75000000000000000 ) ) ;
#14933=CARTESIAN_POINT ( 'NONE',  ( 3.285556943749998737, -3.055208332855376518, -1.896917185911906500 ) ) ;
#14972=CARTESIAN_POINT ( 'NONE',  ( -1.737499999999997824, -2.041666666666667407, 3.009438278150925683 ) ) ;
#14975=CARTESIAN_POINT ( 'NONE',  ( 1.642778471875001811, -0.3427083328553758301, 2.845375778867859751 ) ) ;
#15043=CARTESIAN_POINT ( 'NONE',  ( 1.642778471875001811, -0.7802083328553761632, 2.845375778867859751 ) ) ;
#15064=( BOUNDED_CURVE ( )  B_SPLINE_CURVE ( 2, ( #189731, #155119, #6701, #87975, #72778, #203828, #57613, #56548, #106412 ),
 .UNSPECIFIED., .F., .T. ) 
 B_SPLINE_CURVE_WITH_KNOTS ( ( 3, 2, 2, 2, 3 ),
 ( 0.5208333333333333703, 0.5277777777777777901, 0.5416666666666666297, 0.5555555555555555802, 0.5625000000000000000 ),
 .UNSPECIFIED. ) 
 CURVE ( )  GEOMETRIC_REPRESENTATION_ITEM ( )  RATIONAL_B_SPLINE_CURVE ( ( 0.9330127018922192983, 0.9330127018922198534, 1.000000000000000000, 0.8660254037844387076, 1.000000000000000000, 0.8660254037844387076, 1.000000000000000000, 0.9330127018922194093, 0.9330127018922194093 ) ) 
 REPRESENTATION_ITEM ( '' )  );
#15166=FACE_OUTER_BOUND ( 'NONE', #55996, .T. ) ;
#15184=DIRECTION ( 'NONE',  ( -0.000000000000000000, 1.000000000000000000, -0.000000000000000000 ) ) ;
#15202=DIRECTION ( 'NONE',  ( 0.000000000000000000, 0.7071067811865445751, 0.7071067811865504593 ) ) ;
#15215=ADVANCED_FACE ( 'NONE', ( #64952 ), #133201, .F. ) ;
#15241=CARTESIAN_POINT ( 'NONE',  ( -3.285556943750000070, -0.1093749995220438809, 0.000000000000000000 ) ) ;
#15286=AXIS2_PLACEMENT_3D ( 'NONE', #179695, #180746, #164503 ) ;
#15310=CARTESIAN_POINT ( 'NONE',  ( -3.285556943750000070, -4.046874999522040106, 0.000000000000000000 ) ) ;
#15337=EDGE_LOOP ( 'NONE', ( #6526, #108769, #61261, #64234 ) ) ;
#15360=CARTESIAN_POINT ( 'NONE',  ( 1.394453263437886604E-15, -1.312499999999999556, 3.474999999999999645 ) ) ;
#15375=CARTESIAN_POINT ( 'NONE',  ( 3.166866847460915846, -3.204376093797748126, 0.9919409734452371286 ) ) ;
#15391=DIRECTION ( 'NONE',  ( 0.000000000000000000, -1.000000000000000000, 0.000000000000000000 ) ) ;
#15393=CARTESIAN_POINT ( 'NONE',  ( -3.421712537580930302, -0.02252155983199216616, -0.4161442326466053832 ) ) ;
#15405=CARTESIAN_POINT ( 'NONE',  ( 3.475000000000000533, -2.654166666666666785, 2.006292185433948827 ) ) ;
#15423=PLANE ( 'NONE',  #119867 ) ;
#15508=CIRCLE ( 'NONE', #32850, 2.150000000000000799 ) ;
#15559=ORIENTED_EDGE ( 'NONE', *, *, #197651, .F. ) ;
#15563=CARTESIAN_POINT ( 'NONE',  ( 1.737500000000001155, -3.339583332377417335, 3.009438278150922130 ) ) ;
#15655=CARTESIAN_POINT ( 'NONE',  ( 3.285556943750000514, -2.763541666188707335, 1.896917185911906500 ) ) ;
#15698=LINE ( 'NONE', #81783, #153700 ) ;
#15732=CARTESIAN_POINT ( 'NONE',  ( -0.8683822406226825441, -0.9819185891646172726, 3.363299488115865543 ) ) ;
#15780=EDGE_CURVE ( 'NONE', #134989, #76889, #171673, .T. ) ;
#15800=EDGE_CURVE ( 'NONE', #211199, #42744, #188990, .T. ) ;
#15858=CARTESIAN_POINT ( 'NONE',  ( 1.001543065824772753E-15, -2.471874999522041705, 3.793834371823811669 ) ) ;
#15866=ORIENTED_EDGE ( 'NONE', *, *, #21052, .F. ) ;
#15973=AXIS2_PLACEMENT_3D ( 'NONE', #161683, #65206, #28465 ) ;
#15998=CARTESIAN_POINT ( 'NONE',  ( 3.285556943749998737, -1.655208332855374609, -1.896917185911906500 ) ) ;
#16042=CARTESIAN_POINT ( 'NONE',  ( 1.001543065824772753E-15, -2.909374999522043925, 3.793834371823811669 ) ) ;
#16076=DIRECTION ( 'NONE',  ( 0.000000000000000000, 1.000000000000000000, 0.000000000000000000 ) ) ;
#16102=CARTESIAN_POINT ( 'NONE',  ( 0.000000000000000000, 6.999999999999999112, 0.000000000000000000 ) ) ;
#16106=CARTESIAN_POINT ( 'NONE',  ( 3.285556943750000070, -0.7218749995220423710, 0.000000000000000000 ) ) ;
#16110=DIRECTION ( 'NONE',  ( 0.000000000000000000, 1.000000000000000000, 0.000000000000000000 ) ) ;
#16269=CARTESIAN_POINT ( 'NONE',  ( -3.365144920186191158, -0.9421578975231510444, 0.09679790593341147664 ) ) ;
#16288=CIRCLE ( 'NONE', #147763, 9.999999999999998224 ) ;
#16297=CARTESIAN_POINT ( 'NONE',  ( 1.001543065824772753E-15, -1.771874999522040861, 3.793834371823811669 ) ) ;
#16329=FACE_OUTER_BOUND ( 'NONE', #174362, .T. ) ;
#16369=FACE_OUTER_BOUND ( 'NONE', #173976, .T. ) ;
#16422=DIRECTION ( 'NONE',  ( -0.000000000000000000, -1.000000000000000000, -0.000000000000000000 ) ) ;
#16456=LINE ( 'NONE', #149686, #92926 ) ;
#16458=ORIENTED_EDGE ( 'NONE', *, *, #202477, .F. ) ;
#16467=CARTESIAN_POINT ( 'NONE',  ( -3.475000000000000533, -2.829166666666666607, -2.006292185433948827 ) ) ;
#16527=ORIENTED_EDGE ( 'NONE', *, *, #68847, .T. ) ;
#16536=CARTESIAN_POINT ( 'NONE',  ( 3.475000000000000533, -2.960416665710750905, 2.006292185433948827 ) ) ;
#16567=CARTESIAN_POINT ( 'NONE',  ( 1.001543065824772753E-15, -0.4593749995220425819, 3.793834371823811669 ) ) ;
#16592=CARTESIAN_POINT ( 'NONE',  ( -3.475000000000000533, -1.035416665710751527, -2.006292185433948827 ) ) ;
#16628=CARTESIAN_POINT ( 'NONE',  ( 0.000000000000000000, -3.193749999044083410, -4.012584370867899430 ) ) ;
#16653=CARTESIAN_POINT ( 'NONE',  ( 3.475000000000000533, -1.574999999999999956, 0.000000000000000000 ) ) ;
#16715=CARTESIAN_POINT ( 'NONE',  ( 1.001543065824772753E-15, -2.121874999522043836, 3.793834371823811669 ) ) ;
#16746=EDGE_CURVE ( 'NONE', #184334, #107993, #107683, .T. ) ;
#16791=CARTESIAN_POINT ( 'NONE',  ( -4.124095526617549778E-13, -0.9769569599453676867, 3.449959810851647823 ) ) ;
#16835=VERTEX_POINT ( 'NONE', #144429 ) ;
#16919=CARTESIAN_POINT ( 'NONE',  ( 3.285556943750000514, -3.813541666188710710, 1.896917185911906500 ) ) ;
#16950=AXIS2_PLACEMENT_3D ( 'NONE', #49609, #23225, #155385 ) ;
#17068=CARTESIAN_POINT ( 'NONE',  ( -3.285556943750000514, -3.988541666188710089, -1.896917185911906500 ) ) ;
#17107=CARTESIAN_POINT ( 'NONE',  ( 3.475000000000000533, -3.295833333333334725, -2.006292185433951047 ) ) ;
#17109=CARTESIAN_POINT ( 'NONE',  ( -1.642778471875000035, -0.1677083328553742592, -2.845375778867859751 ) ) ;
#17177=CARTESIAN_POINT ( 'NONE',  ( 1.642778471875001811, -2.180208332855374742, 2.845375778867859751 ) ) ;
#17337=CARTESIAN_POINT ( 'NONE',  ( -3.305895513212903758, -0.9091400625591844475, 0.2125217450545698883 ) ) ;
#17341=CARTESIAN_POINT ( 'NONE',  ( -1.685698123273788429, -1.399999999999998579, 1.979500400907064916 ) ) ;
#17364=CARTESIAN_POINT ( 'NONE',  ( 1.642778471875000035, -2.326041666188709112, -2.845375778867859751 ) ) ;
#17394=FACE_OUTER_BOUND ( 'NONE', #51817, .T. ) ;
#17500=CARTESIAN_POINT ( 'NONE',  ( 3.105163759955598124, -3.206389149015671514, 1.164969029660678723 ) ) ;
#17516=CARTESIAN_POINT ( 'NONE',  ( 0.000000000000000000, 6.999999999999999112, 0.000000000000000000 ) ) ;
#17526=CARTESIAN_POINT ( 'NONE',  ( 1.737499999999999378, -3.266666666666667496, -3.009438278150925683 ) ) ;
#17563=CARTESIAN_POINT ( 'NONE',  ( 1.500000000000035971, 7.750000000000000000, 10.86128356754324109 ) ) ;
#17579=EDGE_LOOP ( 'NONE', ( #26005, #112210, #5682 ) ) ;
#17617=CARTESIAN_POINT ( 'NONE',  ( 3.475000000000000533, -3.354166666666667851, 2.006292185433948827 ) ) ;
#17656=CARTESIAN_POINT ( 'NONE',  ( 3.285556943750000514, -1.363541666188708978, 1.896917185911906722 ) ) ;
#17688=CARTESIAN_POINT ( 'NONE',  ( -3.475000000000000533, -3.135416665710750284, -2.006292185433948827 ) ) ;
#17746=CARTESIAN_POINT ( 'NONE',  ( -1.737500000000000266, -1.108333333333332726, -3.009438278150923907 ) ) ;
#17774=CARTESIAN_POINT ( 'NONE',  ( 3.285556943750000514, -1.363541666188709423, 1.896917185911906500 ) ) ;
#17805=EDGE_CURVE ( 'NONE', #80335, #137341, #82775, .T. ) ;
#17969=DIRECTION ( 'NONE',  ( -0.000000000000000000, 1.000000000000000000, -0.000000000000000000 ) ) ;
#17975=CARTESIAN_POINT ( 'NONE',  ( -3.283337425626721373, -0.1112512837626866702, -0.1207467602163218856 ) ) ;
#17983=CARTESIAN_POINT ( 'NONE',  ( -3.285556943749998737, -3.930208332855377407, 1.896917185911908499 ) ) ;
#18051=AXIS2_PLACEMENT_3D ( 'NONE', #147015, #48446, #180553 ) ;
#18134=CARTESIAN_POINT ( 'NONE',  ( 0.000000000000000000, -0.4374999999999981126, -4.012584370867899430 ) ) ;
#18179=CARTESIAN_POINT ( 'NONE',  ( -3.475000000000000533, -3.179166666666664476, -2.006292185433948827 ) ) ;
#18181=CARTESIAN_POINT ( 'NONE',  ( 1.642778471875000035, -4.163541666188708135, -2.845375778867859751 ) ) ;
#18246=CARTESIAN_POINT ( 'NONE',  ( -3.285556943750000070, -1.946874999522042682, 0.000000000000000000 ) ) ;
#18325=ORIENTED_EDGE ( 'NONE', *, *, #43314, .T. ) ;
#18333=CIRCLE ( 'NONE', #139433, 11.00000000000000000 ) ;
#18413=CARTESIAN_POINT ( 'NONE',  ( -3.246376473470825363, -0.8887487162375362626, 0.5058895364790267912 ) ) ;
#18415=ADVANCED_FACE ( 'NONE', ( #165811, #17394 ), #83478, .F. ) ;
#18424=LINE ( 'NONE', #167886, #192563 ) ;
#18443=CARTESIAN_POINT ( 'NONE',  ( -3.285556943750000514, -2.938541666188710266, -1.896917185911906500 ) ) ;
#18473=DIRECTION ( 'NONE',  ( -0.6483454320283799088, 0.000000000000000000, 0.7613463080411786432 ) ) ;
#18529=CARTESIAN_POINT ( 'NONE',  ( 1.394453263437886604E-15, -1.268749999044084253, 3.474999999999999645 ) ) ;
#18597=CARTESIAN_POINT ( 'NONE',  ( -3.424195918967509300, -0.02093306995252190369, -0.4190893571287980235 ) ) ;
#18600=EDGE_LOOP ( 'NONE', ( #207545, #73144, #119964, #103176 ) ) ;
#18608=CARTESIAN_POINT ( 'NONE',  ( 2.665787487727776295, -3.982249430249628297, -2.473491247225932721 ) ) ;
#18729=CARTESIAN_POINT ( 'NONE',  ( 0.000000000000000000, -1.596874999522041705, -3.793834371823813445 ) ) ;
#18764=CARTESIAN_POINT ( 'NONE',  ( 3.285556943750000514, -1.101041666188710355, 1.896917185911906500 ) ) ;
#18816=DIRECTION ( 'NONE',  ( -0.6483454320283799088, 0.000000000000000000, 0.7613463080411786432 ) ) ;
#18825=AXIS2_PLACEMENT_3D ( 'NONE', #109823, #99627, #210433 ) ;
#18851=CARTESIAN_POINT ( 'NONE',  ( -3.285556943750000514, -1.538541666188708357, -1.896917185911906500 ) ) ;
#18896=CARTESIAN_POINT ( 'NONE',  ( 0.000000000000000000, 8.500000000000000000, 0.000000000000000000 ) ) ;
#18945=ORIENTED_EDGE ( 'NONE', *, *, #67226, .F. ) ;
#18997=EDGE_CURVE ( 'NONE', #155561, #12134, #69849, .T. ) ;
#19013=CARTESIAN_POINT ( 'NONE',  ( 0.000000000000000000, 0.06547992991065912372, -3.399419719642636561 ) ) ;
#19060=CARTESIAN_POINT ( 'NONE',  ( 3.285556943750000514, -2.763541666188707335, 1.896917185911906500 ) ) ;
#19113=PLANE ( 'NONE',  #48041 ) ;
#19186=CARTESIAN_POINT ( 'NONE',  ( -3.474999999999997868, -2.070833333333331971, 2.006292185433951047 ) ) ;
#19211=CARTESIAN_POINT ( 'NONE',  ( 1.737500000000001155, -0.5833333333333314830, 3.009438278150922130 ) ) ;
#19243=CARTESIAN_POINT ( 'NONE',  ( 0.000000000000000000, 0.000000000000000000, 0.000000000000000000 ) ) ;
#19255=CARTESIAN_POINT ( 'NONE',  ( -1.642778471875000035, -1.917708332855375897, -2.845375778867859751 ) ) ;
#19306=EDGE_CURVE ( 'NONE', #73220, #64997, #37227, .T. ) ;
#19320=CARTESIAN_POINT ( 'NONE',  ( 3.285556943749998737, -1.742708332855374076, -1.896917185911906500 ) ) ;
#19444=EDGE_CURVE ( 'NONE', #25653, #136464, #85545, .T. ) ;
#19477=CARTESIAN_POINT ( 'NONE',  ( -3.354001786068215196, -0.9357451212759041459, 0.07218384636315192115 ) ) ;
#19487=DIRECTION ( 'NONE',  ( -3.491481338843133750E-15, -0.000000000000000000, -1.000000000000000000 ) ) ;
#19506=CARTESIAN_POINT ( 'NONE',  ( 1.001543065824772753E-15, -2.821874999522044458, 3.793834371823811669 ) ) ;
#19538=EDGE_LOOP ( 'NONE', ( #202696, #107130, #73533, #161399 ) ) ;
#19550=CARTESIAN_POINT ( 'NONE',  ( -3.475000000000000533, -2.056249999044083232, 0.000000000000000000 ) ) ;
#19665=CARTESIAN_POINT ( 'NONE',  ( -3.421390767332295635, -0.02279856766746886365, -0.4144453184043222493 ) ) ;
#19747=DIRECTION ( 'NONE',  ( 0.000000000000000000, -0.000000000000000000, -1.000000000000000000 ) ) ;
#19801=CARTESIAN_POINT ( 'NONE',  ( 3.285556943750000070, -1.684374999522043836, 0.000000000000000000 ) ) ;
#19835=CARTESIAN_POINT ( 'NONE',  ( 1.737499999999999378, -3.922916665710749040, -3.009438278150925683 ) ) ;
#19896=CARTESIAN_POINT ( 'NONE',  ( -3.475000000000000533, -1.079166666666665941, -2.006292185433948827 ) ) ;
#19922=CARTESIAN_POINT ( 'NONE',  ( -3.285556943749998737, -3.230208332855375897, 1.896917185911908499 ) ) ;
#20123=CARTESIAN_POINT ( 'NONE',  ( 3.285556943750000514, -3.113541666188709645, 1.896917185911906500 ) ) ;
#20137=FACE_OUTER_BOUND ( 'NONE', #45275, .T. ) ;
#20147=VECTOR ( 'NONE', #91990, 1000.000000000000227 ) ;
#20202=EDGE_CURVE ( 'NONE', #153466, #93052, #113307, .T. ) ;
#20254=CARTESIAN_POINT ( 'NONE',  ( 0.000000000000000000, -0.9843749995220403282, -3.793834371823813445 ) ) ;
#20264=DIRECTION ( 'NONE',  ( 1.000000000000000000, 0.000000000000000000, 0.000000000000000000 ) ) ;
#20272=ORIENTED_EDGE ( 'NONE', *, *, #198939, .T. ) ;
#20278=CARTESIAN_POINT ( 'NONE',  ( 0.000000000000000000, -0.7875000000000005329, -4.012584370867899430 ) ) ;
#20320=CARTESIAN_POINT ( 'NONE',  ( -3.475000000000000533, -3.499999999999999556, 0.000000000000000000 ) ) ;
#20322=CARTESIAN_POINT ( 'NONE',  ( 1.642778471875000035, -0.9260416661887073131, -2.845375778867859751 ) ) ;
#20385=CARTESIAN_POINT ( 'NONE',  ( -1.642778471874998480, -2.238541666188708312, 2.845375778867863303 ) ) ;
#20432=CARTESIAN_POINT ( 'NONE',  ( 1.347111479062088405E-15, 5.000000000000000888, 11.00000000000000000 ) ) ;
#20473=EDGE_CURVE ( 'NONE', #54700, #167113, #124617, .T. ) ;
#20536=DIRECTION ( 'NONE',  ( 0.000000000000000000, -1.000000000000000000, 0.000000000000000000 ) ) ;
#20570=CARTESIAN_POINT ( 'NONE',  ( 0.000000000000000000, -1.946874999522044014, -3.793834371823813001 ) ) ;
#20853=CARTESIAN_POINT ( 'NONE',  ( -3.285556943749998737, -2.180208332855376518, 1.896917185911908721 ) ) ;
#20885=CARTESIAN_POINT ( 'NONE',  ( 3.130865767068502503, -4.306442547369423224, -1.507748171479097010 ) ) ;
#20972=ADVANCED_FACE ( 'NONE', ( #94186 ), #131138, .F. ) ;
#20974=CARTESIAN_POINT ( 'NONE',  ( 3.285556943750000514, -3.113541666188709645, 1.896917185911906500 ) ) ;
#21026=ORIENTED_EDGE ( 'NONE', *, *, #20473, .F. ) ;
#21042=AXIS2_PLACEMENT_3D ( 'NONE', #185030, #52913, #68064 ) ;
#21052=EDGE_CURVE ( 'NONE', #12842, #65209, #3014, .T. ) ;
#21103=DIRECTION ( 'NONE',  ( 1.000000000000000000, 0.000000000000000000, -0.000000000000000000 ) ) ;
#21135=CIRCLE ( 'NONE', #114623, 3.475000000000000089 ) ;
#21257=AXIS2_PLACEMENT_3D ( 'NONE', #185622, #106578, #205069 ) ;
#21279=EDGE_CURVE ( 'NONE', #7325, #102958, #59367, .T. ) ;
#21307=CARTESIAN_POINT ( 'NONE',  ( -3.285556943750000070, -1.246874999522043392, 0.000000000000000000 ) ) ;
#21309=ADVANCED_FACE ( 'NONE', ( #190882, #108651 ), #106853, .F. ) ;
#21330=CARTESIAN_POINT ( 'NONE',  ( -3.285556943750000514, -3.638541666188706891, -1.896917185911906500 ) ) ;
#21362=CYLINDRICAL_SURFACE ( 'NONE', #35653, 3.475000000000000089 ) ;
#21373=CARTESIAN_POINT ( 'NONE',  ( 1.642778471875000035, -1.626041666188710044, -2.845375778867859751 ) ) ;
#21433=CARTESIAN_POINT ( 'NONE',  ( -3.285556943750000514, -1.626041666188708046, -1.896917185911906500 ) ) ;
#21614=CARTESIAN_POINT ( 'NONE',  ( -3.475000000000000533, 0.000000000000000000, 0.000000000000000000 ) ) ;
#21703=ORIENTED_EDGE ( 'NONE', *, *, #146654, .F. ) ;
#21785=CARTESIAN_POINT ( 'NONE',  ( -1.500000000000039302, 7.564371094685074404, -10.87018506808106899 ) ) ;
#21863=ADVANCED_FACE ( 'NONE', ( #157902 ), #207135, .F. ) ;
#21888=CARTESIAN_POINT ( 'NONE',  ( 1.642778471875001811, -1.830208332855375097, 2.845375778867859751 ) ) ;
#21911=CARTESIAN_POINT ( 'NONE',  ( -1.642778471874998480, -1.801041666188708090, 2.845375778867863303 ) ) ;
#21944=CARTESIAN_POINT ( 'NONE',  ( -1.737500000000000266, -3.864583332377418579, -3.009438278150923907 ) ) ;
#21969=CARTESIAN_POINT ( 'NONE',  ( -0.5942495929466964366, -3.232243495192077098, 3.244776806288057980 ) ) ;
#22034=CARTESIAN_POINT ( 'NONE',  ( 3.285556943749998737, -3.405208332855374831, -1.896917185911906500 ) ) ;
#22158=AXIS2_PLACEMENT_3D ( 'NONE', #195117, #110734, #212405 ) ;
#22166=AXIS2_PLACEMENT_3D ( 'NONE', #156619, #11401, #205334 ) ;
#22298=EDGE_CURVE ( 'NONE', #142643, #5559, #60371, .T. ) ;
#22324=VERTEX_POINT ( 'NONE', #14807 ) ;
#22347=VERTEX_POINT ( 'NONE', #213006 ) ;
#22378=CARTESIAN_POINT ( 'NONE',  ( 1.642778471875001811, -1.480208332855375453, 2.845375778867859751 ) ) ;
#22379=FACE_OUTER_BOUND ( 'NONE', #81214, .T. ) ;
#22444=CARTESIAN_POINT ( 'NONE',  ( -3.285556943750000514, -1.538541666188708357, -1.896917185911906500 ) ) ;
#22475=ORIENTED_EDGE ( 'NONE', *, *, #17805, .F. ) ;
#22508=CARTESIAN_POINT ( 'NONE',  ( -3.285556943750000070, -4.046874999522040106, 0.000000000000000000 ) ) ;
#22660=CARTESIAN_POINT ( 'NONE',  ( -3.285556943750000070, -0.1093749995220438809, 0.000000000000000000 ) ) ;
#22693=CARTESIAN_POINT ( 'NONE',  ( 1.001543065824772753E-15, -0.2624999999999988454, 4.012584370867899430 ) ) ;
#22815=FACE_OUTER_BOUND ( 'NONE', #160969, .T. ) ;
#22887=ORIENTED_EDGE ( 'NONE', *, *, #97582, .F. ) ;
#22905=CARTESIAN_POINT ( 'NONE',  ( -1.499999999999963141, 7.750000000000000000, 10.86128356754324820 ) ) ;
#22928=DIRECTION ( 'NONE',  ( 0.000000000000000000, 0.000000000000000000, -1.000000000000000000 ) ) ;
#22966=CARTESIAN_POINT ( 'NONE',  ( 3.285556943750000514, -2.501041666188708046, 1.896917185911906500 ) ) ;
#23008=CIRCLE ( 'NONE', #150924, 4.500000000000000000 ) ;
#23025=CARTESIAN_POINT ( 'NONE',  ( -3.285556943750000514, -0.5760416661887087786, -1.896917185911906500 ) ) ;
#23047=CARTESIAN_POINT ( 'NONE',  ( -2.900957617708239678, -3.232243495192087757, 1.542507481629953103 ) ) ;
#23096=ADVANCED_FACE ( 'NONE', ( #107877 ), #186561, .T. ) ;
#23110=DIRECTION ( 'NONE',  ( 0.000000000000000000, -1.000000000000000000, 0.000000000000000000 ) ) ;
#23112=CARTESIAN_POINT ( 'NONE',  ( 0.000000000000000000, -0.08749999999999961975, -4.012584370867899430 ) ) ;
#23222=CARTESIAN_POINT ( 'NONE',  ( -3.475000000000000533, -1.356249999044083943, 0.000000000000000000 ) ) ;
#23225=DIRECTION ( 'NONE',  ( -0.7613463080411786432, 0.000000000000000000, -0.6483454320283800199 ) ) ;
#23277=CARTESIAN_POINT ( 'NONE',  ( 1.500000000000053291, 7.750000000000000000, 15.74999999999999289 ) ) ;
#23287=VECTOR ( 'NONE', #113715, 1000.000000000000000 ) ;
#23289=( BOUNDED_CURVE ( )  B_SPLINE_CURVE ( 2, ( #183035, #181960, #99661, #66058, #115971, #114909, #192071, #148426, #33589 ),
 .UNSPECIFIED., .F., .T. ) 
 B_SPLINE_CURVE_WITH_KNOTS ( ( 3, 2, 2, 2, 3 ),
 ( 0.6041666666666667407, 0.6111111111111111605, 0.6250000000000000000, 0.6388888888888888395, 0.6458333333333333703 ),
 .UNSPECIFIED. ) 
 CURVE ( )  GEOMETRIC_REPRESENTATION_ITEM ( )  RATIONAL_B_SPLINE_CURVE ( ( 0.9330127018922192983, 0.9330127018922198534, 1.000000000000000000, 0.8660254037844387076, 1.000000000000000000, 0.8660254037844387076, 1.000000000000000000, 0.9330127018922187432, 0.9330127018922192983 ) ) 
 REPRESENTATION_ITEM ( '' )  );
#23407=CIRCLE ( 'NONE', #61468, 2.750000000000000444 ) ;
#23452=CARTESIAN_POINT ( 'NONE',  ( 1.642778471875001811, -1.130208332855375808, 2.845375778867859751 ) ) ;
#23454=B_SPLINE_CURVE_WITH_KNOTS ( 'NONE', 3,
 ( #133469, #147562, #199472, #181111, #48995, #134530, #116173, #200536, #182159, #100918, #151826, #33789, #47951, #82536, #51114, #114065, #117239, #52182, #213583, #167006, #180057, #32729, #18597, #84676, #115115, #131359, #118307, #98809, #184294, #31679, #163815, #35919, #101995, #168063, #15393, #19665, #38068, #153952, #4455, #86811, #169123, #5520, #187501, #91100, #73758, #204796 ),
 .UNSPECIFIED., .F., .F.,
 ( 4, 3, 3, 3, 3, 3, 3, 3, 3, 3, 3, 3, 3, 3, 3, 4 ),
 ( 0.000000000000000000, 0.0002001208021641467678, 0.0002987350495539372935, 0.0003974608682140796023, 0.0004175935870586608640, 0.0004226419832867753202, 0.0004238941922970896193, 0.0004244411037539569343, 0.0004249975721417096437, 0.0004254804695417831119, 0.0004261174966295773058, 0.0004273003274780872687, 0.0004324025126211059077, 0.0004525445321848968277, 0.0005326990625275228493, 0.0005514034162145647726 ),
 .UNSPECIFIED. ) ;
#23523=CARTESIAN_POINT ( 'NONE',  ( 3.285556943749998737, -2.005208332855377140, -1.896917185911906500 ) ) ;
#23551=CIRCLE ( 'NONE', #189467, 0.09999999999999982514 ) ;
#23585=CARTESIAN_POINT ( 'NONE',  ( -3.285556943749998737, -3.317708332855375808, 1.896917185911908499 ) ) ;
#23602=CARTESIAN_POINT ( 'NONE',  ( 1.250000000000033973, 8.500000000000000000, 9.921567416492207414 ) ) ;
#23740=CARTESIAN_POINT ( 'NONE',  ( 3.285556943750000070, -0.9843749995220412163, 0.000000000000000000 ) ) ;
#23742=EDGE_CURVE ( 'NONE', #114098, #88263, #200308, .T. ) ;
#23776=CARTESIAN_POINT ( 'NONE',  ( 1.001543065824772753E-15, -0.9624999999999998002, 4.012584370867899430 ) ) ;
#23958=CARTESIAN_POINT ( 'NONE',  ( -3.475000000000000533, -2.406249999044082877, 0.000000000000000000 ) ) ;
#23982=CARTESIAN_POINT ( 'NONE',  ( 3.475000000000000533, -2.552083332377419023, -2.006292185433951047 ) ) ;
#23991=FACE_OUTER_BOUND ( 'NONE', #71003, .T. ) ;
#23995=CYLINDRICAL_SURFACE ( 'NONE', #26274, 3.475000000000000089 ) ;
#24001=DIRECTION ( 'NONE',  ( -0.000000000000000000, -1.000000000000000000, -0.000000000000000000 ) ) ;
#24021=ADVANCED_FACE ( 'NONE', ( #111080 ), #207279, .T. ) ;
#24042=CARTESIAN_POINT ( 'NONE',  ( 0.000000000000000000, -2.034374999522043481, -3.793834371823813001 ) ) ;
#24101=CARTESIAN_POINT ( 'NONE',  ( 1.642778471875000035, -3.113541666188709200, -2.845375778867859751 ) ) ;
#24109=VERTEX_POINT ( 'NONE', #65430 ) ;
#24122=ADVANCED_FACE ( 'NONE', ( #131580 ), #132628, .T. ) ;
#24141=ORIENTED_EDGE ( 'NONE', *, *, #135864, .F. ) ;
#24183=CARTESIAN_POINT ( 'NONE',  ( 1.737499999999999378, -0.1166666666666676955, -3.009438278150925683 ) ) ;
#24248=LINE ( 'NONE', #153207, #152810 ) ;
#24296=DIRECTION ( 'NONE',  ( -0.000000000000000000, -1.000000000000000000, -0.000000000000000000 ) ) ;
#24344=CARTESIAN_POINT ( 'NONE',  ( -1.737499999999997824, -0.9479166657107505056, 3.009438278150925683 ) ) ;
#24404=CARTESIAN_POINT ( 'NONE',  ( 1.394453263437886604E-15, -1.618749999044085230, 3.474999999999999645 ) ) ;
#24522=CARTESIAN_POINT ( 'NONE',  ( 1.001543065824772753E-15, -1.859374999522040550, 3.793834371823810780 ) ) ;
#24541=VERTEX_POINT ( 'NONE', #213809 ) ;
#24590=CARTESIAN_POINT ( 'NONE',  ( 1.642778471875001811, -3.842708332855375275, 2.845375778867859751 ) ) ;
#24651=CARTESIAN_POINT ( 'NONE',  ( -1.642778471875000035, -0.1677083328553742592, -2.845375778867859751 ) ) ;
#24668=ADVANCED_FACE ( 'NONE', ( #171490 ), #155249, .T. ) ;
#24756=DIRECTION ( 'NONE',  ( 0.000000000000000000, -1.000000000000000000, 0.000000000000000000 ) ) ;
#24777=ORIENTED_EDGE ( 'NONE', *, *, #9768, .F. ) ;
#24780=CARTESIAN_POINT ( 'NONE',  ( 0.000000000000000000, -0.02876672507444791305, 0.000000000000000000 ) ) ;
#24805=CARTESIAN_POINT ( 'NONE',  ( -3.285556943750000070, -0.4593749995220435256, 0.000000000000000000 ) ) ;
#24844=CARTESIAN_POINT ( 'NONE',  ( 3.475000000000000533, -0.8458333333333335480, -2.006292185433951047 ) ) ;
#24990=VERTEX_POINT ( 'NONE', #20432 ) ;
#25009=ORIENTED_EDGE ( 'NONE', *, *, #171577, .F. ) ;
#25018=EDGE_CURVE ( 'NONE', #128202, #134989, #96774, .T. ) ;
#25026=CARTESIAN_POINT ( 'NONE',  ( 4.408728476930470165E-16, -0.5000000000000004441, -3.599999999999999201 ) ) ;
#25029=DIRECTION ( 'NONE',  ( -0.000000000000000000, 1.000000000000000000, -0.000000000000000000 ) ) ;
#25035=CARTESIAN_POINT ( 'NONE',  ( -3.380278471875000523, -0.05468749976102194044, 0.000000000000000000 ) ) ;
#25045=ORIENTED_EDGE ( 'NONE', *, *, #97858, .F. ) ;
#25116=CARTESIAN_POINT ( 'NONE',  ( 1.642778471875000035, -1.013541666188708223, -2.845375778867859751 ) ) ;
#25167=DIRECTION ( 'NONE',  ( 0.7613463080411785322, -0.000000000000000000, 0.6483454320283801309 ) ) ;
#25177=CARTESIAN_POINT ( 'NONE',  ( -3.285556943750000514, -2.326041666188709112, -1.896917185911906500 ) ) ;
#25190=CARTESIAN_POINT ( 'NONE',  ( 3.475000000000000533, -2.974999999999998312, 0.000000000000000000 ) ) ;
#25240=AXIS2_PLACEMENT_3D ( 'NONE', #83612, #199480, #180066 ) ;
#25242=CYLINDRICAL_SURFACE ( 'NONE', #59573, 3.475000000000000089 ) ;
#25267=CARTESIAN_POINT ( 'NONE',  ( 3.475000000000000533, -2.245833333333331350, -2.006292185433951047 ) ) ;
#25355=CARTESIAN_POINT ( 'NONE',  ( -1.737499999999997824, -1.691666666666667762, 3.009438278150925683 ) ) ;
#25376=CARTESIAN_POINT ( 'NONE',  ( -3.474999999999997868, -1.327083332377416713, 2.006292185433951047 ) ) ;
#25427=CARTESIAN_POINT ( 'NONE',  ( -3.475000000000000533, -0.3062499990440850639, 0.000000000000000000 ) ) ;
#25591=CARTESIAN_POINT ( 'NONE',  ( 1.737500000000001155, -2.289583332377418401, 3.009438278150922130 ) ) ;
#25595=CARTESIAN_POINT ( 'NONE',  ( 3.285556943750000514, -2.501041666188708046, 1.896917185911906722 ) ) ;
#25603=AXIS2_PLACEMENT_3D ( 'NONE', #93759, #7126, #173952 ) ;
#25652=CIRCLE ( 'NONE', #15286, 3.099999999999999201 ) ;
#25653=VERTEX_POINT ( 'NONE', #211978 ) ;
#25658=ADVANCED_FACE ( 'NONE', ( #13784 ), #129773, .T. ) ;
#25660=CARTESIAN_POINT ( 'NONE',  ( 1.642778471875000035, -2.676041666188708756, -2.845375778867859751 ) ) ;
#25723=CARTESIAN_POINT ( 'NONE',  ( -1.642778471874998480, -0.4010416661887096224, 2.845375778867863303 ) ) ;
#25742=CARTESIAN_POINT ( 'NONE',  ( 1.523611765266693396, 0.5999999999999998668, -1.789163823896769978 ) ) ;
#25829=DIRECTION ( 'NONE',  ( 0.000000000000000000, 0.000000000000000000, 1.000000000000000000 ) ) ;
#25908=CARTESIAN_POINT ( 'NONE',  ( -3.475000000000000533, -0.3791666666666649865, -2.006292185433948827 ) ) ;
#25941=ORIENTED_EDGE ( 'NONE', *, *, #211412, .F. ) ;
#26005=ORIENTED_EDGE ( 'NONE', *, *, #53239, .T. ) ;
#26134=ORIENTED_EDGE ( 'NONE', *, *, #181495, .F. ) ;
#26184=CARTESIAN_POINT ( 'NONE',  ( 3.285556943750000070, -1.071874999522042016, 0.000000000000000000 ) ) ;
#26236=ORIENTED_EDGE ( 'NONE', *, *, #72841, .F. ) ;
#26238=CARTESIAN_POINT ( 'NONE',  ( 3.285556943749998737, -2.792708332855373676, -1.896917185911906500 ) ) ;
#26266=AXIS2_PLACEMENT_3D ( 'NONE', #85266, #53846, #170788 ) ;
#26274=AXIS2_PLACEMENT_3D ( 'NONE', #155088, #138848, #122680 ) ;
#26315=EDGE_CURVE ( 'NONE', #85478, #104308, #32492, .T. ) ;
#26331=CARTESIAN_POINT ( 'NONE',  ( 0.000000000000000000, -1.137499999999999067, -4.012584370867899430 ) ) ;
#26360=CIRCLE ( 'NONE', #40300, 2.400000000000000799 ) ;
#26402=CIRCLE ( 'NONE', #126845, 3.475000000000000089 ) ;
#26422=CARTESIAN_POINT ( 'NONE',  ( -1.737500000000000266, -2.158333333333331439, -3.009438278150923907 ) ) ;
#26563=EDGE_CURVE ( 'NONE', #137341, #101274, #118073, .T. ) ;
#26587=CARTESIAN_POINT ( 'NONE',  ( -1.642778471874998480, -0.4010416661887096224, 2.845375778867863303 ) ) ;
#26638=ORIENTED_EDGE ( 'NONE', *, *, #99699, .F. ) ;
#26639=VECTOR ( 'NONE', #92054, 1000.000000000000000 ) ;
#26667=CARTESIAN_POINT ( 'NONE',  ( -3.285556943750000514, -2.676041666188707424, -1.896917185911906722 ) ) ;
#26731=CARTESIAN_POINT ( 'NONE',  ( -3.285556943750000514, -3.638541666188706891, -1.896917185911906500 ) ) ;
#26791=CARTESIAN_POINT ( 'NONE',  ( 3.285556943749998737, -0.6052083328553753416, -1.896917185911906500 ) ) ;
#26797=CARTESIAN_POINT ( 'NONE',  ( 0.000000000000000000, 5.000000000000000888, 0.000000000000000000 ) ) ;
#26863=ADVANCED_FACE ( 'NONE', ( #109293 ), #73363, .T. ) ;
#26936=CARTESIAN_POINT ( 'NONE',  ( 0.000000000000000000, -0.8968749995220406390, -3.793834371823813001 ) ) ;
#26975=CARTESIAN_POINT ( 'NONE',  ( 3.475000000000000533, -1.954166666666666163, 2.006292185433948827 ) ) ;
#27011=AXIS2_PLACEMENT_3D ( 'NONE', #9345, #155602, #58096 ) ;
#27071=CIRCLE ( 'NONE', #125074, 0.1000000000000000333 ) ;
#27090=ADVANCED_FACE ( 'NONE', ( #176358 ), #156922, .T. ) ;
#27104=CARTESIAN_POINT ( 'NONE',  ( 1.333477130264982380, 8.249568609204944281, -9.911050286642574036 ) ) ;
#27165=CARTESIAN_POINT ( 'NONE',  ( -6.042630808230841359E-15, -2.318749999044084298, 3.474999999999999645 ) ) ;
#27202=ORIENTED_EDGE ( 'NONE', *, *, #71349, .F. ) ;
#27240=VERTEX_POINT ( 'NONE', #124494 ) ;
#27248=CARTESIAN_POINT ( 'NONE',  ( 1.001543065824772753E-15, -3.609374999522044547, 3.793834371823811669 ) ) ;
#27306=CARTESIAN_POINT ( 'NONE',  ( 3.285556943750000514, -2.501041666188708046, 1.896917185911906500 ) ) ;
#27389=CARTESIAN_POINT ( 'NONE',  ( 0.000000000000000000, 0.5000000000000004441, 0.000000000000000000 ) ) ;
#27404=CARTESIAN_POINT ( 'NONE',  ( -3.475000000000000533, -1.750000000000001554, 0.000000000000000000 ) ) ;
#27494=CARTESIAN_POINT ( 'NONE',  ( 3.475000000000000533, -1.924999999999999600, 0.000000000000000000 ) ) ;
#27564=ORIENTED_EDGE ( 'NONE', *, *, #66694, .T. ) ;
#27568=CARTESIAN_POINT ( 'NONE',  ( 3.475000000000000533, -0.8020833323774190227, -2.006292185433951047 ) ) ;
#27672=DIRECTION ( 'NONE',  ( 0.6483454320283799088, 0.000000000000000000, -0.7613463080411786432 ) ) ;
#27718=ORIENTED_EDGE ( 'NONE', *, *, #18997, .T. ) ;
#27743=CARTESIAN_POINT ( 'NONE',  ( -1.642778471875000035, -2.355208332855376341, -2.845375778867859751 ) ) ;
#27805=CARTESIAN_POINT ( 'NONE',  ( 1.642778471875001811, -3.492708332855375630, 2.845375778867859751 ) ) ;
#27828=DIRECTION ( 'NONE',  ( -0.6483454320283800199, 0.000000000000000000, 0.7613463080411786432 ) ) ;
#27867=CARTESIAN_POINT ( 'NONE',  ( -3.285556943749998737, -0.7802083328553744979, 1.896917185911908499 ) ) ;
#27985=ORIENTED_EDGE ( 'NONE', *, *, #167881, .T. ) ;
#28015=CARTESIAN_POINT ( 'NONE',  ( 3.285556943750000514, -1.363541666188709423, 1.896917185911906500 ) ) ;
#28033=CONICAL_SURFACE ( 'NONE', #14253, 3.000000000000000000, 0.7853981633974523868 ) ;
#28034=DIRECTION ( 'NONE',  ( 0.000000000000000000, 1.000000000000000000, 0.000000000000000000 ) ) ;
#28057=CARTESIAN_POINT ( 'NONE',  ( 1.737500000000001155, -2.333333333333333037, 3.009438278150922130 ) ) ;
#28119=CARTESIAN_POINT ( 'NONE',  ( -3.383843058911719215, -3.076622456046647969, 0.6547969591862352612 ) ) ;
#28242=FACE_OUTER_BOUND ( 'NONE', #174602, .T. ) ;
#28313=CARTESIAN_POINT ( 'NONE',  ( 3.285556943750000514, -1.363541666188709423, 1.896917185911906500 ) ) ;
#28383=CARTESIAN_POINT ( 'NONE',  ( 1.642778471875001811, -2.530208332855374387, 2.845375778867859751 ) ) ;
#28438=CARTESIAN_POINT ( 'NONE',  ( 0.000000000000000000, -1.500000000000001332, 0.000000000000000000 ) ) ;
#28465=DIRECTION ( 'NONE',  ( 3.491481338843133355E-15, 0.000000000000000000, 1.000000000000000000 ) ) ;
#28476=EDGE_LOOP ( 'NONE', ( #173645, #138257, #162010, #128864, #71602, #67861 ) ) ;
#28478=CARTESIAN_POINT ( 'NONE',  ( -1.737500000000000266, -1.808333333333332016, -3.009438278150923907 ) ) ;
#28504=DIRECTION ( 'NONE',  ( -0.000000000000000000, -1.000000000000000000, -0.000000000000000000 ) ) ;
#28573=CARTESIAN_POINT ( 'NONE',  ( 3.475000000000000533, -2.654166666666666785, 2.006292185433948827 ) ) ;
#28646=CARTESIAN_POINT ( 'NONE',  ( -3.474999999999998312, -1.677083332377419023, 2.006292185433951047 ) ) ;
#28659=LINE ( 'NONE', #84592, #40504 ) ;
#28755=DIRECTION ( 'NONE',  ( 0.000000000000000000, 1.000000000000000000, 0.000000000000000000 ) ) ;
#28815=CARTESIAN_POINT ( 'NONE',  ( 1.642778471875000035, -2.763541666188709556, -2.845375778867859751 ) ) ;
#28838=CARTESIAN_POINT ( 'NONE',  ( -6.042630808230841359E-15, -1.968749999044084875, 3.474999999999999645 ) ) ;
#28867=COLOUR_RGB ( '', 0.40784314, 0.44705882, 0.49803922) ;
#28878=CARTESIAN_POINT ( 'NONE',  ( -1.642778471875000035, -2.967708332855374831, -2.845375778867859751 ) ) ;
#28913=EDGE_LOOP ( 'NONE', ( #3607, #6077, #149219, #136596, #24777 ) ) ;
#28938=ORIENTED_EDGE ( 'NONE', *, *, #40321, .T. ) ;
#28941=CARTESIAN_POINT ( 'NONE',  ( -3.285556943750000070, -1.859374999522041882, 0.000000000000000000 ) ) ;
#29015=EDGE_CURVE ( 'NONE', #24109, #113311, #23289, .T. ) ;
#29089=CARTESIAN_POINT ( 'NONE',  ( 0.000000000000000000, -2.646874999522040639, -3.793834371823813001 ) ) ;
#29124=CARTESIAN_POINT ( 'NONE',  ( 3.475000000000000533, -2.595833333333334103, -2.006292185433951047 ) ) ;
#29331=AXIS2_PLACEMENT_3D ( 'NONE', #155910, #9640, #154842 ) ;
#29390=CARTESIAN_POINT ( 'NONE',  ( -3.285556943750000514, -1.188541666188710044, -1.896917185911906500 ) ) ;
#29461=CARTESIAN_POINT ( 'NONE',  ( 0.000000000000000000, -3.784374999522044369, -3.793834371823813001 ) ) ;
#29534=ORIENTED_EDGE ( 'NONE', *, *, #176534, .F. ) ;
#29545=ORIENTED_EDGE ( 'NONE', *, *, #194119, .T. ) ;
#29555=CARTESIAN_POINT ( 'NONE',  ( 1.001543065824772753E-15, -1.662500000000000533, 4.012584370867899430 ) ) ;
#29571=DIRECTION ( 'NONE',  ( 2.345077562848782505E-16, 0.000000000000000000, 1.000000000000000000 ) ) ;
#29617=ORIENTED_EDGE ( 'NONE', *, *, #139381, .F. ) ;
#29628=CARTESIAN_POINT ( 'NONE',  ( -3.285556943749998737, -2.880208332855377584, 1.896917185911908721 ) ) ;
#29647=CARTESIAN_POINT ( 'NONE',  ( -1.737499999999997824, -0.9916666666666684726, 3.009438278150925683 ) ) ;
#29720=CARTESIAN_POINT ( 'NONE',  ( 3.475000000000000533, -3.252083332377416092, -2.006292185433951047 ) ) ;
#29806=CARTESIAN_POINT ( 'NONE',  ( -1.642778471875000035, -0.1677083328553742592, -2.845375778867859751 ) ) ;
#29887=CARTESIAN_POINT ( 'NONE',  ( -1.642778471875000035, -3.055208332855375630, -2.845375778867859751 ) ) ;
#29972=DIRECTION ( 'NONE',  ( 1.224646799147353454E-16, 0.000000000000000000, -1.000000000000000000 ) ) ;
#30011=CARTESIAN_POINT ( 'NONE',  ( 3.285556943750000070, -1.684374999522043836, 0.000000000000000000 ) ) ;
#30150=CARTESIAN_POINT ( 'NONE',  ( -3.285556943750000514, -1.538541666188708357, -1.896917185911906500 ) ) ;
#30189=CARTESIAN_POINT ( 'NONE',  ( 3.475000000000000533, -1.895833333333332815, -2.006292185433951047 ) ) ;
#30195=( NAMED_UNIT ( * ) PLANE_ANGLE_UNIT ( ) SI_UNIT ( $, .RADIAN. ) );
#30226=CARTESIAN_POINT ( 'NONE',  ( 0.000000000000000000, 0.4000000000000010214, 0.000000000000000000 ) ) ;
#30234=EDGE_CURVE ( 'NONE', #146583, #36604, #76921, .T. ) ;
#30260=CARTESIAN_POINT ( 'NONE',  ( -1.840780836846555912, -3.118471481109373666, -2.864343303366730265 ) ) ;
#30385=DIRECTION ( 'NONE',  ( -0.000000000000000000, -1.000000000000000000, -0.000000000000000000 ) ) ;
#30408=AXIS2_PLACEMENT_3D ( 'NONE', #81106, #94187, #64849 ) ;
#30455=ORIENTED_EDGE ( 'NONE', *, *, #126255, .T. ) ;
#30460=CARTESIAN_POINT ( 'NONE',  ( -1.642778471874998480, -1.101041666188708801, 2.845375778867863303 ) ) ;
#30498=AXIS2_PLACEMENT_3D ( 'NONE', #44450, #178708, #110567 ) ;
#30533=CARTESIAN_POINT ( 'NONE',  ( 1.642778471875000035, -4.163541666188708135, -2.845375778867859751 ) ) ;
#30543=ORIENTED_EDGE ( 'NONE', *, *, #14538, .F. ) ;
#30599=CARTESIAN_POINT ( 'NONE',  ( 0.3708575915560879954, -3.142560865293257510, -3.359854750545201885 ) ) ;
#30717=CARTESIAN_POINT ( 'NONE',  ( -1.737499999999997824, -3.791666666666665186, 3.009438278150925683 ) ) ;
#30792=CARTESIAN_POINT ( 'NONE',  ( 3.475000000000000533, -3.281249999044083765, 0.000000000000000000 ) ) ;
#30853=( GEOMETRIC_REPRESENTATION_CONTEXT ( 3 ) GLOBAL_UNCERTAINTY_ASSIGNED_CONTEXT ( ( #65884 ) ) GLOBAL_UNIT_ASSIGNED_CONTEXT ( ( #128836, #30195, #96284 ) ) REPRESENTATION_CONTEXT ( 'NONE', 'WORKASPACE' ) );
#30880=CARTESIAN_POINT ( 'NONE',  ( 3.285556943750000070, -0.6343749995220415716, 0.000000000000000000 ) ) ;
#30885=B_SPLINE_CURVE_WITH_KNOTS ( 'NONE', 3,
 ( #17975, #3844, #50506, #82992 ),
 .UNSPECIFIED., .F., .F.,
 ( 4, 4 ),
 ( 5.198109377592358663E-17, 0.0001214485030784780796 ),
 .UNSPECIFIED. ) ;
#31021=PLANE ( 'NONE',  #157884 ) ;
#31087=CARTESIAN_POINT ( 'NONE',  ( -1.642778471875000035, -2.267708332855375541, -2.845375778867859751 ) ) ;
#31225=CARTESIAN_POINT ( 'NONE',  ( 1.642778471875000035, -3.026041666188708401, -2.845375778867859751 ) ) ;
#31266=CARTESIAN_POINT ( 'NONE',  ( 0.000000000000000000, -2.187499999999998668, -4.012584370867899430 ) ) ;
#31268=CARTESIAN_POINT ( 'NONE',  ( 3.285556943750000070, -0.2843749995220419269, 0.000000000000000000 ) ) ;
#31331=CARTESIAN_POINT ( 'NONE',  ( 1.001543065824772753E-15, -0.8093749995220410609, 3.793834371823811669 ) ) ;
#31472=CARTESIAN_POINT ( 'NONE',  ( 0.000000000000000000, 6.999999999999999112, 0.000000000000000000 ) ) ;
#31609=CARTESIAN_POINT ( 'NONE',  ( 0.9311234436981512541, -1.109380368602566946, -3.475000000000000977 ) ) ;
#31679=CARTESIAN_POINT ( 'NONE',  ( -3.423144538496482259, -0.02155739199629116976, -0.4187269634647496352 ) ) ;
#31692=CARTESIAN_POINT ( 'NONE',  ( -3.475000000000000533, -2.479166666666667851, -2.006292185433948827 ) ) ;
#31724=CIRCLE ( 'NONE', #107848, 10.92874649719719571 ) ;
#31763=CIRCLE ( 'NONE', #473, 11.00000000000000000 ) ;
#31782=CARTESIAN_POINT ( 'NONE',  ( -1.737499999999997824, -2.741666666666666696, 3.009438278150925683 ) ) ;
#31817=CARTESIAN_POINT ( 'NONE',  ( -3.475000000000000089, -0.9959404071528829006, 0.7091675535885048065 ) ) ;
#31849=EDGE_CURVE ( 'NONE', #201966, #130778, #15064, .T. ) ;
#31854=CARTESIAN_POINT ( 'NONE',  ( 0.000000000000000000, -3.543749999044085275, -4.012584370867899430 ) ) ;
#31936=CARTESIAN_POINT ( 'NONE',  ( 0.000000000000000000, -2.296874999522042327, -3.793834371823813001 ) ) ;
#31969=ORIENTED_EDGE ( 'NONE', *, *, #210296, .F. ) ;
#31992=VERTEX_POINT ( 'NONE', #171353 ) ;
#32137=CARTESIAN_POINT ( 'NONE',  ( 0.000000000000000000, -0.8968749995220406390, -3.793834371823813001 ) ) ;
#32184=DIRECTION ( 'NONE',  ( 0.000000000000000000, -1.000000000000000000, 0.000000000000000000 ) ) ;
#32283=CARTESIAN_POINT ( 'NONE',  ( -3.285556943750000070, -2.909374999522040817, 0.000000000000000000 ) ) ;
#32321=CARTESIAN_POINT ( 'NONE',  ( 3.475000000000000533, -3.354166666666667851, 2.006292185433948827 ) ) ;
#32323=CARTESIAN_POINT ( 'NONE',  ( 3.285556943750000070, -3.871874999522042504, 0.000000000000000000 ) ) ;
#32361=DIRECTION ( 'NONE',  ( -0.6483454320283799088, 0.000000000000000000, 0.7613463080411786432 ) ) ;
#32391=CARTESIAN_POINT ( 'NONE',  ( 1.642778471875001811, -0.4302083328553765740, 2.845375778867859751 ) ) ;
#32460=EDGE_CURVE ( 'NONE', #205126, #1142, #73682, .T. ) ;
#32492=LINE ( 'NONE', #81245, #49118 ) ;
#32539=ORIENTED_EDGE ( 'NONE', *, *, #210296, .T. ) ;
#32576=CARTESIAN_POINT ( 'NONE',  ( -3.285556943750000070, -1.509374999522042238, 0.000000000000000000 ) ) ;
#32583=DIRECTION ( 'NONE',  ( 0.6483454320283800199, 0.000000000000000000, -0.7613463080411787542 ) ) ;
#32646=CARTESIAN_POINT ( 'NONE',  ( 3.285556943750000514, -3.551041666188707424, 1.896917185911906500 ) ) ;
#32711=CARTESIAN_POINT ( 'NONE',  ( 1.528150327639969719, -3.232243495192087757, 2.908546201585544999 ) ) ;
#32729=CARTESIAN_POINT ( 'NONE',  ( -3.424353449663152027, -0.02084536078685375604, -0.4190369511457813223 ) ) ;
#32730=FACE_OUTER_BOUND ( 'NONE', #101919, .T. ) ;
#32741=CARTESIAN_POINT ( 'NONE',  ( 1.737499999999999378, -2.916666666666668295, -3.009438278150925683 ) ) ;
#32767=ORIENTED_EDGE ( 'NONE', *, *, #82056, .F. ) ;
#32797=EDGE_LOOP ( 'NONE', ( #100071, #188417, #54427, #14248 ) ) ;
#32833=CARTESIAN_POINT ( 'NONE',  ( -1.737500000000000266, -3.558333333333333570, -3.009438278150923907 ) ) ;
#32850=AXIS2_PLACEMENT_3D ( 'NONE', #52167, #121516, #184279 ) ;
#32876=DIRECTION ( 'NONE',  ( 0.000000000000000000, -1.000000000000000000, 0.000000000000000000 ) ) ;
#32904=CARTESIAN_POINT ( 'NONE',  ( -1.737499999999997824, -3.047916665710751705, 3.009438278150925683 ) ) ;
#32994=CARTESIAN_POINT ( 'NONE',  ( 1.642778471875000035, -1.976041666188709689, -2.845375778867859751 ) ) ;
#33131=CARTESIAN_POINT ( 'NONE',  ( 2.960184520039609524, -4.109567588314592790, -1.425549731837409961 ) ) ;
#33188=ORIENTED_EDGE ( 'NONE', *, *, #184990, .F. ) ;
#33194=CARTESIAN_POINT ( 'NONE',  ( 3.285556943749998737, -3.405208332855374831, -1.896917185911906500 ) ) ;
#33285=EDGE_CURVE ( 'NONE', #56590, #155561, #183979, .T. ) ;
#33291=EDGE_LOOP ( 'NONE', ( #68939, #163624, #94778 ) ) ;
#33336=CARTESIAN_POINT ( 'NONE',  ( 3.285556943750000514, -3.113541666188709645, 1.896917185911906500 ) ) ;
#33379=CARTESIAN_POINT ( 'NONE',  ( -3.285556943749998737, -4.017708332855375986, 1.896917185911908499 ) ) ;
#33447=CARTESIAN_POINT ( 'NONE',  ( -1.642778471874998480, -1.188541666188709600, 2.845375778867863303 ) ) ;
#33589=CARTESIAN_POINT ( 'NONE',  ( -1.347971487989957070E-14, -2.712500000000000355, 3.475000000000000089 ) ) ;
#33611=CARTESIAN_POINT ( 'NONE',  ( -3.358905459982799879, -0.9385608918593922878, 0.07968368524804914088 ) ) ;
#33614=ORIENTED_EDGE ( 'NONE', *, *, #46133, .F. ) ;
#33636=CARTESIAN_POINT ( 'NONE',  ( -1.642778471874998480, -3.201041666188710000, 2.845375778867863303 ) ) ;
#33641=DIRECTION ( 'NONE',  ( -2.345077562848777574E-16, 0.000000000000000000, -1.000000000000000000 ) ) ;
#33717=ORIENTED_EDGE ( 'NONE', *, *, #155760, .T. ) ;
#33740=EDGE_CURVE ( 'NONE', #184334, #88263, #110330, .T. ) ;
#33748=ADVANCED_FACE ( 'NONE', ( #52158 ), #184271, .F. ) ;
#33772=AXIS2_PLACEMENT_3D ( 'NONE', #172718, #24296, #125112 ) ;
#33774=CARTESIAN_POINT ( 'NONE',  ( 3.327047314414037338, -3.194760604760761957, 0.08430543425245248801 ) ) ;
#33789=CARTESIAN_POINT ( 'NONE',  ( -3.430537540284197995, -0.01791083384793297137, -0.4075187568799509830 ) ) ;
#33800=CARTESIAN_POINT ( 'NONE',  ( 1.737500000000001155, -2.683333333333332682, 3.009438278150922130 ) ) ;
#33824=VECTOR ( 'NONE', #11366, 1000.000000000000000 ) ;
#33838=CARTESIAN_POINT ( 'NONE',  ( 1.500000000000039524, 7.128742170989512239, 10.89107411574799400 ) ) ;
#33889=CARTESIAN_POINT ( 'NONE',  ( -3.475000000000000533, -3.879166666666665986, -2.006292185433948827 ) ) ;
#33904=CARTESIAN_POINT ( 'NONE',  ( -2.549999999999999378, -7.105553651663779391, 1.849324200890692271 ) ) ;
#33959=ORIENTED_EDGE ( 'NONE', *, *, #156113, .F. ) ;
#33962=CARTESIAN_POINT ( 'NONE',  ( 3.475000000000000533, -2.960416665710750905, 2.006292185433948827 ) ) ;
#33986=CARTESIAN_POINT ( 'NONE',  ( 3.475000000000000533, -1.545833333333334503, -2.006292185433951047 ) ) ;
#34050=CARTESIAN_POINT ( 'NONE',  ( -3.285556943750000070, -2.559374999522041172, 0.000000000000000000 ) ) ;
#34089=CARTESIAN_POINT ( 'NONE',  ( 1.464175926609780964E-14, -2.493749999044085452, -3.475000000000000533 ) ) ;
#34101=ORIENTED_EDGE ( 'NONE', *, *, #127328, .T. ) ;
#34145=ORIENTED_EDGE ( 'NONE', *, *, #73487, .F. ) ;
#34253=CARTESIAN_POINT ( 'NONE',  ( -3.285556943750000070, -3.609374999522043659, 0.000000000000000000 ) ) ;
#34283=AXIS2_PLACEMENT_3D ( 'NONE', #17516, #164862, #66258 ) ;
#34363=ORIENTED_EDGE ( 'NONE', *, *, #74644, .F. ) ;
#34399=CARTESIAN_POINT ( 'NONE',  ( 2.520459450608881991, -4.091624429771669291, -2.338646429533238535 ) ) ;
#34443=CARTESIAN_POINT ( 'NONE',  ( 0.000000000000000000, -3.434374999522041616, -3.793834371823813001 ) ) ;
#34491=ORIENTED_EDGE ( 'NONE', *, *, #128141, .T. ) ;
#34509=CARTESIAN_POINT ( 'NONE',  ( -3.285556943749998737, -2.967708332855377051, 1.896917185911908499 ) ) ;
#34696=CARTESIAN_POINT ( 'NONE',  ( 3.285556943749998737, -1.655208332855374609, -1.896917185911906500 ) ) ;
#34702=CARTESIAN_POINT ( 'NONE',  ( 3.475000000000000533, -1.225000000000000311, 0.000000000000000000 ) ) ;
#34762=ORIENTED_EDGE ( 'NONE', *, *, #117585, .T. ) ;
#34794=ADVANCED_FACE ( 'NONE', ( #110048 ), #80243, .T. ) ;
#34812=DIRECTION ( 'NONE',  ( -0.000000000000000000, 1.000000000000000000, -0.000000000000000000 ) ) ;
#34852=CARTESIAN_POINT ( 'NONE',  ( 1.001543065824772753E-15, -3.412500000000000977, 4.012584370867899430 ) ) ;
#34919=CIRCLE ( 'NONE', #90303, 11.00000000000000000 ) ;
#34958=CARTESIAN_POINT ( 'NONE',  ( 1.642778471875000035, -0.6635416661887084677, -2.845375778867859751 ) ) ;
#34984=CARTESIAN_POINT ( 'NONE',  ( -3.285556943750000514, -1.188541666188710044, -1.896917185911906722 ) ) ;
#35013=ORIENTED_EDGE ( 'NONE', *, *, #161705, .F. ) ;
#35017=CARTESIAN_POINT ( 'NONE',  ( 1.001543065824772753E-15, -0.8093749995220410609, 3.793834371823811669 ) ) ;
#35078=CARTESIAN_POINT ( 'NONE',  ( -0.9311234436981480345, -1.121869630441516996, -3.475000000000001421 ) ) ;
#35106=CARTESIAN_POINT ( 'NONE',  ( -3.285556943750000070, -2.209374999522041527, 0.000000000000000000 ) ) ;
#35312=FACE_OUTER_BOUND ( 'NONE', #92827, .T. ) ;
#35329=LINE ( 'NONE', #51607, #208061 ) ;
#35362=ORIENTED_EDGE ( 'NONE', *, *, #7000, .F. ) ;
#35380=AXIS2_PLACEMENT_3D ( 'NONE', #167942, #40083, #123555 ) ;
#35390=VERTEX_POINT ( 'NONE', #108496 ) ;
#35402=EDGE_CURVE ( 'NONE', #35390, #170914, #94174, .T. ) ;
#35466=CARTESIAN_POINT ( 'NONE',  ( -3.474999999999998312, -0.3208333333333319715, 2.006292185433951047 ) ) ;
#35507=CARTESIAN_POINT ( 'NONE',  ( 1.737500000000001155, -3.033333333333332327, 3.009438278150922130 ) ) ;
#35509=CARTESIAN_POINT ( 'NONE',  ( 1.642778471875001811, -1.742708332855374298, 2.845375778867859751 ) ) ;
#35570=CARTESIAN_POINT ( 'NONE',  ( 1.642778471875000035, -1.363541666188707646, -2.845375778867859751 ) ) ;
#35653=AXIS2_PLACEMENT_3D ( 'NONE', #50688, #202246, #153536 ) ;
#35656=CARTESIAN_POINT ( 'NONE',  ( 0.2209699231256057605, -0.9756392058242843168, 3.445770853192297256 ) ) ;
#35722=ORIENTED_EDGE ( 'NONE', *, *, #194119, .F. ) ;
#35765=CARTESIAN_POINT ( 'NONE',  ( -1.642778471874998480, -1.801041666188708090, 2.845375778867863303 ) ) ;
#35804=CARTESIAN_POINT ( 'NONE',  ( -2.324088772396477673E-16, -2.143749999044084031, -3.475000000000000089 ) ) ;
#35805=AXIS2_PLACEMENT_3D ( 'NONE', #93466, #121758, #122842 ) ;
#35884=EDGE_LOOP ( 'NONE', ( #181968, #34145, #150975, #95989 ) ) ;
#35919=CARTESIAN_POINT ( 'NONE',  ( -3.422770014095240398, -0.02179599533581897189, -0.4183011094369343819 ) ) ;
#35920=CARTESIAN_POINT ( 'NONE',  ( -1.499999999999960476, 7.128742170989517568, 10.89107411574800111 ) ) ;
#35969=CARTESIAN_POINT ( 'NONE',  ( 1.500000000000039524, 7.378742179571327497, 10.87908636427990494 ) ) ;
#36010=AXIS2_PLACEMENT_3D ( 'NONE', #110279, #210892, #176288 ) ;
#36030=CARTESIAN_POINT ( 'NONE',  ( 1.642778471875000035, -0.3135416661887088785, -2.845375778867859751 ) ) ;
#36053=CARTESIAN_POINT ( 'NONE',  ( 3.285556943749998737, -2.355208332855375453, -1.896917185911906722 ) ) ;
#36085=CARTESIAN_POINT ( 'NONE',  ( 3.285556943750000070, -1.071874999522042016, 0.000000000000000000 ) ) ;
#36108=CARTESIAN_POINT ( 'NONE',  ( -6.042630808230841359E-15, -1.662500000000000533, 3.474999999999999645 ) ) ;
#36177=CARTESIAN_POINT ( 'NONE',  ( -3.285556943749998737, -2.530208332855374831, 1.896917185911908499 ) ) ;
#36192=CARTESIAN_POINT ( 'NONE',  ( 2.550000000000000266, 1.000000000000000888, -1.849324200890695824 ) ) ;
#36365=CARTESIAN_POINT ( 'NONE',  ( -1.500000000000039524, 6.999999999999999112, -10.89724735885167739 ) ) ;
#36372=ORIENTED_EDGE ( 'NONE', *, *, #186277, .T. ) ;
#36381=CARTESIAN_POINT ( 'NONE',  ( -1.642778471874998480, -2.851041666188706802, 2.845375778867863303 ) ) ;
#36385=EDGE_LOOP ( 'NONE', ( #63641, #59927, #89702, #49776 ) ) ;
#36461=VERTEX_POINT ( 'NONE', #205949 ) ;
#36467=AXIS2_PLACEMENT_3D ( 'NONE', #31472, #136431, #201383 ) ;
#36482=ORIENTED_EDGE ( 'NONE', *, *, #19306, .F. ) ;
#36509=CARTESIAN_POINT ( 'NONE',  ( 1.642778471875001811, -1.830208332855375097, 2.845375778867859751 ) ) ;
#36532=CARTESIAN_POINT ( 'NONE',  ( -3.474999999999998312, -0.6708333333333343917, 2.006292185433951047 ) ) ;
#36562=ADVANCED_FACE ( 'NONE', ( #23991 ), #107462, .T. ) ;
#36573=CARTESIAN_POINT ( 'NONE',  ( 0.000000000000000000, -3.587500000000000355, -4.012584370867899430 ) ) ;
#36575=CARTESIAN_POINT ( 'NONE',  ( -1.642778471875000035, -0.8677083328553769626, -2.845375778867859751 ) ) ;
#36604=VERTEX_POINT ( 'NONE', #188638 ) ;
#36632=VECTOR ( 'NONE', #85863, 1000.000000000000000 ) ;
#36639=CARTESIAN_POINT ( 'NONE',  ( 0.000000000000000000, -2.034374999522043481, -3.793834371823813001 ) ) ;
#36641=CARTESIAN_POINT ( 'NONE',  ( -6.042630808230841359E-15, -1.968749999044084875, 3.474999999999999645 ) ) ;
#36642=LINE ( 'NONE', #49702, #55864 ) ;
#36712=ORIENTED_EDGE ( 'NONE', *, *, #189945, .F. ) ;
#36796=CARTESIAN_POINT ( 'NONE',  ( -3.298413662870199659, -0.9801510035281409960, 1.084536036895182187 ) ) ;
#36807=CARTESIAN_POINT ( 'NONE',  ( 1.734723475976807094E-15, 1.000000000000000888, 3.150000000000001243 ) ) ;
#36826=CARTESIAN_POINT ( 'NONE',  ( 1.642778471875000035, -1.626041666188710044, -2.845375778867859751 ) ) ;
#36860=CARTESIAN_POINT ( 'NONE',  ( -3.474999999999997868, -2.420833333333334725, 2.006292185433951047 ) ) ;
#36986=CARTESIAN_POINT ( 'NONE',  ( -1.499999999999963141, 7.750000000000000000, 10.86128356754324820 ) ) ;
#37126=CARTESIAN_POINT ( 'NONE',  ( -1.642778471874998480, -2.151041666188707957, 2.845375778867863303 ) ) ;
#37156=ADVANCED_BREP_SHAPE_REPRESENTATION ( '', ( #84085, #200407 ), #13653 ) ;
#37163=CARTESIAN_POINT ( 'NONE',  ( 1.001543065824772753E-15, -1.159374999522043481, 3.793834371823811669 ) ) ;
#37226=CIRCLE ( 'NONE', #130691, 11.00000000000000000 ) ;
#37227=( BOUNDED_CURVE ( )  B_SPLINE_CURVE ( 2, ( #137060, #69880, #55795 ),
 .UNSPECIFIED., .F., .T. ) 
 B_SPLINE_CURVE_WITH_KNOTS ( ( 3, 3 ),
 ( 0.000000000000000000, 0.0005080973304710143749 ),
 .UNSPECIFIED. ) 
 CURVE ( )  GEOMETRIC_REPRESENTATION_ITEM ( )  RATIONAL_B_SPLINE_CURVE ( ( 1.000000000000000000, 0.9950988063024598373, 0.9905562134193928170 ) ) 
 REPRESENTATION_ITEM ( '' )  );
#37256=CARTESIAN_POINT ( 'NONE',  ( -1.642778471875000035, -3.317708332855374476, -2.845375778867859751 ) ) ;
#37357=CARTESIAN_POINT ( 'NONE',  ( 1.394453263437886604E-15, -1.312499999999999556, 3.474999999999999645 ) ) ;
#37453=CARTESIAN_POINT ( 'NONE',  ( -3.285556943749998737, -3.230208332855375897, 1.896917185911908499 ) ) ;
#37457=VERTEX_POINT ( 'NONE', #207808 ) ;
#37463=ORIENTED_EDGE ( 'NONE', *, *, #68847, .F. ) ;
#37588=CARTESIAN_POINT ( 'NONE',  ( -3.246376473470825363, -0.8887487162375362626, 0.5058895364790267912 ) ) ;
#37611=CARTESIAN_POINT ( 'NONE',  ( 3.285556943750000070, -3.784374999522041705, 0.000000000000000000 ) ) ;
#37656=CARTESIAN_POINT ( 'NONE',  ( 1.001543065824772753E-15, -1.071874999522043792, 3.793834371823811669 ) ) ;
#37718=CARTESIAN_POINT ( 'NONE',  ( -1.642778471874998480, -1.888541666188708890, 2.845375778867863303 ) ) ;
#37803=CARTESIAN_POINT ( 'NONE',  ( 1.080614271145773575, -0.9701817977426218098, 3.262761386485118376 ) ) ;
#37909=CARTESIAN_POINT ( 'NONE',  ( -3.474999999999998312, -0.6708333333333343917, 2.006292185433951047 ) ) ;
#37943=CARTESIAN_POINT ( 'NONE',  ( 1.499999999999959588, 7.128742170989514904, -10.89107411574800288 ) ) ;
#37945=CARTESIAN_POINT ( 'NONE',  ( -0.9311234436981447038, -2.521869630441519572, -3.475000000000004086 ) ) ;
#38055=CARTESIAN_POINT ( 'NONE',  ( 1.173530994449854870, -3.042800438942089514, 3.270848514539542506 ) ) ;
#38068=CARTESIAN_POINT ( 'NONE',  ( -3.421105596467043153, -0.02305168933490822636, -0.4127856329643360134 ) ) ;
#38123=CARTESIAN_POINT ( 'NONE',  ( -1.333315192109695957, 8.250054423670803772, 10.85938449304425468 ) ) ;
#38182=CARTESIAN_POINT ( 'NONE',  ( 3.285556943749998737, -2.442708332855375364, -1.896917185911906500 ) ) ;
#38205=CARTESIAN_POINT ( 'NONE',  ( 3.285556943749998737, -0.9552083328553737651, -1.896917185911906722 ) ) ;
#38237=CARTESIAN_POINT ( 'NONE',  ( 1.737500000000001155, -4.039583332377416625, 3.009438278150922130 ) ) ;
#38324=CARTESIAN_POINT ( 'NONE',  ( -3.285556943750000070, -3.259374999522044014, 0.000000000000000000 ) ) ;
#38387=CARTESIAN_POINT ( 'NONE',  ( 0.000000000000000000, -0.02876672507444788529, 3.432849766368870181 ) ) ;
#38454=EDGE_LOOP ( 'NONE', ( #141487, #80237, #109650, #50695 ) ) ;
#38613=CIRCLE ( 'NONE', #21257, 3.017800438942085606 ) ;
#38662=CARTESIAN_POINT ( 'NONE',  ( -1.642778471875000035, -1.305208332855377407, -2.845375778867859751 ) ) ;
#38728=CARTESIAN_POINT ( 'NONE',  ( -1.642778471874998480, -1.801041666188708090, 2.845375778867863303 ) ) ;
#38787=CARTESIAN_POINT ( 'NONE',  ( -3.285556943750000514, -3.726041666188710799, -1.896917185911906500 ) ) ;
#38795=DIRECTION ( 'NONE',  ( 0.000000000000000000, 1.000000000000000000, 0.000000000000000000 ) ) ;
#38871=CARTESIAN_POINT ( 'NONE',  ( 2.668637133679951035, -0.9572936134980876144, 2.114570777442663640 ) ) ;
#38891=DIRECTION ( 'NONE',  ( 0.000000000000000000, -1.000000000000000000, 0.000000000000000000 ) ) ;
#38911=ORIENTED_EDGE ( 'NONE', *, *, #51077, .T. ) ;
#38924=PLANE ( 'NONE',  #126355 ) ;
#38934=ORIENTED_EDGE ( 'NONE', *, *, #41175, .F. ) ;
#38942=CARTESIAN_POINT ( 'NONE',  ( 3.285556943750000514, -0.6635416661887083567, 1.896917185911906500 ) ) ;
#38978=CARTESIAN_POINT ( 'NONE',  ( 1.737500000000001155, -0.9333333333333346804, 3.009438278150922130 ) ) ;
#38982=EDGE_CURVE ( 'NONE', #897, #16835, #119071, .T. ) ;
#39020=DIRECTION ( 'NONE',  ( 0.000000000000000000, 0.7071067811865445751, 0.7071067811865504593 ) ) ;
#39109=CARTESIAN_POINT ( 'NONE',  ( 1.499999999999959588, 7.750000000000000000, -10.86128356754324820 ) ) ;
#39148=CARTESIAN_POINT ( 'NONE',  ( -1.500000000000039524, 7.750000000000000000, -10.86128356754322688 ) ) ;
#39163=CARTESIAN_POINT ( 'NONE',  ( -3.475000000000000533, -2.435416665710753215, -2.006292185433948827 ) ) ;
#39244=CARTESIAN_POINT ( 'NONE',  ( -3.285556943749998737, -1.217708332855376607, 1.896917185911908499 ) ) ;
#39294=( BOUNDED_CURVE ( )  B_SPLINE_CURVE ( 3, ( #155075, #38123, #187558, #22905 ),
 .UNSPECIFIED., .F., .T. ) 
 B_SPLINE_CURVE_WITH_KNOTS ( ( 4, 4 ),
 ( 4.683789229004537091, 4.706575325518645769 ),
 .UNSPECIFIED. ) 
 CURVE ( )  GEOMETRIC_REPRESENTATION_ITEM ( )  RATIONAL_B_SPLINE_CURVE ( ( 1.000000000000000000, 0.9999567332851475587, 0.9999567332851475587, 1.000000000000000000 ) ) 
 REPRESENTATION_ITEM ( '' )  );
#39302=CARTESIAN_POINT ( 'NONE',  ( 3.475000000000000533, -3.981249999044082610, 0.000000000000000000 ) ) ;
#39391=CARTESIAN_POINT ( 'NONE',  ( -3.475000000000000533, -0.02916666666666653876, -2.006292185433948827 ) ) ;
#39523=CIRCLE ( 'NONE', #136483, 11.00000000000000000 ) ;
#39583=EDGE_LOOP ( 'NONE', ( #177873, #57526, #34491, #106577, #75822, #72338, #10286, #202055 ) ) ;
#39604=DIRECTION ( 'NONE',  ( -0.000000000000000000, 1.000000000000000000, 0.000000000000000000 ) ) ;
#39612=CARTESIAN_POINT ( 'NONE',  ( 0.000000000000000000, 2.999999999999999112, -11.00000000000000000 ) ) ;
#39676=VECTOR ( 'NONE', #156181, 1000.000000000000000 ) ;
#39722=ORIENTED_EDGE ( 'NONE', *, *, #15800, .F. ) ;
#39726=CARTESIAN_POINT ( 'NONE',  ( -3.285556943749998737, -1.567708332855375142, 1.896917185911908721 ) ) ;
#39796=CARTESIAN_POINT ( 'NONE',  ( 0.000000000000000000, -1.246874999522042948, -3.793834371823813001 ) ) ;
#39862=CARTESIAN_POINT ( 'NONE',  ( 1.001543065824772753E-15, -3.259374999522042682, 3.793834371823811669 ) ) ;
#39871=ORIENTED_EDGE ( 'NONE', *, *, #112217, .T. ) ;
#40014=CARTESIAN_POINT ( 'NONE',  ( 1.642778471875000035, -0.9260416661887073131, -2.845375778867859751 ) ) ;
#40041=CIRCLE ( 'NONE', #36467, 9.999999999999998224 ) ;
#40051=CARTESIAN_POINT ( 'NONE',  ( -3.285556943750000070, -3.609374999522043659, 0.000000000000000000 ) ) ;
#40083=DIRECTION ( 'NONE',  ( 0.000000000000000000, 1.000000000000000000, 0.000000000000000000 ) ) ;
#40178=CARTESIAN_POINT ( 'NONE',  ( -1.718115394875207258, -1.600000000000000755, 2.017567716309124126 ) ) ;
#40239=ORIENTED_EDGE ( 'NONE', *, *, #51077, .F. ) ;
#40241=VERTEX_POINT ( 'NONE', #51632 ) ;
#40259=DIRECTION ( 'NONE',  ( 0.000000000000000000, -1.000000000000000000, 0.000000000000000000 ) ) ;
#40268=CARTESIAN_POINT ( 'NONE',  ( 0.000000000000000000, 12.31951671548121219, 0.000000000000000000 ) ) ;
#40300=AXIS2_PLACEMENT_3D ( 'NONE', #27389, #86259, #202105 ) ;
#40321=EDGE_CURVE ( 'NONE', #10807, #201966, #154464, .T. ) ;
#40328=CARTESIAN_POINT ( 'NONE',  ( -3.285556943750000514, -0.9260416661887070910, -1.896917185911906500 ) ) ;
#40386=CARTESIAN_POINT ( 'NONE',  ( -3.285556943750000514, -2.676041666188707424, -1.896917185911906500 ) ) ;
#40444=CARTESIAN_POINT ( 'NONE',  ( 0.000000000000000000, 2.499999999999998668, 0.000000000000000000 ) ) ;
#40475=CARTESIAN_POINT ( 'NONE',  ( 3.475000000000000533, -0.2041666666666657748, 2.006292185433948827 ) ) ;
#40500=DIRECTION ( 'NONE',  ( -8.881784197001252323E-16, 0.000000000000000000, 1.000000000000000000 ) ) ;
#40504=VECTOR ( 'NONE', #78463, 1000.000000000000000 ) ;
#40514=ORIENTED_EDGE ( 'NONE', *, *, #200594, .F. ) ;
#40594=ORIENTED_EDGE ( 'NONE', *, *, #73487, .T. ) ;
#40604=CIRCLE ( 'NONE', #54372, 2.600000000000000533 ) ;
#40812=CARTESIAN_POINT ( 'NONE',  ( 3.285556943750000070, -1.071874999522042016, 0.000000000000000000 ) ) ;
#40838=LINE ( 'NONE', #75454, #2067 ) ;
#40862=VECTOR ( 'NONE', #132939, 1000.000000000000000 ) ;
#40879=CARTESIAN_POINT ( 'NONE',  ( -3.285556943749998737, -2.880208332855377584, 1.896917185911908499 ) ) ;
#40884=ADVANCED_FACE ( 'NONE', ( #103056 ), #133457, .T. ) ;
#40938=CARTESIAN_POINT ( 'NONE',  ( -1.642778471875000035, -4.105208332855374564, -2.845375778867859751 ) ) ;
#41005=( BOUNDED_CURVE ( )  B_SPLINE_CURVE ( 2, ( #60940, #181083, #112963, #178975, #14295, #180031, #80390, #77179, #64147 ),
 .UNSPECIFIED., .F., .T. ) 
 B_SPLINE_CURVE_WITH_KNOTS ( ( 3, 2, 2, 2, 3 ),
 ( 0.3958333333333333703, 0.4027777777777777901, 0.4166666666666666852, 0.4305555555555555802, 0.4375000000000000000 ),
 .UNSPECIFIED. ) 
 CURVE ( )  GEOMETRIC_REPRESENTATION_ITEM ( )  RATIONAL_B_SPLINE_CURVE ( ( 0.9330127018922194093, 0.9330127018922196314, 1.000000000000000000, 0.8660254037844387076, 1.000000000000000000, 0.8660254037844387076, 1.000000000000000000, 0.9330127018922194093, 0.9330127018922194093 ) ) 
 REPRESENTATION_ITEM ( '' )  );
#41018=EDGE_CURVE ( 'NONE', #94296, #102958, #61083, .T. ) ;
#41086=DIRECTION ( 'NONE',  ( 0.000000000000000000, -1.000000000000000000, 0.000000000000000000 ) ) ;
#41103=FACE_OUTER_BOUND ( 'NONE', #97157, .T. ) ;
#41130=CARTESIAN_POINT ( 'NONE',  ( 1.737499999999999378, -0.4666666666666673402, -3.009438278150925683 ) ) ;
#41171=EDGE_CURVE ( 'NONE', #187973, #153164, #52625, .T. ) ;
#41175=EDGE_CURVE ( 'NONE', #205126, #206199, #86194, .T. ) ;
#41362=CARTESIAN_POINT ( 'NONE',  ( 1.734723475976807094E-15, 2.499999999999998668, 3.150000000000001243 ) ) ;
#41403=CARTESIAN_POINT ( 'NONE',  ( -3.285556943749998737, -1.917708332855377673, 1.896917185911908499 ) ) ;
#41462=CARTESIAN_POINT ( 'NONE',  ( 0.000000000000000000, -2.034374999522043481, -3.793834371823813001 ) ) ;
#41550=CARTESIAN_POINT ( 'NONE',  ( -3.285556943749998737, -2.880208332855377584, 1.896917185911908499 ) ) ;
#41578=EDGE_LOOP ( 'NONE', ( #167068, #197166, #175308, #145820 ) ) ;
#41640=CARTESIAN_POINT ( 'NONE',  ( -1.737500000000000266, -1.458333333333332371, -3.009438278150923907 ) ) ;
#41716=CARTESIAN_POINT ( 'NONE',  ( -3.475000000000000533, -0.6562499990440846531, 0.000000000000000000 ) ) ;
#41738=EDGE_CURVE ( 'NONE', #132336, #176259, #82560, .T. ) ;
#41746=EDGE_LOOP ( 'NONE', ( #92048, #50092, #93957, #174674, #105968, #13310, #213228, #156894 ) ) ;
#41822=DIRECTION ( 'NONE',  ( 0.000000000000000000, 1.000000000000000000, 0.000000000000000000 ) ) ;
#41850=EDGE_CURVE ( 'NONE', #37457, #145929, #175781, .T. ) ;
#41870=ORIENTED_EDGE ( 'NONE', *, *, #175293, .T. ) ;
#41884=CARTESIAN_POINT ( 'NONE',  ( 1.737499999999999378, -2.172916665710750816, -3.009438278150925683 ) ) ;
#41887=CARTESIAN_POINT ( 'NONE',  ( 3.285556943750000070, -2.471874999522040373, 0.000000000000000000 ) ) ;
#41949=CARTESIAN_POINT ( 'NONE',  ( 0.000000000000000000, -3.696874999522040017, -3.793834371823813001 ) ) ;
#42014=CARTESIAN_POINT ( 'NONE',  ( 1.001543065824772753E-15, -3.959374999522043304, 3.793834371823811669 ) ) ;
#42074=AXIS2_PLACEMENT_3D ( 'NONE', #92478, #6897, #171552 ) ;
#42094=CARTESIAN_POINT ( 'NONE',  ( 2.678940061867811195, -0.9218674704012446153, -1.992856458623322835 ) ) ;
#42160=CARTESIAN_POINT ( 'NONE',  ( -3.285556943750000070, -1.159374999522042815, 0.000000000000000000 ) ) ;
#42175=EDGE_CURVE ( 'NONE', #75662, #126440, #166550, .T. ) ;
#42180=DIRECTION ( 'NONE',  ( -1.000000000000000000, 0.000000000000000000, 0.000000000000000000 ) ) ;
#42197=CARTESIAN_POINT ( 'NONE',  ( 3.475000000000000533, -0.1458333333333326765, -2.006292185433951047 ) ) ;
#42436=DIRECTION ( 'NONE',  ( 0.000000000000000000, -1.000000000000000000, 0.000000000000000000 ) ) ;
#42470=CARTESIAN_POINT ( 'NONE',  ( -3.285556943749998737, -2.267708332855375986, 1.896917185911908499 ) ) ;
#42532=CARTESIAN_POINT ( 'NONE',  ( 1.642778471875000035, -2.763541666188709556, -2.845375778867859751 ) ) ;
#42557=CARTESIAN_POINT ( 'NONE',  ( -1.565491486567922363, -3.232243495192119731, 2.892400742676151104 ) ) ;
#42620=CARTESIAN_POINT ( 'NONE',  ( 3.475000000000000533, -1.604166666666667629, 2.006292185433948827 ) ) ;
#42712=CARTESIAN_POINT ( 'NONE',  ( -3.475000000000000533, -2.450000000000000622, 0.000000000000000000 ) ) ;
#42744=VERTEX_POINT ( 'NONE', #77153 ) ;
#42753=VECTOR ( 'NONE', #210863, 1000.000000000000000 ) ;
#42760=DIRECTION ( 'NONE',  ( 0.000000000000000000, -1.000000000000000000, 0.000000000000000000 ) ) ;
#42785=CARTESIAN_POINT ( 'NONE',  ( 1.737500000000001155, -0.8895833323774166024, 3.009438278150922130 ) ) ;
#42798=DIRECTION ( 'NONE',  ( 0.6483454320283799088, 0.000000000000000000, -0.7613463080411786432 ) ) ;
#42809=AXIS2_PLACEMENT_3D ( 'NONE', #186403, #119349, #169094 ) ;
#42874=CARTESIAN_POINT ( 'NONE',  ( 3.285556943750000514, -0.3135416661887098777, 1.896917185911906500 ) ) ;
#42903=EDGE_LOOP ( 'NONE', ( #123987, #881 ) ) ;
#42955=CARTESIAN_POINT ( 'NONE',  ( -3.285556943749998737, -2.267708332855375986, 1.896917185911908721 ) ) ;
#43018=CARTESIAN_POINT ( 'NONE',  ( 3.285556943750000514, -2.763541666188707335, 1.896917185911906500 ) ) ;
#43084=CARTESIAN_POINT ( 'NONE',  ( -1.642778471875000035, -0.5177083328553738761, -2.845375778867859751 ) ) ;
#43104=DIRECTION ( 'NONE',  ( 0.6483454320283812411, 0.000000000000000000, -0.7613463080411777550 ) ) ;
#43130=CARTESIAN_POINT ( 'NONE',  ( 1.394453263437886604E-15, -1.618749999044085230, 3.474999999999999645 ) ) ;
#43229=CARTESIAN_POINT ( 'NONE',  ( 0.000000000000000000, -0.5468749995220422155, -3.793834371823813001 ) ) ;
#43264=CARTESIAN_POINT ( 'NONE',  ( 1.001543065824772753E-15, -1.662500000000000533, 4.012584370867899430 ) ) ;
#43314=EDGE_CURVE ( 'NONE', #211199, #7595, #148448, .T. ) ;
#43443=CARTESIAN_POINT ( 'NONE',  ( 1.499999999999963141, 7.750000000000000000, -9.886859966642596476 ) ) ;
#43469=DIRECTION ( 'NONE',  ( 0.000000000000000000, 0.000000000000000000, -1.000000000000000000 ) ) ;
#43536=CARTESIAN_POINT ( 'NONE',  ( -3.285556943750000070, -2.996874999522041616, 0.000000000000000000 ) ) ;
#43587=FACE_OUTER_BOUND ( 'NONE', #126789, .T. ) ;
#43592=CARTESIAN_POINT ( 'NONE',  ( -3.285556943750000070, -2.996874999522041616, 0.000000000000000000 ) ) ;
#43619=VECTOR ( 'NONE', #15202, 1000.000000000000114 ) ;
#43640=ORIENTED_EDGE ( 'NONE', *, *, #6091, .F. ) ;
#43684=CARTESIAN_POINT ( 'NONE',  ( -3.474999999999998312, -0.6708333333333343917, 2.006292185433951047 ) ) ;
#43705=CYLINDRICAL_SURFACE ( 'NONE', #18825, 3.150000000000000799 ) ;
#43713=ORIENTED_EDGE ( 'NONE', *, *, #83547, .T. ) ;
#43777=CARTESIAN_POINT ( 'NONE',  ( -3.475000000000000533, -1.079166666666665941, -2.006292185433948827 ) ) ;
#43798=SURFACE_SIDE_STYLE ('',( #147684 ) ) ;
#43906=AXIS2_PLACEMENT_3D ( 'NONE', #76714, #13834, #25829 ) ;
#43974=DIRECTION ( 'NONE',  ( -0.000000000000000000, 1.000000000000000000, -0.000000000000000000 ) ) ;
#43989=ORIENTED_EDGE ( 'NONE', *, *, #205891, .F. ) ;
#44009=CARTESIAN_POINT ( 'NONE',  ( 3.475000000000000533, -1.954166666666666163, 2.006292185433948827 ) ) ;
#44012=DIRECTION ( 'NONE',  ( -0.6483454320283800199, 0.000000000000000000, 0.7613463080411787542 ) ) ;
#44075=CARTESIAN_POINT ( 'NONE',  ( -1.642778471875000035, -3.317708332855374476, -2.845375778867859751 ) ) ;
#44136=CARTESIAN_POINT ( 'NONE',  ( -3.285556943750000070, -2.559374999522041172, 0.000000000000000000 ) ) ;
#44158=DIRECTION ( 'NONE',  ( -0.6483454320283800199, 0.000000000000000000, 0.7613463080411786432 ) ) ;
#44160=VECTOR ( 'NONE', #191070, 1000.000000000000000 ) ;
#44184=CARTESIAN_POINT ( 'NONE',  ( 7.204675194429079505E-15, -1.793749999044084831, -3.475000000000000089 ) ) ;
#44211=ORIENTED_EDGE ( 'NONE', *, *, #116234, .T. ) ;
#44278=ORIENTED_EDGE ( 'NONE', *, *, #6091, .T. ) ;
#44284=CARTESIAN_POINT ( 'NONE',  ( 3.285556943750000070, -1.334374999522040861, 0.000000000000000000 ) ) ;
#44321=CARTESIAN_POINT ( 'NONE',  ( -1.737500000000000266, -2.508333333333334636, -3.009438278150923907 ) ) ;
#44385=CARTESIAN_POINT ( 'NONE',  ( -2.703472480837374903, -3.106478463707009308, -2.089468915991812725 ) ) ;
#44395=FACE_OUTER_BOUND ( 'NONE', #51476, .T. ) ;
#44412=ORIENTED_EDGE ( 'NONE', *, *, #48185, .T. ) ;
#44450=CARTESIAN_POINT ( 'NONE',  ( 0.000000000000000000, 2.999999999999999112, -10.25000000000000000 ) ) ;
#44480=CARTESIAN_POINT ( 'NONE',  ( -1.333477130264982158, 8.249568609204956715, 9.911050286642574036 ) ) ;
#44587=CARTESIAN_POINT ( 'NONE',  ( 1.001543065824772753E-15, -1.071874999522043792, 3.793834371823811669 ) ) ;
#44595=DIRECTION ( 'NONE',  ( 0.000000000000000000, 1.000000000000000000, 0.000000000000000000 ) ) ;
#44629=CONICAL_SURFACE ( 'NONE', #61457, 10.92874649719719571, 0.04746665426984499059 ) ;
#44654=CARTESIAN_POINT ( 'NONE',  ( -3.285556943750000514, -1.626041666188708046, -1.896917185911906500 ) ) ;
#44663=AXIS2_PLACEMENT_3D ( 'NONE', #136275, #100554, #165553 ) ;
#44701=CARTESIAN_POINT ( 'NONE',  ( -6.042630808230841359E-15, -2.012500000000000178, 3.474999999999999645 ) ) ;
#44706=EDGE_LOOP ( 'NONE', ( #20272, #655 ) ) ;
#44724=CARTESIAN_POINT ( 'NONE',  ( -1.620863580070950549, -1.399999999999998579, 1.903365770102946941 ) ) ;
#44753=CARTESIAN_POINT ( 'NONE',  ( 3.475000000000000533, -1.895833333333332815, -2.006292185433951047 ) ) ;
#44844=CARTESIAN_POINT ( 'NONE',  ( 3.475000000000000533, -2.595833333333334103, -2.006292185433951047 ) ) ;
#44916=CARTESIAN_POINT ( 'NONE',  ( -3.474999999999998312, -0.9770833323774182899, 2.006292185433951047 ) ) ;
#44975=LINE ( 'NONE', #195475, #33824 ) ;
#45001=CARTESIAN_POINT ( 'NONE',  ( -3.285556943750000070, -0.1093749995220438809, 0.000000000000000000 ) ) ;
#45087=CARTESIAN_POINT ( 'NONE',  ( 3.285556943750000070, -3.171874999522043215, 0.000000000000000000 ) ) ;
#45090=ADVANCED_FACE ( 'NONE', ( #46579, #112698 ), #10841, .T. ) ;
#45148=CARTESIAN_POINT ( 'NONE',  ( -1.642778471875000035, -2.267708332855375541, -2.845375778867859751 ) ) ;
#45209=CARTESIAN_POINT ( 'NONE',  ( -1.642778471875000035, -1.217708332855376607, -2.845375778867859751 ) ) ;
#45275=EDGE_LOOP ( 'NONE', ( #51667, #65421 ) ) ;
#45350=CARTESIAN_POINT ( 'NONE',  ( 1.642778471875000035, -1.976041666188709689, -2.845375778867859751 ) ) ;
#45367=FACE_OUTER_BOUND ( 'NONE', #92904, .T. ) ;
#45390=CARTESIAN_POINT ( 'NONE',  ( -1.737500000000000266, -1.108333333333332726, -3.009438278150923907 ) ) ;
#45414=CARTESIAN_POINT ( 'NONE',  ( -3.420250508247430155, -0.02876672507465954931, -0.2938434605158617985 ) ) ;
#45454=CARTESIAN_POINT ( 'NONE',  ( -3.285556943750000514, -0.9260416661887070910, -1.896917185911906500 ) ) ;
#45455=CARTESIAN_POINT ( 'NONE',  ( -3.159337285218927427, -3.068491660968841295, 1.397772451703464425 ) ) ;
#45545=CARTESIAN_POINT ( 'NONE',  ( -2.900957617708239678, -3.232243495192087757, 1.542507481629953103 ) ) ;
#45548=CARTESIAN_POINT ( 'NONE',  ( -1.249999999999966471, 8.500000000000000000, 9.921567416492214520 ) ) ;
#45578=DIRECTION ( 'NONE',  ( 0.000000000000000000, 1.000000000000000000, 0.000000000000000000 ) ) ;
#45651=CARTESIAN_POINT ( 'NONE',  ( 3.285556943749998737, -0.9552083328553737651, -1.896917185911906500 ) ) ;
#45657=EDGE_LOOP ( 'NONE', ( #48655, #61812, #209455 ) ) ;
#45776=CARTESIAN_POINT ( 'NONE',  ( -3.285556943750000070, -0.1093749995220438809, 0.000000000000000000 ) ) ;
#45818=CARTESIAN_POINT ( 'NONE',  ( -3.475000000000000533, -1.399999999999998579, 0.000000000000000000 ) ) ;
#45909=CARTESIAN_POINT ( 'NONE',  ( 0.000000000000000000, -2.187499999999998668, -4.012584370867899430 ) ) ;
#45980=CARTESIAN_POINT ( 'NONE',  ( -3.475000000000000533, -2.056249999044083232, 0.000000000000000000 ) ) ;
#46133=EDGE_CURVE ( 'NONE', #141673, #157888, #113535, .T. ) ;
#46145=DIRECTION ( 'NONE',  ( 0.6483454320283799088, 0.000000000000000000, -0.7613463080411786432 ) ) ;
#46218=AXIS2_PLACEMENT_3D ( 'NONE', #206171, #28504, #40500 ) ;
#46258=CARTESIAN_POINT ( 'NONE',  ( -3.474999999999997868, -2.727083332377417957, 2.006292185433951047 ) ) ;
#46267=EDGE_LOOP ( 'NONE', ( #27202, #205556, #145134, #171190 ) ) ;
#46270=CARTESIAN_POINT ( 'NONE',  ( -3.285556943750000070, -0.8093749995220431703, 0.000000000000000000 ) ) ;
#46292=CIRCLE ( 'NONE', #198388, 9.999999999999996447 ) ;
#46294=FACE_OUTER_BOUND ( 'NONE', #44706, .T. ) ;
#46383=CARTESIAN_POINT ( 'NONE',  ( -0.1937322346335085266, -3.136378490158120425, -3.381421948784809839 ) ) ;
#46387=AXIS2_PLACEMENT_3D ( 'NONE', #136582, #55319, #86746 ) ;
#46411=CARTESIAN_POINT ( 'NONE',  ( -3.285556943750000070, -2.209374999522041527, 0.000000000000000000 ) ) ;
#46449=CARTESIAN_POINT ( 'NONE',  ( 1.001543065824772753E-15, -2.712499999999999911, 4.012584370867899430 ) ) ;
#46517=CARTESIAN_POINT ( 'NONE',  ( -2.446432203289806484, -3.110604623059922247, -2.379386263155008674 ) ) ;
#46518=CIRCLE ( 'NONE', #153805, 0.1000000000000000333 ) ;
#46522=CARTESIAN_POINT ( 'NONE',  ( 0.000000000000000000, 6.999999999999999112, 0.000000000000000000 ) ) ;
#46579=FACE_BOUND ( 'NONE', #104372, .T. ) ;
#46704=EDGE_CURVE ( 'NONE', #42744, #204603, #27071, .T. ) ;
#46720=CARTESIAN_POINT ( 'NONE',  ( 3.285556943750000070, -0.9843749995220412163, 0.000000000000000000 ) ) ;
#46791=VERTEX_POINT ( 'NONE', #111155 ) ;
#46794=CARTESIAN_POINT ( 'NONE',  ( 3.285556943750000514, -3.901041666188710177, 1.896917185911906500 ) ) ;
#46830=CARTESIAN_POINT ( 'NONE',  ( -3.246376473470825363, -0.8887487162375362626, 0.5058895364790267912 ) ) ;
#46888=CARTESIAN_POINT ( 'NONE',  ( -1.737500000000000266, -2.158333333333331439, -3.009438278150923907 ) ) ;
#46973=CARTESIAN_POINT ( 'NONE',  ( 1.737499999999999378, -3.616666666666667140, -3.009438278150925683 ) ) ;
#47009=CARTESIAN_POINT ( 'NONE',  ( -2.324088772396477673E-16, -1.093749999044084653, -3.475000000000000089 ) ) ;
#47029=DIRECTION ( 'NONE',  ( -0.000000000000000000, -1.000000000000000000, -0.000000000000000000 ) ) ;
#47048=CARTESIAN_POINT ( 'NONE',  ( 3.475000000000000533, -2.581249999044084475, 0.000000000000000000 ) ) ;
#47136=CARTESIAN_POINT ( 'NONE',  ( 3.285556943749998737, -0.6052083328553753416, -1.896917185911906500 ) ) ;
#47344=CARTESIAN_POINT ( 'NONE',  ( -1.642778471874998480, -2.151041666188707957, 2.845375778867863303 ) ) ;
#47491=CARTESIAN_POINT ( 'NONE',  ( 0.000000000000000000, -2.996874999522043392, -3.793834371823813001 ) ) ;
#47528=CARTESIAN_POINT ( 'NONE',  ( -3.474999999999998312, -1.370833333333331350, 2.006292185433951047 ) ) ;
#47530=CARTESIAN_POINT ( 'NONE',  ( 1.642778471875000035, -0.2260416661887081069, -2.845375778867859751 ) ) ;
#47579=ORIENTED_EDGE ( 'NONE', *, *, #67226, .T. ) ;
#47734=FACE_OUTER_BOUND ( 'NONE', #39583, .T. ) ;
#47739=CARTESIAN_POINT ( 'NONE',  ( -2.550000000000001155, -7.105553651663779391, -1.849324200890690717 ) ) ;
#47754=CARTESIAN_POINT ( 'NONE',  ( 0.000000000000000000, -3.517800438942085606, 3.000000000000000000 ) ) ;
#47782=AXIS2_PLACEMENT_3D ( 'NONE', #53280, #102033, #205918 ) ;
#47794=CARTESIAN_POINT ( 'NONE',  ( -3.285556943750000514, -0.8385416661887076240, -1.896917185911906500 ) ) ;
#47867=CARTESIAN_POINT ( 'NONE',  ( -3.285556943749998737, -3.317708332855375808, 1.896917185911908499 ) ) ;
#47917=ORIENTED_EDGE ( 'NONE', *, *, #139916, .F. ) ;
#47951=CARTESIAN_POINT ( 'NONE',  ( -3.427975237612759241, -0.01905636783647302046, -0.4136213213207836636 ) ) ;
#47953=ORIENTED_EDGE ( 'NONE', *, *, #71672, .T. ) ;
#47960=ORIENTED_EDGE ( 'NONE', *, *, #69586, .F. ) ;
#47961=CARTESIAN_POINT ( 'NONE',  ( 1.737499999999999378, -2.566666666666668650, -3.009438278150925683 ) ) ;
#48020=DIRECTION ( 'NONE',  ( -5.329070518200751394E-15, 0.000000000000000000, 1.000000000000000000 ) ) ;
#48031=CARTESIAN_POINT ( 'NONE',  ( -1.347971487989957070E-14, -3.018749999044084475, 3.475000000000000089 ) ) ;
#48041=AXIS2_PLACEMENT_3D ( 'NONE', #169645, #203190, #199995 ) ;
#48050=CARTESIAN_POINT ( 'NONE',  ( -1.737499999999997824, -3.441666666666665986, 3.009438278150925683 ) ) ;
#48085=CARTESIAN_POINT ( 'NONE',  ( -0.9311234436981514762, -1.078119629485602804, -3.474999999999999645 ) ) ;
#48121=CARTESIAN_POINT ( 'NONE',  ( -3.475000000000000533, -2.435416665710753215, -2.006292185433948827 ) ) ;
#48185=EDGE_CURVE ( 'NONE', #144530, #160528, #155801, .T. ) ;
#48206=CARTESIAN_POINT ( 'NONE',  ( -1.642778471874998480, -2.151041666188707957, 2.845375778867863303 ) ) ;
#48237=EDGE_LOOP ( 'NONE', ( #101022, #137261, #5655, #123710, #153540 ) ) ;
#48386=ADVANCED_FACE ( 'NONE', ( #118359 ), #83539, .F. ) ;
#48410=CARTESIAN_POINT ( 'NONE',  ( 1.642778471875001811, -2.442708332855377140, 2.845375778867859751 ) ) ;
#48418=CARTESIAN_POINT ( 'NONE',  ( 1.347111479062088405E-15, 6.999999999999999112, 11.00000000000000000 ) ) ;
#48446=DIRECTION ( 'NONE',  ( -0.000000000000000000, 1.000000000000000000, -0.000000000000000000 ) ) ;
#48546=CARTESIAN_POINT ( 'NONE',  ( 1.642778471875000035, -1.626041666188710044, -2.845375778867859751 ) ) ;
#48586=CARTESIAN_POINT ( 'NONE',  ( 1.737500000000001155, -3.383333333333331971, 3.009438278150922130 ) ) ;
#48588=CARTESIAN_POINT ( 'NONE',  ( -3.285556943750000514, -2.676041666188707424, -1.896917185911906500 ) ) ;
#48646=CYLINDRICAL_SURFACE ( 'NONE', #139951, 11.00000000000000000 ) ;
#48650=CARTESIAN_POINT ( 'NONE',  ( 3.285556943749998737, -0.6927083328553748087, -1.896917185911906500 ) ) ;
#48655=ORIENTED_EDGE ( 'NONE', *, *, #7876, .F. ) ;
#48659=DIRECTION ( 'NONE',  ( 0.000000000000000000, 1.000000000000000000, 0.000000000000000000 ) ) ;
#48694=EDGE_CURVE ( 'NONE', #85130, #60185, #84656, .T. ) ;
#48812=CARTESIAN_POINT ( 'NONE',  ( -3.197123283245616676, -0.9841229182759280159, 1.361626862150112860 ) ) ;
#48825=ADVANCED_FACE ( 'NONE', ( #14112 ), #78070, .F. ) ;
#48839=CARTESIAN_POINT ( 'NONE',  ( 0.000000000000000000, -1.246874999522042948, -3.793834371823813001 ) ) ;
#48851=CARTESIAN_POINT ( 'NONE',  ( -0.4577034257980932552, -0.8887487162305418575, -3.253519940713586855 ) ) ;
#48898=CARTESIAN_POINT ( 'NONE',  ( 1.528150327639969719, -3.232243495192087757, 2.908546201585544999 ) ) ;
#48910=CARTESIAN_POINT ( 'NONE',  ( 2.960183528328370173, -4.197067547847380453, -1.425551791145183156 ) ) ;
#48968=ADVANCED_FACE ( 'NONE', ( #47734 ), #180494, .T. ) ;
#48979=CARTESIAN_POINT ( 'NONE',  ( 2.540449947701581390, -3.218732648277128572, 2.112750016026112565 ) ) ;
#48985=CARTESIAN_POINT ( 'NONE',  ( 0.000000000000000000, 0.5000000000000004441, 0.000000000000000000 ) ) ;
#48995=CARTESIAN_POINT ( 'NONE',  ( -3.459886018179104017, -0.007765290029630126691, -0.2323671850544757334 ) ) ;
#49005=CARTESIAN_POINT ( 'NONE',  ( -3.283337425626721373, -0.1112512837626866702, -0.1207467602163218856 ) ) ;
#49007=CARTESIAN_POINT ( 'NONE',  ( -3.475000000000000533, -3.499999999999999556, 0.000000000000000000 ) ) ;
#49095=CARTESIAN_POINT ( 'NONE',  ( 3.475000000000000533, -3.295833333333334725, -2.006292185433951047 ) ) ;
#49118=VECTOR ( 'NONE', #132168, 1000.000000000000000 ) ;
#49169=CARTESIAN_POINT ( 'NONE',  ( 1.001543065824772753E-15, -2.318749999044082966, 4.012584370867899430 ) ) ;
#49173=CIRCLE ( 'NONE', #111387, 2.150000000000000799 ) ;
#49231=CARTESIAN_POINT ( 'NONE',  ( -1.737499999999997824, -0.9916666666666684726, 3.009438278150925683 ) ) ;
#49255=CARTESIAN_POINT ( 'NONE',  ( 0.000000000000000000, -1.596874999522041705, -3.793834371823813001 ) ) ;
#49320=ORIENTED_EDGE ( 'NONE', *, *, #48185, .F. ) ;
#49451=CARTESIAN_POINT ( 'NONE',  ( -3.285556943750000070, -2.909374999522040817, 0.000000000000000000 ) ) ;
#49544=ORIENTED_EDGE ( 'NONE', *, *, #102718, .F. ) ;
#49583=CIRCLE ( 'NONE', #46218, 3.150000000000000799 ) ;
#49592=CARTESIAN_POINT ( 'NONE',  ( 3.285556943749998737, -3.405208332855374831, -1.896917185911906500 ) ) ;
#49609=CARTESIAN_POINT ( 'NONE',  ( -1.393942678861017415, 0.9000000000000014655, 1.636894562288534694 ) ) ;
#49631=CARTESIAN_POINT ( 'NONE',  ( -1.737499999999997824, -3.791666666666665186, 3.009438278150925683 ) ) ;
#49634=CARTESIAN_POINT ( 'NONE',  ( 1.642778471875001811, -3.230208332855373676, 2.845375778867859751 ) ) ;
#49640=SURFACE_STYLE_USAGE ( .BOTH. , #111510 ) ;
#49667=ORIENTED_EDGE ( 'NONE', *, *, #84346, .F. ) ;
#49677=DIRECTION ( 'NONE',  ( 0.000000000000000000, -1.000000000000000000, 0.000000000000000000 ) ) ;
#49700=CARTESIAN_POINT ( 'NONE',  ( -1.642778471875000035, -0.9552083328553742092, -2.845375778867859751 ) ) ;
#49702=CARTESIAN_POINT ( 'NONE',  ( 0.000000000000000000, 0.5000000000000004441, -3.475000000000000089 ) ) ;
#49776=ORIENTED_EDGE ( 'NONE', *, *, #175293, .F. ) ;
#49812=VERTEX_POINT ( 'NONE', #139939 ) ;
#49895=CARTESIAN_POINT ( 'NONE',  ( 1.642778471875000035, -3.026041666188708401, -2.845375778867859751 ) ) ;
#49962=CYLINDRICAL_SURFACE ( 'NONE', #127152, 10.25000000000000000 ) ;
#49966=CARTESIAN_POINT ( 'NONE',  ( -1.642778471875000035, -3.405208332855375275, -2.845375778867859751 ) ) ;
#50063=CARTESIAN_POINT ( 'NONE',  ( 1.001543065824772753E-15, -3.062499999999998668, 4.012584370867899430 ) ) ;
#50092=ORIENTED_EDGE ( 'NONE', *, *, #95039, .T. ) ;
#50224=CARTESIAN_POINT ( 'NONE',  ( 1.737500000000001155, -3.689583332377416980, 3.009438278150922130 ) ) ;
#50312=CARTESIAN_POINT ( 'NONE',  ( 3.285556943750000514, -2.413541666188708579, 1.896917185911906500 ) ) ;
#50342=ORIENTED_EDGE ( 'NONE', *, *, #128454, .F. ) ;
#50381=AXIS2_PLACEMENT_3D ( 'NONE', #25026, #58607, #9847 ) ;
#50503=CARTESIAN_POINT ( 'NONE',  ( -1.737499999999997824, -2.697916665710752060, 3.009438278150925683 ) ) ;
#50506=CARTESIAN_POINT ( 'NONE',  ( -3.291193844602480212, -0.1067382855773401085, -0.04028451622573153701 ) ) ;
#50513=CARTESIAN_POINT ( 'NONE',  ( -3.285556943750000514, -2.938541666188710266, -1.896917185911906500 ) ) ;
#50630=DIRECTION ( 'NONE',  ( 0.000000000000000000, 1.000000000000000000, 0.000000000000000000 ) ) ;
#50658=CARTESIAN_POINT ( 'NONE',  ( 1.737500000000001155, -0.2333333333333319215, 3.009438278150922130 ) ) ;
#50688=CARTESIAN_POINT ( 'NONE',  ( 0.000000000000000000, 0.5000000000000004441, 0.000000000000000000 ) ) ;
#50695=ORIENTED_EDGE ( 'NONE', *, *, #60337, .F. ) ;
#50700=CARTESIAN_POINT ( 'NONE',  ( 3.475000000000000533, -3.645833333333333037, -2.006292185433951047 ) ) ;
#50702=CARTESIAN_POINT ( 'NONE',  ( -1.642778471874998480, -3.638541666188710444, 2.845375778867863303 ) ) ;
#50763=CARTESIAN_POINT ( 'NONE',  ( -1.642778471875000035, -1.305208332855377407, -2.845375778867859751 ) ) ;
#50766=CARTESIAN_POINT ( 'NONE',  ( 3.475000000000000533, -1.852083332377418401, -2.006292185433951047 ) ) ;
#50820=CARTESIAN_POINT ( 'NONE',  ( -2.768263461985202234, -0.8887487162373161054, -1.782739746934519198 ) ) ;
#50851=DIRECTION ( 'NONE',  ( 0.000000000000000000, -1.000000000000000000, -0.000000000000000000 ) ) ;
#50961=CARTESIAN_POINT ( 'NONE',  ( -1.642778471875000035, -1.917708332855375897, -2.845375778867859751 ) ) ;
#51050=ORIENTED_EDGE ( 'NONE', *, *, #146654, .T. ) ;
#51077=EDGE_CURVE ( 'NONE', #56590, #88193, #6840, .T. ) ;
#51114=CARTESIAN_POINT ( 'NONE',  ( -3.426641765799319561, -0.01965654466554235882, -0.4167094806288151321 ) ) ;
#51128=CARTESIAN_POINT ( 'NONE',  ( 1.737500000000001155, -3.733333333333331616, 3.009438278150922130 ) ) ;
#51156=ORIENTED_EDGE ( 'NONE', *, *, #15800, .T. ) ;
#51190=PLANE ( 'NONE',  #94333 ) ;
#51220=CARTESIAN_POINT ( 'NONE',  ( 1.737499999999999378, -2.916666666666668295, -3.009438278150925683 ) ) ;
#51256=CARTESIAN_POINT ( 'NONE',  ( 0.6628206911954310776, -0.9086430318470575251, -3.411154667337676916 ) ) ;
#51292=CARTESIAN_POINT ( 'NONE',  ( -3.474999999999998312, -4.127083332377416980, 2.006292185433951047 ) ) ;
#51334=( BOUNDED_SURFACE ( )  B_SPLINE_SURFACE ( 1, 2, ( 
 ( #162400, #98456, #95281, #112639, #127855, #13976, #129974, #94212, #32391, #178648, #64876, #145109, #65915, #195961, #197014, #179714, #193805, #48650, #16106, #211115, #15043, #31331, #97408, #161329, #163463, #45454, #49700, #132062, #12913, #198072, #160252, #144051, #1983, #115828, #33447, #69121, #68047, #135242, #50763, #83252, #35570, #149336, #99524, #119030, #52896, #150416, #51846, #167717, #181815, #21433, #916, #185012, #134184, #19320, #183959, #200193, #166656, #201256, #37718, #117965, #18246, #85396, #101650, #36639, #103796, #151482, #3052, #102723, #17177, #199120, #20385, #168780, #86469, #152533, #4118, #66983, #70187, #84330, #136299, #202322, #116893, #133121, #53971, #165583, #120108, #186087, #169846, #87541, #153610, #5181, #100582, #71257, #137370, #203387, #182892, #34509, #55040, #6258, #154673, #59296, #72329, #57172, #123334, #206608, #189298, #39862, #108123, #23585, #91832, #8406, #56107, #187158, #138435, #121189, #88618, #155743, #105971, #7328, #171993, #170913, #140597, #38787, #58237, #174150, #104868, #89692, #190352, #9483, #125455, #42014, #92896, #73405, #22508, #139508, #40938, #107043, #205535, #157891, #141666 ),
 ( #173070, #204453, #24651, #90758, #122264, #156819, #175209, #188222, #74491, #124394, #25723, #75555, #207677, #191417, #43084, #109197, #158941, #26791, #10537, #76610, #142724, #110257, #11606, #27867, #46270, #176266, #210871, #32137, #129725, #143801, #62496, #208733, #128661, #78740, #209798, #161075, #114522, #61433, #45209, #12666, #144864, #93964, #127600, #194627, #146978, #97160, #98218, #112387, #126523, #212996, #178399, #160005, #77680, #193566, #30011, #111323, #96095, #164269, #195709, #177327, #28941, #162150, #13737, #60360, #180517, #95025, #211934, #79810, #145922, #63568, #47344, #113458, #179463, #130772, #31087, #163215, #14797, #80888, #64633, #196767, #48410, #15858, #81945, #192484, #44136, #52640, #117714, #183704, #101389, #167464, #181566, #19060, #198866, #182630, #36381, #82999, #49451, #50513, #65663, #84072, #116635, #202051, #200995, #20123, #51589, #132862, #134984, #37453, #151225, #149075, #2794, #148028, #99277, #33194, #152280, #165326, #150161, #1729, #85138, #67786, #34253, #118769, #100325, #184753, #68865, #652, #131811, #16919, #214038, #66718, #166392, #17983, #133936, #199941, #115570, #102459, #197820, #168525, #86209 ) ),
 .UNSPECIFIED., .F., .F., .T. ) 
 B_SPLINE_SURFACE_WITH_KNOTS ( ( 2, 2 ),
 ( 3, 2, 2, 2, 2, 2, 2, 2, 2, 2, 2, 2, 2, 2, 2, 2, 2, 2, 2, 2, 2, 2, 2, 2, 2, 2, 2, 2, 2, 2, 2, 2, 2, 2, 2, 2, 2, 2, 2, 2, 2, 2, 2, 2, 2, 2, 2, 2, 2, 2, 2, 2, 2, 2, 2, 2, 2, 2, 2, 2, 2, 2, 2, 2, 2, 2, 2, 2, 2, 3 ),
 ( 0.000000000000000000, 1.000000000000000000 ),
 ( 0.000000000000000000, 0.01388888888888888812, 0.02777777777777777624, 0.04166666666666666435, 0.05555555555555555247, 0.06944444444444444753, 0.08333333333333332871, 0.09722222222222222376, 0.1111111111111111049, 0.1250000000000000000, 0.1388888888888888951, 0.1527777777777777901, 0.1666666666666666574, 0.1805555555555555525, 0.1944444444444444475, 0.2083333333333333426, 0.2222222222222222099, 0.2361111111111111049, 0.2500000000000000000, 0.2638888888888888951, 0.2777777777777777901, 0.2916666666666666852, 0.3055555555555555802, 0.3194444444444444198, 0.3333333333333333148, 0.3472222222222222099, 0.3611111111111111049, 0.3750000000000000000, 0.3888888888888888951, 0.4027777777777777901, 0.4166666666666666852, 0.4305555555555555802, 0.4444444444444444198, 0.4583333333333333148, 0.4722222222222222099, 0.4861111111111111049, 0.5000000000000000000, 0.5138888888888888395, 0.5277777777777777901, 0.5416666666666666297, 0.5555555555555555802, 0.5694444444444444198, 0.5833333333333333703, 0.5972222222222222099, 0.6111111111111111605, 0.6250000000000000000, 0.6388888888888888395, 0.6527777777777777901, 0.6666666666666666297, 0.6805555555555555802, 0.6944444444444444198, 0.7083333333333333703, 0.7222222222222222099, 0.7361111111111111605, 0.7500000000000000000, 0.7638888888888888395, 0.7777777777777777901, 0.7916666666666666297, 0.8055555555555555802, 0.8194444444444444198, 0.8333333333333333703, 0.8472222222222222099, 0.8611111111111111605, 0.8750000000000000000, 0.8888888888888888395, 0.9027777777777777901, 0.9166666666666666297, 0.9305555555555555802, 0.9444444444444444198, 0.9523586353390159909 ),
 .UNSPECIFIED. ) 
 GEOMETRIC_REPRESENTATION_ITEM ( )  RATIONAL_B_SPLINE_SURFACE ( (
 ( 1.000000000000000000, 0.8660254037844387076, 1.000000000000000000, 0.8660254037844387076, 1.000000000000000000, 0.8660254037844387076, 1.000000000000000000, 0.8660254037844387076, 1.000000000000000000, 0.8660254037844387076, 1.000000000000000000, 0.8660254037844387076, 1.000000000000000000, 0.8660254037844387076, 1.000000000000000000, 0.8660254037844387076, 1.000000000000000000, 0.8660254037844387076, 1.000000000000000000, 0.8660254037844387076, 1.000000000000000000, 0.8660254037844387076, 1.000000000000000000, 0.8660254037844387076, 1.000000000000000000, 0.8660254037844387076, 1.000000000000000000, 0.8660254037844387076, 1.000000000000000000, 0.8660254037844387076, 1.000000000000000000, 0.8660254037844387076, 1.000000000000000000, 0.8660254037844387076, 1.000000000000000000, 0.8660254037844387076, 1.000000000000000000, 0.8660254037844387076, 1.000000000000000000, 0.8660254037844387076, 1.000000000000000000, 0.8660254037844387076, 1.000000000000000000, 0.8660254037844387076, 1.000000000000000000, 0.8660254037844387076, 1.000000000000000000, 0.8660254037844387076, 1.000000000000000000, 0.8660254037844387076, 1.000000000000000000, 0.8660254037844387076, 1.000000000000000000, 0.8660254037844387076, 1.000000000000000000, 0.8660254037844387076, 1.000000000000000000, 0.8660254037844387076, 1.000000000000000000, 0.8660254037844387076, 1.000000000000000000, 0.8660254037844387076, 1.000000000000000000, 0.8660254037844387076, 1.000000000000000000, 0.8660254037844387076, 1.000000000000000000, 0.8660254037844387076, 1.000000000000000000, 0.8660254037844387076, 1.000000000000000000, 0.8660254037844387076, 1.000000000000000000, 0.8660254037844387076, 1.000000000000000000, 0.8660254037844387076, 1.000000000000000000, 0.8660254037844387076, 1.000000000000000000, 0.8660254037844387076, 1.000000000000000000, 0.8660254037844387076, 1.000000000000000000, 0.8660254037844387076, 1.000000000000000000, 0.8660254037844387076, 1.000000000000000000, 0.8660254037844387076, 1.000000000000000000, 0.8660254037844387076, 1.000000000000000000, 0.8660254037844387076, 1.000000000000000000, 0.8660254037844387076, 1.000000000000000000, 0.8660254037844387076, 1.000000000000000000, 0.8660254037844387076, 1.000000000000000000, 0.8660254037844387076, 1.000000000000000000, 0.8660254037844387076, 1.000000000000000000, 0.8660254037844387076, 1.000000000000000000, 0.8660254037844387076, 1.000000000000000000, 0.8660254037844387076, 1.000000000000000000, 0.8660254037844387076, 1.000000000000000000, 0.8660254037844387076, 1.000000000000000000, 0.8660254037844387076, 1.000000000000000000, 0.8660254037844387076, 1.000000000000000000, 0.8660254037844387076, 1.000000000000000000, 0.8660254037844387076, 1.000000000000000000, 0.8660254037844387076, 1.000000000000000000, 0.8660254037844387076, 1.000000000000000000, 0.8660254037844387076, 1.000000000000000000, 0.8660254037844387076, 1.000000000000000000, 0.8660254037844387076, 1.000000000000000000, 0.8660254037844387076, 1.000000000000000000, 0.8660254037844387076, 1.000000000000000000, 0.8660254037844387076, 1.000000000000000000, 0.9236583618779372618, 0.9343189745674063129),
 ( 1.000000000000000000, 0.8660254037844387076, 1.000000000000000000, 0.8660254037844387076, 1.000000000000000000, 0.8660254037844387076, 1.000000000000000000, 0.8660254037844387076, 1.000000000000000000, 0.8660254037844387076, 1.000000000000000000, 0.8660254037844387076, 1.000000000000000000, 0.8660254037844387076, 1.000000000000000000, 0.8660254037844387076, 1.000000000000000000, 0.8660254037844387076, 1.000000000000000000, 0.8660254037844387076, 1.000000000000000000, 0.8660254037844387076, 1.000000000000000000, 0.8660254037844387076, 1.000000000000000000, 0.8660254037844387076, 1.000000000000000000, 0.8660254037844387076, 1.000000000000000000, 0.8660254037844387076, 1.000000000000000000, 0.8660254037844387076, 1.000000000000000000, 0.8660254037844387076, 1.000000000000000000, 0.8660254037844387076, 1.000000000000000000, 0.8660254037844387076, 1.000000000000000000, 0.8660254037844387076, 1.000000000000000000, 0.8660254037844387076, 1.000000000000000000, 0.8660254037844387076, 1.000000000000000000, 0.8660254037844387076, 1.000000000000000000, 0.8660254037844387076, 1.000000000000000000, 0.8660254037844387076, 1.000000000000000000, 0.8660254037844387076, 1.000000000000000000, 0.8660254037844387076, 1.000000000000000000, 0.8660254037844387076, 1.000000000000000000, 0.8660254037844387076, 1.000000000000000000, 0.8660254037844387076, 1.000000000000000000, 0.8660254037844387076, 1.000000000000000000, 0.8660254037844387076, 1.000000000000000000, 0.8660254037844387076, 1.000000000000000000, 0.8660254037844387076, 1.000000000000000000, 0.8660254037844387076, 1.000000000000000000, 0.8660254037844387076, 1.000000000000000000, 0.8660254037844387076, 1.000000000000000000, 0.8660254037844387076, 1.000000000000000000, 0.8660254037844387076, 1.000000000000000000, 0.8660254037844387076, 1.000000000000000000, 0.8660254037844387076, 1.000000000000000000, 0.8660254037844387076, 1.000000000000000000, 0.8660254037844387076, 1.000000000000000000, 0.8660254037844387076, 1.000000000000000000, 0.8660254037844387076, 1.000000000000000000, 0.8660254037844387076, 1.000000000000000000, 0.8660254037844387076, 1.000000000000000000, 0.8660254037844387076, 1.000000000000000000, 0.8660254037844387076, 1.000000000000000000, 0.8660254037844387076, 1.000000000000000000, 0.8660254037844387076, 1.000000000000000000, 0.8660254037844387076, 1.000000000000000000, 0.8660254037844387076, 1.000000000000000000, 0.8660254037844387076, 1.000000000000000000, 0.8660254037844387076, 1.000000000000000000, 0.8660254037844387076, 1.000000000000000000, 0.8660254037844387076, 1.000000000000000000, 0.8660254037844387076, 1.000000000000000000, 0.8660254037844387076, 1.000000000000000000, 0.8660254037844387076, 1.000000000000000000, 0.8660254037844387076, 1.000000000000000000, 0.8660254037844387076, 1.000000000000000000, 0.8660254037844387076, 1.000000000000000000, 0.8660254037844387076, 1.000000000000000000, 0.8660254037844387076, 1.000000000000000000, 0.8660254037844387076, 1.000000000000000000, 0.8660254037844387076, 1.000000000000000000, 0.8660254037844387076, 1.000000000000000000, 0.9236583618779372618, 0.9343189745674063129) ) ) 
 REPRESENTATION_ITEM ( '' )  SURFACE ( )  );
#51349=DIRECTION ( 'NONE',  ( 0.000000000000000000, 0.000000000000000000, -1.000000000000000000 ) ) ;
#51380=ADVANCED_FACE ( 'NONE', ( #157403 ), #25242, .T. ) ;
#51384=CARTESIAN_POINT ( 'NONE',  ( 1.642778471875001811, -2.092708332855373943, 2.845375778867859751 ) ) ;
#51429=DIRECTION ( 'NONE',  ( 0.000000000000000000, -1.000000000000000000, 0.000000000000000000 ) ) ;
#51476=EDGE_LOOP ( 'NONE', ( #32767, #87042, #62091, #44278 ) ) ;
#51488=VECTOR ( 'NONE', #168508, 1000.000000000000000 ) ;
#51495=FACE_OUTER_BOUND ( 'NONE', #176818, .T. ) ;
#51499=VERTEX_POINT ( 'NONE', #44724 ) ;
#51589=CARTESIAN_POINT ( 'NONE',  ( 1.642778471875001811, -3.142708332855375986, 2.845375778867859751 ) ) ;
#51607=CARTESIAN_POINT ( 'NONE',  ( -1.620863580070949883, 0.5000000000000004441, 1.903365770102947607 ) ) ;
#51632=CARTESIAN_POINT ( 'NONE',  ( 1.394453263437886604E-15, -2.668749999044085275, 3.474999999999999645 ) ) ;
#51667=ORIENTED_EDGE ( 'NONE', *, *, #103372, .T. ) ;
#51709=CIRCLE ( 'NONE', #103500, 2.500000000000000888 ) ;
#51739=CARTESIAN_POINT ( 'NONE',  ( 1.642778471875000035, -4.076041666188710444, -2.845375778867859751 ) ) ;
#51787=CARTESIAN_POINT ( 'NONE',  ( 1.642778471875000035, -1.976041666188709689, -2.845375778867859751 ) ) ;
#51817=EDGE_LOOP ( 'NONE', ( #50342, #77428 ) ) ;
#51846=CARTESIAN_POINT ( 'NONE',  ( -1.642778471874998480, -1.538541666188709245, 2.845375778867863303 ) ) ;
#51928=EDGE_CURVE ( 'NONE', #192349, #142998, #194128, .T. ) ;
#51972=ORIENTED_EDGE ( 'NONE', *, *, #66641, .F. ) ;
#51986=CARTESIAN_POINT ( 'NONE',  ( -1.500000000000035971, 7.750000000000000000, -9.886859966642584041 ) ) ;
#52002=CARTESIAN_POINT ( 'NONE',  ( -3.384026120672947613, -0.9549381201899959093, 0.2424983683859719685 ) ) ;
#52031=CARTESIAN_POINT ( 'NONE',  ( 0.000000000000000000, -1.596874999522041705, -3.793834371823813001 ) ) ;
#52158=FACE_OUTER_BOUND ( 'NONE', #139922, .T. ) ;
#52167=CARTESIAN_POINT ( 'NONE',  ( 0.000000000000000000, 1.000000000000000888, 0.000000000000000000 ) ) ;
#52177=ADVANCED_FACE ( 'NONE', ( #187978, #20137 ), #3868, .T. ) ;
#52182=CARTESIAN_POINT ( 'NONE',  ( -3.425116838706585565, -0.02043104031221949779, -0.4185867116033271107 ) ) ;
#52227=EDGE_CURVE ( 'NONE', #111991, #37457, #186912, .T. ) ;
#52259=CARTESIAN_POINT ( 'NONE',  ( 1.458777222063855294, 1.000000000000000888, -1.713029193092652447 ) ) ;
#52320=CARTESIAN_POINT ( 'NONE',  ( 0.000000000000000000, -2.296874999522042327, -3.793834371823813445 ) ) ;
#52356=CARTESIAN_POINT ( 'NONE',  ( -3.285556943750000070, -0.8968749995220438587, 0.000000000000000000 ) ) ;
#52418=CARTESIAN_POINT ( 'NONE',  ( -3.474999999999997868, -1.020833333333332815, 2.006292185433951047 ) ) ;
#52444=CARTESIAN_POINT ( 'NONE',  ( 3.285556943749998737, -0.9552083328553737651, -1.896917185911906500 ) ) ;
#52566=ORIENTED_EDGE ( 'NONE', *, *, #66641, .T. ) ;
#52625=LINE ( 'NONE', #36365, #51488 ) ;
#52640=CARTESIAN_POINT ( 'NONE',  ( -3.285556943750000514, -2.588541666188707513, -1.896917185911906500 ) ) ;
#52789=CARTESIAN_POINT ( 'NONE',  ( 0.000000000000000000, -4.046874999522043659, -3.793834371823813001 ) ) ;
#52831=CARTESIAN_POINT ( 'NONE',  ( -1.737500000000000266, -3.558333333333333570, -3.009438278150923907 ) ) ;
#52833=CARTESIAN_POINT ( 'NONE',  ( 0.000000000000000000, -0.5468749995220422155, -3.793834371823813001 ) ) ;
#52896=CARTESIAN_POINT ( 'NONE',  ( 1.642778471875001811, -1.480208332855375453, 2.845375778867859751 ) ) ;
#52913=DIRECTION ( 'NONE',  ( 0.000000000000000000, -1.000000000000000000, 0.000000000000000000 ) ) ;
#52916=VECTOR ( 'NONE', #203580, 1000.000000000000000 ) ;
#52976=AXIS2_PLACEMENT_3D ( 'NONE', #19243, #118959, #4044 ) ;
#53012=( BOUNDED_CURVE ( )  B_SPLINE_CURVE ( 2, ( #167144, #51256, #100002, #38205, #68539, #166069, #168202, #153020, #202808, #121675, #134667, #34984, #154092, #69606, #4595, #120600, #200670, #17656, #84813, #102133, #186577, #71740, #187640, #55519, #83739, #18729, #5660, #104279, #19801, #170323, #184436, #137854, #21911, #149831, #1401, #101055, #88020, #169267, #203875, #67462, #133608, #199613, #183378, #150902, #37126, #20853, #2463, #185501, #103205, #52320, #118449, #36053, #85885, #135713, #151961, #3531, #201739, #53380, #119515, #194245, #108802, #160686, #75171, #144480, #211547, #93573, #95713, #92516, #78359, #29628, #61049, #63182, #127209, #126132, #109872, #13358, #193177, #12281, #142337, #141281, #143408, #207289, #175885 ),
 .UNSPECIFIED., .F., .T. ) 
 B_SPLINE_CURVE_WITH_KNOTS ( ( 3, 2, 2, 2, 2, 2, 2, 2, 2, 2, 2, 2, 2, 2, 2, 2, 2, 2, 2, 2, 2, 2, 2, 2, 2, 2, 2, 2, 2, 2, 2, 2, 2, 2, 2, 2, 2, 2, 2, 2, 2, 3 ),
 ( 0.1856859352924667417, 0.1944444444444444475, 0.2083333333333333426, 0.2222222222222222099, 0.2361111111111111049, 0.2500000000000000000, 0.2638888888888888951, 0.2777777777777777901, 0.2916666666666666852, 0.3055555555555555802, 0.3194444444444444198, 0.3333333333333333148, 0.3472222222222222099, 0.3611111111111111049, 0.3750000000000000000, 0.3888888888888888951, 0.4027777777777777901, 0.4166666666666666852, 0.4305555555555555802, 0.4444444444444444198, 0.4583333333333333148, 0.4722222222222222099, 0.4861111111111111049, 0.5000000000000000000, 0.5138888888888888395, 0.5277777777777777901, 0.5416666666666666297, 0.5555555555555555802, 0.5694444444444444198, 0.5833333333333333703, 0.5972222222222222099, 0.6111111111111111605, 0.6250000000000000000, 0.6388888888888888395, 0.6527777777777777901, 0.6666666666666667407, 0.6805555555555555802, 0.6944444444444444198, 0.7083333333333332593, 0.7222222222222220989, 0.7361111111111111605, 0.7435077961461751261 ),
 .UNSPECIFIED. ) 
 CURVE ( )  GEOMETRIC_REPRESENTATION_ITEM ( )  RATIONAL_B_SPLINE_CURVE ( ( 0.9375838258011983672, 0.9155139236497713551, 1.000000000000000000, 0.8660254037844387076, 1.000000000000000000, 0.8660254037844387076, 1.000000000000000000, 0.8660254037844387076, 1.000000000000000000, 0.8660254037844387076, 1.000000000000000000, 0.8660254037844387076, 1.000000000000000000, 0.8660254037844387076, 1.000000000000000000, 0.8660254037844387076, 1.000000000000000000, 0.8660254037844387076, 1.000000000000000000, 0.8660254037844387076, 1.000000000000000000, 0.8660254037844387076, 1.000000000000000000, 0.8660254037844387076, 1.000000000000000000, 0.8660254037844387076, 1.000000000000000000, 0.8660254037844387076, 1.000000000000000000, 0.8660254037844387076, 1.000000000000000000, 0.8660254037844387076, 1.000000000000000000, 0.8660254037844387076, 1.000000000000000000, 0.8660254037844387076, 1.000000000000000000, 0.8660254037844387076, 1.000000000000000000, 0.8660254037844387076, 1.000000000000000000, 0.8660254037844387076, 1.000000000000000000, 0.8660254037844387076, 1.000000000000000000, 0.8660254037844387076, 1.000000000000000000, 0.8660254037844387076, 1.000000000000000000, 0.8660254037844387076, 1.000000000000000000, 0.8660254037844387076, 1.000000000000000000, 0.8660254037844387076, 1.000000000000000000, 0.8660254037844387076, 1.000000000000000000, 0.8660254037844387076, 1.000000000000000000, 0.8660254037844387076, 1.000000000000000000, 0.8660254037844387076, 1.000000000000000000, 0.8660254037844387076, 1.000000000000000000, 0.8660254037844387076, 1.000000000000000000, 0.8660254037844387076, 1.000000000000000000, 0.8660254037844387076, 1.000000000000000000, 0.8660254037844387076, 1.000000000000000000, 0.8660254037844387076, 1.000000000000000000, 0.8660254037844387076, 1.000000000000000000, 0.8660254037844387076, 1.000000000000000000, 0.8660254037844387076, 1.000000000000000000, 0.9286503118547393409, 0.9332967922701964625 ) ) 
 REPRESENTATION_ITEM ( '' )  );
#53039=EDGE_CURVE ( 'NONE', #145305, #160077, #106576, .T. ) ;
#53053=CARTESIAN_POINT ( 'NONE',  ( -3.375444385298249195, -0.9484041558699626284, 0.1508549929727657779 ) ) ;
#53083=CARTESIAN_POINT ( 'NONE',  ( 3.285556943749998737, -3.055208332855376518, -1.896917185911906500 ) ) ;
#53085=CARTESIAN_POINT ( 'NONE',  ( 0.000000000000000000, 2.499999999999998668, -4.500000000000000000 ) ) ;
#53090=CARTESIAN_POINT ( 'NONE',  ( 3.475000000000000533, -1.254166666666665098, 2.006292185433948827 ) ) ;
#53168=ORIENTED_EDGE ( 'NONE', *, *, #106621, .T. ) ;
#53236=ORIENTED_EDGE ( 'NONE', *, *, #58935, .F. ) ;
#53239=EDGE_CURVE ( 'NONE', #146583, #64997, #10735, .T. ) ;
#53280=CARTESIAN_POINT ( 'NONE',  ( 0.000000000000000000, 2.000000000000001776, -10.25000000000000000 ) ) ;
#53281=ORIENTED_EDGE ( 'NONE', *, *, #78072, .T. ) ;
#53285=DIRECTION ( 'NONE',  ( -0.6483454320283799088, 0.000000000000000000, 0.7613463080411786432 ) ) ;
#53296=CARTESIAN_POINT ( 'NONE',  ( 0.000000000000000000, 0.000000000000000000, 0.000000000000000000 ) ) ;
#53380=CARTESIAN_POINT ( 'NONE',  ( -3.285556943749998737, -2.530208332855374831, 1.896917185911908721 ) ) ;
#53412=CARTESIAN_POINT ( 'NONE',  ( -3.475000000000000533, -3.806249999044084564, 0.000000000000000000 ) ) ;
#53505=CARTESIAN_POINT ( 'NONE',  ( 1.642778471875000035, -4.076041666188710444, -2.845375778867859751 ) ) ;
#53541=ADVANCED_FACE ( 'NONE', ( #196315 ), #212544, .F. ) ;
#53711=DIRECTION ( 'NONE',  ( -3.706092522800016599E-15, 0.000000000000000000, -1.000000000000000000 ) ) ;
#53735=CARTESIAN_POINT ( 'NONE',  ( 3.475000000000000533, -1.560416665710748996, 2.006292185433948827 ) ) ;
#53846=DIRECTION ( 'NONE',  ( 0.000000000000000000, 1.000000000000000000, 0.000000000000000000 ) ) ;
#53868=CARTESIAN_POINT ( 'NONE',  ( -3.285556943750000514, -3.288541666188709023, -1.896917185911906500 ) ) ;
#53910=CARTESIAN_POINT ( 'NONE',  ( -3.285556943750000070, -1.859374999522041882, 0.000000000000000000 ) ) ;
#53971=CARTESIAN_POINT ( 'NONE',  ( -1.642778471874998480, -2.588541666188707957, 2.845375778867863303 ) ) ;
#53987=CARTESIAN_POINT ( 'NONE',  ( 1.500000000000032641, 7.750000000000000000, 9.886859966642587594 ) ) ;
#54161=CARTESIAN_POINT ( 'NONE',  ( -3.285556943750000070, -2.209374999522041527, 0.000000000000000000 ) ) ;
#54262=AXIS2_PLACEMENT_3D ( 'NONE', #69116, #123330, #185009 ) ;
#54356=PLANE ( 'NONE',  #47782 ) ;
#54372=AXIS2_PLACEMENT_3D ( 'NONE', #126480, #176226, #27828 ) ;
#54427=ORIENTED_EDGE ( 'NONE', *, *, #31849, .F. ) ;
#54434=CARTESIAN_POINT ( 'NONE',  ( 3.285556943750000514, -0.4010416661887095113, 1.896917185911906500 ) ) ;
#54489=CARTESIAN_POINT ( 'NONE',  ( 1.642778471875001811, -0.4302083328553765740, 2.845375778867859751 ) ) ;
#54510=CARTESIAN_POINT ( 'NONE',  ( -1.431838407952683134, -3.232243495192085092, 2.960863168642819510 ) ) ;
#54574=CARTESIAN_POINT ( 'NONE',  ( 3.285556943749998737, -3.055208332855376518, -1.896917185911906500 ) ) ;
#54636=DIRECTION ( 'NONE',  ( 0.000000000000000000, 1.000000000000000000, 0.000000000000000000 ) ) ;
#54700=VERTEX_POINT ( 'NONE', #203776 ) ;
#54733=PLANE ( 'NONE',  #59725 ) ;
#54793=DIRECTION ( 'NONE',  ( 0.000000000000000000, -1.000000000000000000, 0.000000000000000000 ) ) ;
#54978=CARTESIAN_POINT ( 'NONE',  ( 3.285556943750000070, -1.334374999522040861, 0.000000000000000000 ) ) ;
#55040=CARTESIAN_POINT ( 'NONE',  ( -3.285556943750000070, -2.996874999522041616, 0.000000000000000000 ) ) ;
#55124=CARTESIAN_POINT ( 'NONE',  ( 2.529878086979381546, -0.9588891237051863081, 2.284325849096846106 ) ) ;
#55184=VERTEX_POINT ( 'NONE', #161087 ) ;
#55228=CARTESIAN_POINT ( 'NONE',  ( -1.642778471874998480, -3.551041666188709645, 2.845375778867863303 ) ) ;
#55319=DIRECTION ( 'NONE',  ( 0.000000000000000000, -1.000000000000000000, 0.000000000000000000 ) ) ;
#55366=CARTESIAN_POINT ( 'NONE',  ( 0.7941172694243576746, -3.057670337906326807, 3.391178412236372175 ) ) ;
#55408=CARTESIAN_POINT ( 'NONE',  ( 0.000000000000000000, -0.9841229182759280159, 0.000000000000000000 ) ) ;
#55412=ORIENTED_EDGE ( 'NONE', *, *, #208932, .T. ) ;
#55430=DIRECTION ( 'NONE',  ( 0.000000000000000000, 0.000000000000000000, 1.000000000000000000 ) ) ;
#55495=CARTESIAN_POINT ( 'NONE',  ( 1.642778471875000035, -1.363541666188707646, -2.845375778867859751 ) ) ;
#55519=CARTESIAN_POINT ( 'NONE',  ( -3.285556943750000514, -1.538541666188708357, -1.896917185911906722 ) ) ;
#55534=EDGE_CURVE ( 'NONE', #183045, #202980, #66788, .T. ) ;
#55555=CARTESIAN_POINT ( 'NONE',  ( 3.285556943749998737, -0.6927083328553748087, -1.896917185911906500 ) ) ;
#55637=CARTESIAN_POINT ( 'NONE',  ( -3.285556943749998737, -3.580208332855374653, 1.896917185911908499 ) ) ;
#55664=DIRECTION ( 'NONE',  ( 0.000000000000000000, 0.000000000000000000, 1.000000000000000000 ) ) ;
#55684=ORIENTED_EDGE ( 'NONE', *, *, #142758, .T. ) ;
#55795=CARTESIAN_POINT ( 'NONE',  ( -3.283337425626721373, -0.1112512837626866702, -0.1207467602163218856 ) ) ;
#55855=CARTESIAN_POINT ( 'NONE',  ( 0.000000000000000000, 5.000000000000000888, -10.25000000000000000 ) ) ;
#55864=VECTOR ( 'NONE', #65917, 1000.000000000000000 ) ;
#55880=DIRECTION ( 'NONE',  ( 0.000000000000000000, 1.000000000000000000, 0.000000000000000000 ) ) ;
#55892=VERTEX_POINT ( 'NONE', #39612 ) ;
#55978=CARTESIAN_POINT ( 'NONE',  ( 3.285556943750000070, -1.771874999522041083, 0.000000000000000000 ) ) ;
#55996=EDGE_LOOP ( 'NONE', ( #71832, #195603, #174526, #86847 ) ) ;
#56045=CARTESIAN_POINT ( 'NONE',  ( -1.642778471875000035, -1.567708332855376252, -2.845375778867859751 ) ) ;
#56061=EDGE_CURVE ( 'NONE', #113311, #7325, #171956, .T. ) ;
#56107=CARTESIAN_POINT ( 'NONE',  ( -1.642778471875000035, -3.405208332855375275, -2.845375778867859751 ) ) ;
#56252=EDGE_LOOP ( 'NONE', ( #122776, #87016, #193789, #87725 ) ) ;
#56260=CARTESIAN_POINT ( 'NONE',  ( -1.642778471875000035, -0.1677083328553742592, -2.845375778867859751 ) ) ;
#56290=VERTEX_POINT ( 'NONE', #70760 ) ;
#56295=CARTESIAN_POINT ( 'NONE',  ( -3.285556943749998737, -3.580208332855374653, 1.896917185911908499 ) ) ;
#56330=CARTESIAN_POINT ( 'NONE',  ( -1.737500000000000266, -2.508333333333334636, -3.009438278150923907 ) ) ;
#56449=CARTESIAN_POINT ( 'NONE',  ( 1.734723475976807094E-15, 1.000000000000000888, 0.000000000000000000 ) ) ;
#56486=CIRCLE ( 'NONE', #163795, 11.00000000000000000 ) ;
#56504=CARTESIAN_POINT ( 'NONE',  ( 0.9311234436981525864, -2.653119629485602537, 3.474999999999998757 ) ) ;
#56519=ORIENTED_EDGE ( 'NONE', *, *, #151772, .T. ) ;
#56530=CARTESIAN_POINT ( 'NONE',  ( -3.399419719642636117, 0.06547992991065912372, 0.000000000000000000 ) ) ;
#56548=CARTESIAN_POINT ( 'NONE',  ( 0.9311234436981525864, -2.346869630441518861, 3.474999999999998757 ) ) ;
#56570=CARTESIAN_POINT ( 'NONE',  ( -1.642778471874998480, -0.8385416661887100664, 2.845375778867863303 ) ) ;
#56590=VERTEX_POINT ( 'NONE', #104371 ) ;
#56618=DIRECTION ( 'NONE',  ( -0.000000000000000000, 1.000000000000000000, -0.000000000000000000 ) ) ;
#56623=CARTESIAN_POINT ( 'NONE',  ( -3.285556943749998737, -2.967708332855377051, 1.896917185911908499 ) ) ;
#56712=CARTESIAN_POINT ( 'NONE',  ( -3.285556943750000514, -3.288541666188709023, -1.896917185911906500 ) ) ;
#56718=DIRECTION ( 'NONE',  ( -0.000000000000000000, -1.000000000000000000, -0.000000000000000000 ) ) ;
#56773=CARTESIAN_POINT ( 'NONE',  ( -3.432849766368863964, -0.02876672507445138249, 0.000000000000000000 ) ) ;
#56816=CARTESIAN_POINT ( 'NONE',  ( -1.737500000000000266, -1.414583332377417735, -3.009438278150923907 ) ) ;
#57042=ORIENTED_EDGE ( 'NONE', *, *, #214118, .T. ) ;
#57045=CARTESIAN_POINT ( 'NONE',  ( 3.285556943750000514, -2.151041666188709733, 1.896917185911906722 ) ) ;
#57109=CARTESIAN_POINT ( 'NONE',  ( 3.285556943749998737, -2.355208332855375453, -1.896917185911906500 ) ) ;
#57172=CARTESIAN_POINT ( 'NONE',  ( 3.285556943749998737, -3.142708332855375986, -1.896917185911906500 ) ) ;
#57190=CARTESIAN_POINT ( 'NONE',  ( 0.000000000000000000, -3.517800438942085606, 0.000000000000000000 ) ) ;
#57196=AXIS2_PLACEMENT_3D ( 'NONE', #61810, #30385, #197127 ) ;
#57277=EDGE_CURVE ( 'NONE', #94066, #46791, #204508, .T. ) ;
#57297=DIRECTION ( 'NONE',  ( 0.6483454320283799088, 0.000000000000000000, -0.7613463080411786432 ) ) ;
#57312=CARTESIAN_POINT ( 'NONE',  ( -1.500000000000039524, 6.999999999999999112, -10.89724735885167739 ) ) ;
#57360=CARTESIAN_POINT ( 'NONE',  ( 3.475000000000000533, -0.1750000000000015432, 0.000000000000000000 ) ) ;
#57387=ORIENTED_EDGE ( 'NONE', *, *, #209784, .T. ) ;
#57468=LINE ( 'NONE', #156035, #188871 ) ;
#57526=ORIENTED_EDGE ( 'NONE', *, *, #74644, .T. ) ;
#57601=CARTESIAN_POINT ( 'NONE',  ( -0.4577034257980932552, -0.8887487162305418575, -3.253519940713586855 ) ) ;
#57613=CARTESIAN_POINT ( 'NONE',  ( 1.737500000000001155, -2.333333333333333037, 3.009438278150922130 ) ) ;
#57634=CARTESIAN_POINT ( 'NONE',  ( -3.285556943750000514, -1.626041666188708046, -1.896917185911906500 ) ) ;
#57684=CARTESIAN_POINT ( 'NONE',  ( 1.685698123273788651, -1.399999999999998579, -1.979500400907064916 ) ) ;
#57692=CARTESIAN_POINT ( 'NONE',  ( 1.642778471875001811, -2.180208332855374742, 2.845375778867859751 ) ) ;
#57713=CARTESIAN_POINT ( 'NONE',  ( -2.587713642112661638, -3.232243495192087757, 2.046355377693061861 ) ) ;
#57776=CARTESIAN_POINT ( 'NONE',  ( -3.475000000000000533, -0.3791666666666649865, -2.006292185433948827 ) ) ;
#57806=EDGE_LOOP ( 'NONE', ( #185531, #34363 ) ) ;
#57861=CARTESIAN_POINT ( 'NONE',  ( -3.474999999999998312, -1.020833333333332815, 2.006292185433951047 ) ) ;
#57936=CARTESIAN_POINT ( 'NONE',  ( 3.475000000000000533, -0.4812499990440831654, 0.000000000000000000 ) ) ;
#58059=AXIS2_PLACEMENT_3D ( 'NONE', #142986, #48659, #195973 ) ;
#58096=DIRECTION ( 'NONE',  ( 0.000000000000000000, 0.000000000000000000, -1.000000000000000000 ) ) ;
#58106=CIRCLE ( 'NONE', #106558, 10.92874649719719571 ) ;
#58111=CARTESIAN_POINT ( 'NONE',  ( -3.285556943750000070, -1.946874999522042682, 0.000000000000000000 ) ) ;
#58174=CARTESIAN_POINT ( 'NONE',  ( 1.642778471875000035, -4.076041666188710444, -2.845375778867859751 ) ) ;
#58237=CARTESIAN_POINT ( 'NONE',  ( -1.642778471875000035, -3.755208332855374476, -2.845375778867859751 ) ) ;
#58255=DIRECTION ( 'NONE',  ( -0.000000000000000000, 1.000000000000000000, -0.000000000000000000 ) ) ;
#58389=CARTESIAN_POINT ( 'NONE',  ( 1.642778471875001811, -0.3427083328553758301, 2.845375778867859751 ) ) ;
#58399=CARTESIAN_POINT ( 'NONE',  ( 1.458777222063855294, 0.5999999999999998668, -1.713029193092652225 ) ) ;
#58427=CARTESIAN_POINT ( 'NONE',  ( 3.285556943749998737, -3.405208332855374831, -1.896917185911906500 ) ) ;
#58497=EDGE_CURVE ( 'NONE', #198335, #12234, #126923, .T. ) ;
#58508=ORIENTED_EDGE ( 'NONE', *, *, #95890, .T. ) ;
#58607=DIRECTION ( 'NONE',  ( 1.000000000000000000, 0.000000000000000000, 1.224646799147353207E-16 ) ) ;
#58696=CARTESIAN_POINT ( 'NONE',  ( 1.001543065824772753E-15, -2.209374999522042859, 3.793834371823811669 ) ) ;
#58704=CARTESIAN_POINT ( 'NONE',  ( 1.416652131158681049, 8.000043606524066320, 10.86080395187256897 ) ) ;
#58708=( BOUNDED_SURFACE ( )  B_SPLINE_SURFACE ( 1, 2, ( 
 ( #25427, #157592, #141371, #9187, #90454, #59004, #57936, #60069, #78452, #92604, #106742, #75258, #41716, #8111, #109964, #76321, #207383, #27568, #107826, #125160, #42785, #190064, #24344, #44916, #174917, #156520, #158647, #159708, #143501, #128371, #10245, #142426, #160779, #208435, #11307, #77385, #126225, #74199, #192186, #175974, #209498, #61138, #193270, #111024, #177029, #62214, #140293, #28646, #206312, #94733, #12372, #144570, #210583, #194338, #178104, #79524, #114233, #182334, #161858, #115287, #45980, #149867, #112101, #13447, #83774, #197525, #181278, #145642, #131522, #49169, #95802, #133646, #211637, #48121, #81650, #63273, #129435, #166102, #47048, #147737, #195418, #113164, #132574, #165035, #179168, #148789, #1435, #97930, #100038, #96871, #82711, #33962, #65375, #67500, #32904, #130492, #180231, #17688, #98982, #16628, #146689, #29720, #30792, #162921, #15563, #14501, #198577, #80593, #212705, #64346, #196479, #31854, #163988, #213753, #359, #66431, #50224, #116343, #168236, #199645, #53412, #186611, #21944, #6775, #19835, #134700, #39302, #169301, #38237, #104310, #85921, #51292, #184468, #201772, #170359, #151993, #88054, #3566, #20885 ),
 ( #154126, #69640, #105397, #5696, #183414, #72850, #200705, #71773, #54489, #137889, #121709, #171435, #203908, #23025, #2501, #117416, #103241, #55555, #187672, #153052, #86982, #35017, #119549, #135748, #52356, #118484, #89140, #101088, #155194, #167175, #36085, #18764, #84848, #37163, #150938, #68573, #4628, #102169, #185535, #70700, #136813, #202840, #120633, #110768, #59817, #123849, #93411, #174664, #143248, #44654, #207127, #142168, #208184, #209238, #90205, #58753, #188747, #191928, #108636, #175714, #156269, #125971, #189812, #41462, #7851, #107571, #122788, #206057, #57692, #73938, #124905, #140032, #173605, #25177, #94478, #91279, #176768, #157338, #160518, #27306, #28383, #12122, #8926, #138957, #75007, #40386, #141116, #190868, #42532, #26238, #92355, #158393, #9991, #204978, #76068, #56623, #43592, #106490, #159449, #172516, #24101, #109710, #11047, #77126, #60882, #127041, #193001, #47867, #79269, #164782, #49966, #129181, #131283, #13192, #197270, #32646, #179975, #130232, #146432, #61956, #213504, #95550, #147482, #29461, #181029, #82452, #145386, #46794, #211385, #80331, #162667, #161603, #15310, #65125, #212446, #144321, #30533, #210319, #48910 ) ),
 .UNSPECIFIED., .F., .F., .T. ) 
 B_SPLINE_SURFACE_WITH_KNOTS ( ( 2, 2 ),
 ( 3, 2, 2, 2, 2, 2, 2, 2, 2, 2, 2, 2, 2, 2, 2, 2, 2, 2, 2, 2, 2, 2, 2, 2, 2, 2, 2, 2, 2, 2, 2, 2, 2, 2, 2, 2, 2, 2, 2, 2, 2, 2, 2, 2, 2, 2, 2, 2, 2, 2, 2, 2, 2, 2, 2, 2, 2, 2, 2, 2, 2, 2, 2, 2, 2, 2, 2, 2, 2, 3 ),
 ( 0.000000000000000000, 1.000000000000000000 ),
 ( 0.000000000000000000, 0.01388888888888888812, 0.02777777777777777624, 0.04166666666666666435, 0.05555555555555555247, 0.06944444444444444753, 0.08333333333333332871, 0.09722222222222222376, 0.1111111111111111049, 0.1250000000000000000, 0.1388888888888888951, 0.1527777777777777901, 0.1666666666666666574, 0.1805555555555555525, 0.1944444444444444475, 0.2083333333333333426, 0.2222222222222222099, 0.2361111111111111049, 0.2500000000000000000, 0.2638888888888888951, 0.2777777777777777901, 0.2916666666666666852, 0.3055555555555555802, 0.3194444444444444198, 0.3333333333333333148, 0.3472222222222222099, 0.3611111111111111049, 0.3750000000000000000, 0.3888888888888888951, 0.4027777777777777901, 0.4166666666666666852, 0.4305555555555555802, 0.4444444444444444198, 0.4583333333333333148, 0.4722222222222222099, 0.4861111111111111049, 0.5000000000000000000, 0.5138888888888888395, 0.5277777777777777901, 0.5416666666666666297, 0.5555555555555555802, 0.5694444444444444198, 0.5833333333333333703, 0.5972222222222222099, 0.6111111111111111605, 0.6250000000000000000, 0.6388888888888888395, 0.6527777777777777901, 0.6666666666666666297, 0.6805555555555555802, 0.6944444444444444198, 0.7083333333333333703, 0.7222222222222222099, 0.7361111111111111605, 0.7500000000000000000, 0.7638888888888888395, 0.7777777777777777901, 0.7916666666666666297, 0.8055555555555555802, 0.8194444444444444198, 0.8333333333333333703, 0.8472222222222222099, 0.8611111111111111605, 0.8750000000000000000, 0.8888888888888888395, 0.9027777777777777901, 0.9166666666666666297, 0.9305555555555555802, 0.9444444444444444198, 0.9523586263115634276 ),
 .UNSPECIFIED. ) 
 GEOMETRIC_REPRESENTATION_ITEM ( )  RATIONAL_B_SPLINE_SURFACE ( (
 ( 1.000000000000000000, 0.8660254037844387076, 1.000000000000000000, 0.8660254037844387076, 1.000000000000000000, 0.8660254037844387076, 1.000000000000000000, 0.8660254037844387076, 1.000000000000000000, 0.8660254037844387076, 1.000000000000000000, 0.8660254037844387076, 1.000000000000000000, 0.8660254037844387076, 1.000000000000000000, 0.8660254037844387076, 1.000000000000000000, 0.8660254037844387076, 1.000000000000000000, 0.8660254037844387076, 1.000000000000000000, 0.8660254037844387076, 1.000000000000000000, 0.8660254037844387076, 1.000000000000000000, 0.8660254037844387076, 1.000000000000000000, 0.8660254037844387076, 1.000000000000000000, 0.8660254037844387076, 1.000000000000000000, 0.8660254037844387076, 1.000000000000000000, 0.8660254037844387076, 1.000000000000000000, 0.8660254037844387076, 1.000000000000000000, 0.8660254037844387076, 1.000000000000000000, 0.8660254037844387076, 1.000000000000000000, 0.8660254037844387076, 1.000000000000000000, 0.8660254037844387076, 1.000000000000000000, 0.8660254037844387076, 1.000000000000000000, 0.8660254037844387076, 1.000000000000000000, 0.8660254037844387076, 1.000000000000000000, 0.8660254037844387076, 1.000000000000000000, 0.8660254037844387076, 1.000000000000000000, 0.8660254037844387076, 1.000000000000000000, 0.8660254037844387076, 1.000000000000000000, 0.8660254037844387076, 1.000000000000000000, 0.8660254037844387076, 1.000000000000000000, 0.8660254037844387076, 1.000000000000000000, 0.8660254037844387076, 1.000000000000000000, 0.8660254037844387076, 1.000000000000000000, 0.8660254037844387076, 1.000000000000000000, 0.8660254037844387076, 1.000000000000000000, 0.8660254037844387076, 1.000000000000000000, 0.8660254037844387076, 1.000000000000000000, 0.8660254037844387076, 1.000000000000000000, 0.8660254037844387076, 1.000000000000000000, 0.8660254037844387076, 1.000000000000000000, 0.8660254037844387076, 1.000000000000000000, 0.8660254037844387076, 1.000000000000000000, 0.8660254037844387076, 1.000000000000000000, 0.8660254037844387076, 1.000000000000000000, 0.8660254037844387076, 1.000000000000000000, 0.8660254037844387076, 1.000000000000000000, 0.8660254037844387076, 1.000000000000000000, 0.8660254037844387076, 1.000000000000000000, 0.8660254037844387076, 1.000000000000000000, 0.8660254037844387076, 1.000000000000000000, 0.8660254037844387076, 1.000000000000000000, 0.8660254037844387076, 1.000000000000000000, 0.8660254037844387076, 1.000000000000000000, 0.8660254037844387076, 1.000000000000000000, 0.8660254037844387076, 1.000000000000000000, 0.8660254037844387076, 1.000000000000000000, 0.8660254037844387076, 1.000000000000000000, 0.8660254037844387076, 1.000000000000000000, 0.8660254037844387076, 1.000000000000000000, 0.8660254037844387076, 1.000000000000000000, 0.8660254037844387076, 1.000000000000000000, 0.8660254037844387076, 1.000000000000000000, 0.8660254037844387076, 1.000000000000000000, 0.8660254037844387076, 1.000000000000000000, 0.8660254037844387076, 1.000000000000000000, 0.8660254037844387076, 1.000000000000000000, 0.8660254037844387076, 1.000000000000000000, 0.9236584489582877477, 0.9343189502471116459),
 ( 1.000000000000000000, 0.8660254037844387076, 1.000000000000000000, 0.8660254037844387076, 1.000000000000000000, 0.8660254037844387076, 1.000000000000000000, 0.8660254037844387076, 1.000000000000000000, 0.8660254037844387076, 1.000000000000000000, 0.8660254037844387076, 1.000000000000000000, 0.8660254037844387076, 1.000000000000000000, 0.8660254037844387076, 1.000000000000000000, 0.8660254037844387076, 1.000000000000000000, 0.8660254037844387076, 1.000000000000000000, 0.8660254037844387076, 1.000000000000000000, 0.8660254037844387076, 1.000000000000000000, 0.8660254037844387076, 1.000000000000000000, 0.8660254037844387076, 1.000000000000000000, 0.8660254037844387076, 1.000000000000000000, 0.8660254037844387076, 1.000000000000000000, 0.8660254037844387076, 1.000000000000000000, 0.8660254037844387076, 1.000000000000000000, 0.8660254037844387076, 1.000000000000000000, 0.8660254037844387076, 1.000000000000000000, 0.8660254037844387076, 1.000000000000000000, 0.8660254037844387076, 1.000000000000000000, 0.8660254037844387076, 1.000000000000000000, 0.8660254037844387076, 1.000000000000000000, 0.8660254037844387076, 1.000000000000000000, 0.8660254037844387076, 1.000000000000000000, 0.8660254037844387076, 1.000000000000000000, 0.8660254037844387076, 1.000000000000000000, 0.8660254037844387076, 1.000000000000000000, 0.8660254037844387076, 1.000000000000000000, 0.8660254037844387076, 1.000000000000000000, 0.8660254037844387076, 1.000000000000000000, 0.8660254037844387076, 1.000000000000000000, 0.8660254037844387076, 1.000000000000000000, 0.8660254037844387076, 1.000000000000000000, 0.8660254037844387076, 1.000000000000000000, 0.8660254037844387076, 1.000000000000000000, 0.8660254037844387076, 1.000000000000000000, 0.8660254037844387076, 1.000000000000000000, 0.8660254037844387076, 1.000000000000000000, 0.8660254037844387076, 1.000000000000000000, 0.8660254037844387076, 1.000000000000000000, 0.8660254037844387076, 1.000000000000000000, 0.8660254037844387076, 1.000000000000000000, 0.8660254037844387076, 1.000000000000000000, 0.8660254037844387076, 1.000000000000000000, 0.8660254037844387076, 1.000000000000000000, 0.8660254037844387076, 1.000000000000000000, 0.8660254037844387076, 1.000000000000000000, 0.8660254037844387076, 1.000000000000000000, 0.8660254037844387076, 1.000000000000000000, 0.8660254037844387076, 1.000000000000000000, 0.8660254037844387076, 1.000000000000000000, 0.8660254037844387076, 1.000000000000000000, 0.8660254037844387076, 1.000000000000000000, 0.8660254037844387076, 1.000000000000000000, 0.8660254037844387076, 1.000000000000000000, 0.8660254037844387076, 1.000000000000000000, 0.8660254037844387076, 1.000000000000000000, 0.8660254037844387076, 1.000000000000000000, 0.8660254037844387076, 1.000000000000000000, 0.8660254037844387076, 1.000000000000000000, 0.8660254037844387076, 1.000000000000000000, 0.8660254037844387076, 1.000000000000000000, 0.8660254037844387076, 1.000000000000000000, 0.8660254037844387076, 1.000000000000000000, 0.8660254037844387076, 1.000000000000000000, 0.8660254037844387076, 1.000000000000000000, 0.9236584489582877477, 0.9343189502471116459) ) ) 
 REPRESENTATION_ITEM ( '' )  SURFACE ( )  );
#58739=DIRECTION ( 'NONE',  ( -0.000000000000000000, 1.000000000000000000, -0.000000000000000000 ) ) ;
#58744=DIRECTION ( 'NONE',  ( 0.000000000000000000, -1.000000000000000000, 0.000000000000000000 ) ) ;
#58747=DIRECTION ( 'NONE',  ( 0.000000000000000000, 0.000000000000000000, -1.000000000000000000 ) ) ;
#58753=CARTESIAN_POINT ( 'NONE',  ( 3.285556943750000514, -1.801041666188707424, 1.896917185911906500 ) ) ;
#58766=CARTESIAN_POINT ( 'NONE',  ( 1.173530994449854870, -3.042800438942089514, 3.270848514539542506 ) ) ;
#58788=ADVANCED_FACE ( 'NONE', ( #91952 ), #204581, .F. ) ;
#58841=CARTESIAN_POINT ( 'NONE',  ( 1.001543065824772753E-15, -0.6125000000000012657, 4.012584370867899430 ) ) ;
#58871=ORIENTED_EDGE ( 'NONE', *, *, #83547, .F. ) ;
#58878=CARTESIAN_POINT ( 'NONE',  ( -1.967994056399313907, -3.170678274948564468, 2.724402440660230962 ) ) ;
#58931=CARTESIAN_POINT ( 'NONE',  ( -1.737500000000000266, -1.808333333333332016, -3.009438278150923907 ) ) ;
#58935=EDGE_CURVE ( 'NONE', #136464, #59550, #7448, .T. ) ;
#59004=CARTESIAN_POINT ( 'NONE',  ( 3.475000000000000533, -0.4520833323774166024, -2.006292185433951047 ) ) ;
#59015=CYLINDRICAL_SURFACE ( 'NONE', #116184, 2.500000000000000888 ) ;
#59090=CARTESIAN_POINT ( 'NONE',  ( -1.642778471874998480, -0.7510416661887092671, 2.845375778867863303 ) ) ;
#59131=CARTESIAN_POINT ( 'NONE',  ( 0.000000000000000000, 2.999999999999999112, 0.000000000000000000 ) ) ;
#59168=CARTESIAN_POINT ( 'NONE',  ( 1.001543065824772753E-15, -2.909374999522043925, 3.793834371823810780 ) ) ;
#59229=CARTESIAN_POINT ( 'NONE',  ( -1.642778471874998480, -2.851041666188706802, 2.845375778867863303 ) ) ;
#59296=CARTESIAN_POINT ( 'NONE',  ( 0.000000000000000000, -3.084374999522042859, -3.793834371823813001 ) ) ;
#59367=( BOUNDED_CURVE ( )  B_SPLINE_CURVE ( 2, ( #145401, #211401, #63030, #129197, #25190, #157352, #8941, #207142, #58766 ),
 .UNSPECIFIED., .F., .T. ) 
 B_SPLINE_CURVE_WITH_KNOTS ( ( 3, 2, 2, 2, 3 ),
 ( 0.6875000000000000000, 0.6944444444444444198, 0.7083333333333333703, 0.7222222222222222099, 0.7246580528728726600 ),
 .UNSPECIFIED. ) 
 CURVE ( )  GEOMETRIC_REPRESENTATION_ITEM ( )  RATIONAL_B_SPLINE_CURVE ( ( 0.9330127018922194093, 0.9330127018922194093, 1.000000000000000000, 0.8660254037844387076, 1.000000000000000000, 0.8660254037844387076, 1.000000000000000000, 0.9765035611933325921, 0.9612487241856686460 ) ) 
 REPRESENTATION_ITEM ( '' )  );
#59413=AXIS2_PLACEMENT_3D ( 'NONE', #96492, #15184, #81274 ) ;
#59448=FACE_OUTER_BOUND ( 'NONE', #127417, .T. ) ;
#59484=CARTESIAN_POINT ( 'NONE',  ( 1.737500000000001155, -0.5833333333333314830, 3.009438278150922130 ) ) ;
#59550=VERTEX_POINT ( 'NONE', #38387 ) ;
#59573=AXIS2_PLACEMENT_3D ( 'NONE', #8995, #141183, #128182 ) ;
#59598=EDGE_CURVE ( 'NONE', #144530, #12134, #31763, .T. ) ;
#59702=DIRECTION ( 'NONE',  ( 0.000000000000000000, 0.000000000000000000, 1.000000000000000000 ) ) ;
#59704=EDGE_CURVE ( 'NONE', #197566, #192999, #172671, .T. ) ;
#59714=EDGE_CURVE ( 'NONE', #1142, #55184, #24248, .T. ) ;
#59725=AXIS2_PLACEMENT_3D ( 'NONE', #23277, #184712, #87235 ) ;
#59749=ORIENTED_EDGE ( 'NONE', *, *, #88437, .T. ) ;
#59757=CARTESIAN_POINT ( 'NONE',  ( 2.520460663003311730, -4.179124451297094645, -2.338645729556988240 ) ) ;
#59791=TOROIDAL_SURFACE ( 'NONE', #166955, 3.599999999999999201, 0.4999999999999998890 ) ;
#59817=CARTESIAN_POINT ( 'NONE',  ( 1.642778471875001811, -1.480208332855375453, 2.845375778867859751 ) ) ;
#59905=CARTESIAN_POINT ( 'NONE',  ( 1.737500000000001155, -1.633333333333333748, 3.009438278150922130 ) ) ;
#59927=ORIENTED_EDGE ( 'NONE', *, *, #35402, .T. ) ;
#59955=ORIENTED_EDGE ( 'NONE', *, *, #122422, .F. ) ;
#59997=CARTESIAN_POINT ( 'NONE',  ( 0.000000000000000000, -2.537500000000000977, -4.012584370867899430 ) ) ;
#60069=CARTESIAN_POINT ( 'NONE',  ( 3.475000000000000533, -0.5104166657107496174, 2.006292185433948827 ) ) ;
#60185=VERTEX_POINT ( 'NONE', #13979 ) ;
#60196=FACE_OUTER_BOUND ( 'NONE', #124500, .T. ) ;
#60216=VECTOR ( 'NONE', #24001, 1000.000000000000000 ) ;
#60299=CARTESIAN_POINT ( 'NONE',  ( 1.642778471875000035, -3.026041666188708401, -2.845375778867859751 ) ) ;
#60337=EDGE_CURVE ( 'NONE', #170914, #24109, #36642, .T. ) ;
#60351=LINE ( 'NONE', #161067, #42753 ) ;
#60360=CARTESIAN_POINT ( 'NONE',  ( 0.000000000000000000, -1.946874999522044014, -3.793834371823813001 ) ) ;
#60371=LINE ( 'NONE', #48418, #72290 ) ;
#60409=CARTESIAN_POINT ( 'NONE',  ( -3.475000000000000533, -1.735416665710752149, -2.006292185433948827 ) ) ;
#60499=CYLINDRICAL_SURFACE ( 'NONE', #5106, 4.500000000000000000 ) ;
#60507=CARTESIAN_POINT ( 'NONE',  ( -1.642778471875000035, -2.617708332855375186, -2.845375778867859751 ) ) ;
#60524=CARTESIAN_POINT ( 'NONE',  ( -1.249999999999966471, 8.500000000000000000, 9.921567416492214520 ) ) ;
#60537=( BOUNDED_CURVE ( )  B_SPLINE_CURVE ( 2, ( #152756, #155967, #170063, #36860, #4339, #203610, #56330, #37945, #153833 ),
 .UNSPECIFIED., .F., .T. ) 
 B_SPLINE_CURVE_WITH_KNOTS ( ( 3, 2, 2, 2, 3 ),
 ( 0.5625000000000000000, 0.5694444444444444198, 0.5833333333333333703, 0.5972222222222222099, 0.6041666666666667407 ),
 .UNSPECIFIED. ) 
 CURVE ( )  GEOMETRIC_REPRESENTATION_ITEM ( )  RATIONAL_B_SPLINE_CURVE ( ( 0.9330127018922194093, 0.9330127018922194093, 1.000000000000000000, 0.8660254037844387076, 1.000000000000000000, 0.8660254037844387076, 1.000000000000000000, 0.9330127018922187432, 0.9330127018922192983 ) ) 
 REPRESENTATION_ITEM ( '' )  );
#60548=CARTESIAN_POINT ( 'NONE',  ( -3.475000000000000533, -1.049999999999998934, 0.000000000000000000 ) ) ;
#60579=ORIENTED_EDGE ( 'NONE', *, *, #35402, .F. ) ;
#60637=ORIENTED_EDGE ( 'NONE', *, *, #144738, .F. ) ;
#60753=CARTESIAN_POINT ( 'NONE',  ( -1.500000000000039524, 7.750000000000000000, -10.86128356754322688 ) ) ;
#60867=CARTESIAN_POINT ( 'NONE',  ( 0.000000000000000000, -3.499999999999999556, 0.000000000000000000 ) ) ;
#60869=ORIENTED_EDGE ( 'NONE', *, *, #192668, .T. ) ;
#60882=CARTESIAN_POINT ( 'NONE',  ( 1.642778471875001811, -3.230208332855373676, 2.845375778867859751 ) ) ;
#60940=CARTESIAN_POINT ( 'NONE',  ( -6.042630808230841359E-15, -1.662500000000000533, 3.474999999999999645 ) ) ;
#60978=CARTESIAN_POINT ( 'NONE',  ( -1.737499999999997824, -1.691666666666667762, 3.009438278150925683 ) ) ;
#61049=CARTESIAN_POINT ( 'NONE',  ( -3.285556943750000070, -2.909374999522040817, 0.000000000000000000 ) ) ;
#61068=CARTESIAN_POINT ( 'NONE',  ( -3.474999999999998312, -2.070833333333331971, 2.006292185433951047 ) ) ;
#61083=B_SPLINE_CURVE_WITH_KNOTS ( 'NONE', 3,
 ( #121520, #7661, #55366, #38055 ),
 .UNSPECIFIED., .F., .F.,
 ( 4, 4 ),
 ( 0.003648968938405892752, 0.004840739682861143652 ),
 .UNSPECIFIED. ) ;
#61138=CARTESIAN_POINT ( 'NONE',  ( 3.475000000000000533, -1.502083332377415870, -2.006292185433951047 ) ) ;
#61149=ORIENTED_EDGE ( 'NONE', *, *, #159826, .F. ) ;
#61261=ORIENTED_EDGE ( 'NONE', *, *, #172591, .T. ) ;
#61308=CARTESIAN_POINT ( 'NONE',  ( -6.042630808230841359E-15, -2.318749999044084298, 3.474999999999999645 ) ) ;
#61312=CARTESIAN_POINT ( 'NONE',  ( -3.285556943749998737, -2.967708332855377051, 1.896917185911908721 ) ) ;
#61378=CARTESIAN_POINT ( 'NONE',  ( -3.285556943750000070, -2.909374999522040817, 0.000000000000000000 ) ) ;
#61408=ORIENTED_EDGE ( 'NONE', *, *, #207484, .F. ) ;
#61433=CARTESIAN_POINT ( 'NONE',  ( -3.285556943750000514, -1.188541666188710044, -1.896917185911906500 ) ) ;
#61457=AXIS2_PLACEMENT_3D ( 'NONE', #133843, #70903, #118682 ) ;
#61468=AXIS2_PLACEMENT_3D ( 'NONE', #66839, #50630, #7196 ) ;
#61581=CARTESIAN_POINT ( 'NONE',  ( 3.285556943749998737, -1.305208332855376296, -1.896917185911906500 ) ) ;
#61596=AXIS2_PLACEMENT_3D ( 'NONE', #205964, #42436, #22928 ) ;
#61619=CARTESIAN_POINT ( 'NONE',  ( 3.475000000000000533, -2.245833333333331350, -2.006292185433951047 ) ) ;
#61686=FACE_OUTER_BOUND ( 'NONE', #185159, .T. ) ;
#61708=CARTESIAN_POINT ( 'NONE',  ( 1.250000000000037526, 8.500000000000000000, 10.85702537530423406 ) ) ;
#61810=CARTESIAN_POINT ( 'NONE',  ( 0.000000000000000000, 0.5000000000000004441, 0.000000000000000000 ) ) ;
#61812=ORIENTED_EDGE ( 'NONE', *, *, #41018, .T. ) ;
#61875=DIRECTION ( 'NONE',  ( -0.6483454320283799088, 0.000000000000000000, 0.7613463080411786432 ) ) ;
#61956=CARTESIAN_POINT ( 'NONE',  ( -3.285556943749998737, -3.667708332855377673, 1.896917185911908499 ) ) ;
#62056=CARTESIAN_POINT ( 'NONE',  ( 3.475000000000000533, -0.8458333333333335480, -2.006292185433951047 ) ) ;
#62082=ORIENTED_EDGE ( 'NONE', *, *, #41738, .F. ) ;
#62091=ORIENTED_EDGE ( 'NONE', *, *, #13231, .T. ) ;
#62141=CARTESIAN_POINT ( 'NONE',  ( 3.475000000000000533, -1.954166666666666163, 2.006292185433948827 ) ) ;
#62214=CARTESIAN_POINT ( 'NONE',  ( 1.001543065824772753E-15, -1.618749999044086119, 4.012584370867899430 ) ) ;
#62225=DIRECTION ( 'NONE',  ( 0.000000000000000000, -1.000000000000000000, -0.000000000000000000 ) ) ;
#62337=DIRECTION ( 'NONE',  ( 0.000000000000000000, 0.000000000000000000, 1.000000000000000000 ) ) ;
#62373=CARTESIAN_POINT ( 'NONE',  ( -1.642778471874998480, -2.588541666188707957, 2.845375778867863303 ) ) ;
#62389=ORIENTED_EDGE ( 'NONE', *, *, #88437, .F. ) ;
#62399=ADVANCED_FACE ( 'NONE', ( #138135 ), #54733, .F. ) ;
#62496=CARTESIAN_POINT ( 'NONE',  ( 3.285556943750000070, -0.9843749995220412163, 0.000000000000000000 ) ) ;
#62572=ADVANCED_FACE ( 'NONE', ( #127300 ), #58708, .T. ) ;
#62633=CARTESIAN_POINT ( 'NONE',  ( 1.642778471875000035, -1.276041666188710400, -2.845375778867859751 ) ) ;
#62672=CARTESIAN_POINT ( 'NONE',  ( 3.475000000000000533, -1.545833333333334503, -2.006292185433951047 ) ) ;
#62797=CARTESIAN_POINT ( 'NONE',  ( -2.880977623208980098, -0.8887487162373146621, -1.594386611912667284 ) ) ;
#62883=FACE_OUTER_BOUND ( 'NONE', #6336, .T. ) ;
#62885=DIRECTION ( 'NONE',  ( -0.000000000000000000, 1.000000000000000000, -0.000000000000000000 ) ) ;
#62940=CARTESIAN_POINT ( 'NONE',  ( 3.285556943749998737, -0.2552083328553768071, -1.896917185911906500 ) ) ;
#63006=DIRECTION ( 'NONE',  ( 0.3162277660168376636, 0.9486832980505138790, 0.000000000000000000 ) ) ;
#63030=CARTESIAN_POINT ( 'NONE',  ( 1.737499999999999378, -2.916666666666668295, -3.009438278150925683 ) ) ;
#63041=VERTEX_POINT ( 'NONE', #183161 ) ;
#63113=CARTESIAN_POINT ( 'NONE',  ( 0.000000000000000000, -1.837499999999999911, -4.012584370867899430 ) ) ;
#63138=VECTOR ( 'NONE', #90265, 1000.000000000000000 ) ;
#63182=CARTESIAN_POINT ( 'NONE',  ( -3.285556943750000514, -2.938541666188710266, -1.896917185911906722 ) ) ;
#63199=CARTESIAN_POINT ( 'NONE',  ( -1.737500000000000266, -3.208333333333333925, -3.009438278150923907 ) ) ;
#63273=CARTESIAN_POINT ( 'NONE',  ( 0.000000000000000000, -2.493749999044085897, -4.012584370867899430 ) ) ;
#63364=CARTESIAN_POINT ( 'NONE',  ( 1.642778471875001811, -0.3427083328553758301, 2.845375778867859751 ) ) ;
#63396=ORIENTED_EDGE ( 'NONE', *, *, #120662, .F. ) ;
#63408=ORIENTED_EDGE ( 'NONE', *, *, #150659, .F. ) ;
#63506=DIRECTION ( 'NONE',  ( 0.000000000000000000, 0.000000000000000000, 1.000000000000000000 ) ) ;
#63557=CARTESIAN_POINT ( 'NONE',  ( -0.9311234436981447038, -2.828119629485603248, -3.475000000000004086 ) ) ;
#63568=CARTESIAN_POINT ( 'NONE',  ( 1.001543065824772753E-15, -2.121874999522043836, 3.793834371823811669 ) ) ;
#63641=ORIENTED_EDGE ( 'NONE', *, *, #118518, .F. ) ;
#63650=CIRCLE ( 'NONE', #198460, 11.00000000000000000 ) ;
#63669=ORIENTED_EDGE ( 'NONE', *, *, #3140, .F. ) ;
#63710=CARTESIAN_POINT ( 'NONE',  ( 1.642778471875001811, -2.092708332855373943, 2.845375778867859751 ) ) ;
#63747=CARTESIAN_POINT ( 'NONE',  ( -1.737500000000000266, -1.808333333333332016, -3.009438278150923907 ) ) ;
#63749=CARTESIAN_POINT ( 'NONE',  ( -3.285556943750000514, -3.376041666188708490, -1.896917185911906500 ) ) ;
#63753=SHAPE_REPRESENTATION_RELATIONSHIP ( 'NONE' , 'NONE' ,  #203468, #37156 ) ;
#63872=CARTESIAN_POINT ( 'NONE',  ( -3.273028085023368394, -0.8887487162373572946, -0.3592362057191292868 ) ) ;
#63954=CARTESIAN_POINT ( 'NONE',  ( -1.333315192109771230, 8.250054423670807324, -10.85938449304424402 ) ) ;
#64014=CARTESIAN_POINT ( 'NONE',  ( -3.285556943750000514, -0.4885416661887091450, -1.896917185911906500 ) ) ;
#64021=EDGE_CURVE ( 'NONE', #118628, #126440, #53012, .T. ) ;
#64023=PLANE ( 'NONE',  #196871 ) ;
#64103=CARTESIAN_POINT ( 'NONE',  ( 1.737500000000001155, -1.239583332377419689, 3.009438278150922130 ) ) ;
#64147=CARTESIAN_POINT ( 'NONE',  ( -2.324088772396477673E-16, -1.837499999999999245, -3.475000000000000089 ) ) ;
#64158=CARTESIAN_POINT ( 'NONE',  ( 1.850927770832884622, -3.228592521950734096, 2.725326427519580541 ) ) ;
#64187=CARTESIAN_POINT ( 'NONE',  ( -1.737500000000000266, -3.908333333333333215, -3.009438278150923907 ) ) ;
#64234=ORIENTED_EDGE ( 'NONE', *, *, #202630, .F. ) ;
#64236=ORIENTED_EDGE ( 'NONE', *, *, #12527, .F. ) ;
#64273=CARTESIAN_POINT ( 'NONE',  ( 3.475000000000000533, -2.974999999999998312, 0.000000000000000000 ) ) ;
#64298=AXIS2_PLACEMENT_3D ( 'NONE', #123365, #156852, #204485 ) ;
#64346=CARTESIAN_POINT ( 'NONE',  ( -3.475000000000000533, -3.485416665710752593, -2.006292185433948827 ) ) ;
#64430=CARTESIAN_POINT ( 'NONE',  ( -1.642778471874998480, -1.451041666188708446, 2.845375778867863303 ) ) ;
#64563=AXIS2_PLACEMENT_3D ( 'NONE', #9157, #42760, #156493 ) ;
#64633=CARTESIAN_POINT ( 'NONE',  ( 3.285556943750000070, -2.384374999522043126, 0.000000000000000000 ) ) ;
#64757=DIRECTION ( 'NONE',  ( 0.000000000000000000, 1.000000000000000000, 0.000000000000000000 ) ) ;
#64760=DIRECTION ( 'NONE',  ( 0.6483454320283789096, 0.000000000000000000, -0.7613463080411795314 ) ) ;
#64772=CARTESIAN_POINT ( 'NONE',  ( -1.642778471875000035, -2.967708332855374831, -2.845375778867859751 ) ) ;
#64809=CARTESIAN_POINT ( 'NONE',  ( -3.474999999999998312, -3.120833333333331350, 2.006292185433951047 ) ) ;
#64811=CARTESIAN_POINT ( 'NONE',  ( 3.285556943750000514, -2.851041666188706802, 1.896917185911906500 ) ) ;
#64849=DIRECTION ( 'NONE',  ( -0.6483454320283800199, 0.000000000000000000, 0.7613463080411787542 ) ) ;
#64876=CARTESIAN_POINT ( 'NONE',  ( -1.642778471874998480, -0.4885416661887104217, 2.845375778867863303 ) ) ;
#64877=CARTESIAN_POINT ( 'NONE',  ( -1.787771076284315308, -3.046595646931173906, 3.001059505585823572 ) ) ;
#64952=FACE_OUTER_BOUND ( 'NONE', #18600, .T. ) ;
#64986=DIRECTION ( 'NONE',  ( 1.000000000000000000, 0.000000000000000000, -3.491481338843133355E-15 ) ) ;
#64997=VERTEX_POINT ( 'NONE', #133316 ) ;
#65001=CARTESIAN_POINT ( 'NONE',  ( -1.500000000000039524, 8.500000000000000000, -10.89724735885167739 ) ) ;
#65034=DIRECTION ( 'NONE',  ( -0.7613463080411786432, 0.000000000000000000, -0.6483454320283800199 ) ) ;
#65049=EDGE_CURVE ( 'NONE', #36461, #145929, #86657, .T. ) ;
#65056=CARTESIAN_POINT ( 'NONE',  ( 1.642778471875000035, -0.5760416661887077794, -2.845375778867859751 ) ) ;
#65086=ORIENTED_EDGE ( 'NONE', *, *, #82056, .T. ) ;
#65125=CARTESIAN_POINT ( 'NONE',  ( -3.285556943750000514, -4.076041666188709556, -1.896917185911906500 ) ) ;
#65174=CARTESIAN_POINT ( 'NONE',  ( 7.204675194429079505E-15, -1.487500000000000044, -3.475000000000000089 ) ) ;
#65189=CARTESIAN_POINT ( 'NONE',  ( 0.7335685072721549460, -3.146544515318441704, -3.295627537534667972 ) ) ;
#65206=DIRECTION ( 'NONE',  ( -1.000000000000000000, 0.000000000000000000, 3.491481338843133355E-15 ) ) ;
#65209=VERTEX_POINT ( 'NONE', #152724 ) ;
#65217=CARTESIAN_POINT ( 'NONE',  ( -3.475000000000000533, -2.800000000000000266, 0.000000000000000000 ) ) ;
#65304=CARTESIAN_POINT ( 'NONE',  ( 0.000000000000000000, -3.937499999999998224, -4.012584370867899430 ) ) ;
#65340=CARTESIAN_POINT ( 'NONE',  ( -3.197123283245616676, -0.9841229182759280159, 1.361626862150112860 ) ) ;
#65375=CARTESIAN_POINT ( 'NONE',  ( 1.737500000000001155, -2.989583332377417690, 3.009438278150922130 ) ) ;
#65421=ORIENTED_EDGE ( 'NONE', *, *, #71349, .T. ) ;
#65430=CARTESIAN_POINT ( 'NONE',  ( 1.464175926609780964E-14, -2.537500000000001865, -3.475000000000000533 ) ) ;
#65461=CARTESIAN_POINT ( 'NONE',  ( -3.285556943750000070, -1.509374999522042238, 0.000000000000000000 ) ) ;
#65663=CARTESIAN_POINT ( 'NONE',  ( -1.642778471875000035, -2.967708332855374831, -2.845375778867859751 ) ) ;
#65679=DIRECTION ( 'NONE',  ( 0.000000000000000000, -1.000000000000000000, -0.000000000000000000 ) ) ;
#65700=CARTESIAN_POINT ( 'NONE',  ( -3.197123283245616676, -0.9841229182759280159, 1.361626862150112860 ) ) ;
#65803=CARTESIAN_POINT ( 'NONE',  ( -1.249999999999963807, 8.500000000000000000, 10.85702537530424827 ) ) ;
#65805=CARTESIAN_POINT ( 'NONE',  ( -3.285556943749998737, -3.580208332855374653, 1.896917185911908499 ) ) ;
#65820=CARTESIAN_POINT ( 'NONE',  ( -1.620863580070950327, 0.4000000000000010214, 1.903365770102947385 ) ) ;
#65847=CARTESIAN_POINT ( 'NONE',  ( 3.130865642711470276, -4.000192543527539613, -1.507748429708645199 ) ) ;
#65849=CARTESIAN_POINT ( 'NONE',  ( 0.000000000000000000, -3.084374999522042859, -3.793834371823813001 ) ) ;
#65866=ADVANCED_FACE ( 'NONE', ( #117633 ), #575, .T. ) ;
#65884=UNCERTAINTY_MEASURE_WITH_UNIT (LENGTH_MEASURE( 1.000000000000000082E-05 ), #128836, 'distance_accuracy_value', 'NONE');
#65915=CARTESIAN_POINT ( 'NONE',  ( -3.285556943750000070, -0.5468749995220407722, 0.000000000000000000 ) ) ;
#65917=DIRECTION ( 'NONE',  ( 0.000000000000000000, -1.000000000000000000, 0.000000000000000000 ) ) ;
#66058=CARTESIAN_POINT ( 'NONE',  ( 3.475000000000000533, -2.595833333333334103, -2.006292185433951047 ) ) ;
#66105=CARTESIAN_POINT ( 'NONE',  ( 3.285556943749998737, -2.355208332855375453, -1.896917185911906500 ) ) ;
#66170=CARTESIAN_POINT ( 'NONE',  ( 0.000000000000000000, 12.31951671548121219, 0.000000000000000000 ) ) ;
#66188=CARTESIAN_POINT ( 'NONE',  ( 1.737499999999999378, -1.122916665710751882, -3.009438278150925683 ) ) ;
#66241=CARTESIAN_POINT ( 'NONE',  ( 2.953507107040155066, -3.210470589277563569, 1.499658823967387145 ) ) ;
#66258=DIRECTION ( 'NONE',  ( 0.000000000000000000, 0.000000000000000000, -1.000000000000000000 ) ) ;
#66270=CARTESIAN_POINT ( 'NONE',  ( -3.475000000000000533, -3.849999999999999201, 0.000000000000000000 ) ) ;
#66297=EDGE_LOOP ( 'NONE', ( #49320, #209911, #21703, #110114 ) ) ;
#66373=CARTESIAN_POINT ( 'NONE',  ( -1.642778471875000035, -0.6052083328553746755, -2.845375778867859751 ) ) ;
#66428=ORIENTED_EDGE ( 'NONE', *, *, #32460, .T. ) ;
#66431=CARTESIAN_POINT ( 'NONE',  ( 3.475000000000000533, -3.660416665710751971, 2.006292185433948827 ) ) ;
#66517=CARTESIAN_POINT ( 'NONE',  ( -3.285556943750000514, -2.238541666188709200, -1.896917185911906500 ) ) ;
#66641=EDGE_CURVE ( 'NONE', #27240, #135098, #11272, .T. ) ;
#66694=EDGE_CURVE ( 'NONE', #54700, #153986, #56486, .T. ) ;
#66706=CARTESIAN_POINT ( 'NONE',  ( 1.464175926609780964E-14, -2.843749999044085541, -3.475000000000000533 ) ) ;
#66718=CARTESIAN_POINT ( 'NONE',  ( 1.001543065824772753E-15, -3.871874999522043836, 3.793834371823811669 ) ) ;
#66719=AXIS2_PLACEMENT_3D ( 'NONE', #185844, #166412, #183725 ) ;
#66779=EDGE_CURVE ( 'NONE', #174327, #88062, #73895, .T. ) ;
#66788=CIRCLE ( 'NONE', #94543, 10.25000000000000000 ) ;
#66839=CARTESIAN_POINT ( 'NONE',  ( 0.000000000000000000, -3.499999999999999556, 0.000000000000000000 ) ) ;
#66859=VECTOR ( 'NONE', #171721, 1000.000000000000000 ) ;
#66868=CARTESIAN_POINT ( 'NONE',  ( 1.737499999999999378, -0.1166666666666676955, -3.009438278150925683 ) ) ;
#66912=CARTESIAN_POINT ( 'NONE',  ( 1.737499999999999378, -3.266666666666667496, -3.009438278150925683 ) ) ;
#66914=CARTESIAN_POINT ( 'NONE',  ( -3.285556943749998737, -2.967708332855377051, 1.896917185911908499 ) ) ;
#66983=CARTESIAN_POINT ( 'NONE',  ( 0.000000000000000000, -2.384374999522042238, -3.793834371823813001 ) ) ;
#67020=CIRCLE ( 'NONE', #25603, 3.432849766368862632 ) ;
#67147=CARTESIAN_POINT ( 'NONE',  ( -3.360593407046564618, -0.9395304069187625506, 0.08390535222174622110 ) ) ;
#67175=CARTESIAN_POINT ( 'NONE',  ( -1.642778471874998480, -2.151041666188707957, 2.845375778867863303 ) ) ;
#67216=CARTESIAN_POINT ( 'NONE',  ( -3.475000000000000533, -2.085416665710750905, -2.006292185433948827 ) ) ;
#67226=EDGE_CURVE ( 'NONE', #146583, #73220, #152512, .T. ) ;
#67265=DIRECTION ( 'NONE',  ( 0.000000000000000000, 0.000000000000000000, -1.000000000000000000 ) ) ;
#67322=VECTOR ( 'NONE', #143162, 1000.000000000000000 ) ;
#67335=CARTESIAN_POINT ( 'NONE',  ( 3.475000000000000533, -3.675000000000001155, 0.000000000000000000 ) ) ;
#67427=CARTESIAN_POINT ( 'NONE',  ( 3.475000000000000533, -3.704166666666666163, 2.006292185433948827 ) ) ;
#67440=CARTESIAN_POINT ( 'NONE',  ( 3.285556943749998737, -0.3427083328553764408, -1.896917185911906500 ) ) ;
#67457=ORIENTED_EDGE ( 'NONE', *, *, #139381, .T. ) ;
#67462=CARTESIAN_POINT ( 'NONE',  ( 3.285556943749998737, -2.005208332855377140, -1.896917185911906722 ) ) ;
#67500=CARTESIAN_POINT ( 'NONE',  ( 1.001543065824772753E-15, -3.018749999044083587, 4.012584370867899430 ) ) ;
#67558=ORIENTED_EDGE ( 'NONE', *, *, #117585, .F. ) ;
#67586=CARTESIAN_POINT ( 'NONE',  ( 1.642778471875001811, -1.742708332855374298, 2.845375778867859751 ) ) ;
#67786=CARTESIAN_POINT ( 'NONE',  ( -3.285556943749998737, -3.580208332855374653, 1.896917185911908499 ) ) ;
#67861=ORIENTED_EDGE ( 'NONE', *, *, #59598, .F. ) ;
#67937=CARTESIAN_POINT ( 'NONE',  ( 3.475000000000000533, -0.5541666666666681396, 2.006292185433948827 ) ) ;
#67980=CARTESIAN_POINT ( 'NONE',  ( 1.001543065824772753E-15, -3.412500000000000977, 4.012584370867899430 ) ) ;
#67982=CARTESIAN_POINT ( 'NONE',  ( 1.642778471875001811, -1.042708332855375009, 2.845375778867859751 ) ) ;
#68047=CARTESIAN_POINT ( 'NONE',  ( -3.285556943750000070, -1.246874999522043392, 0.000000000000000000 ) ) ;
#68064=DIRECTION ( 'NONE',  ( 0.000000000000000000, 0.000000000000000000, -1.000000000000000000 ) ) ;
#68081=CIRCLE ( 'NONE', #102597, 0.5000000000000000000 ) ;
#68198=DIRECTION ( 'NONE',  ( 0.000000000000000000, -0.000000000000000000, 1.000000000000000000 ) ) ;
#68218=CARTESIAN_POINT ( 'NONE',  ( -3.299093274330711978, -0.9061123214685398164, 0.2492867766378724925 ) ) ;
#68222=DIRECTION ( 'NONE',  ( -0.6483454320283789096, 0.000000000000000000, 0.7613463080411795314 ) ) ;
#68245=CARTESIAN_POINT ( 'NONE',  ( -1.642778471874998480, -2.851041666188706802, 2.845375778867863303 ) ) ;
#68288=CARTESIAN_POINT ( 'NONE',  ( -3.474999999999997868, -2.027083332377417335, 2.006292185433951047 ) ) ;
#68365=ORIENTED_EDGE ( 'NONE', *, *, #109904, .F. ) ;
#68378=CARTESIAN_POINT ( 'NONE',  ( 1.249999999999961142, 8.500000000000000000, -10.85702537530424472 ) ) ;
#68403=CARTESIAN_POINT ( 'NONE',  ( -1.499999999999960476, 7.193113254731351880, 10.88798745763944176 ) ) ;
#68414=CARTESIAN_POINT ( 'NONE',  ( -3.474999999999998312, -2.420833333333334725, 2.006292185433951047 ) ) ;
#68518=LINE ( 'NONE', #33904, #36632 ) ;
#68539=CARTESIAN_POINT ( 'NONE',  ( 3.285556943750000070, -0.9843749995220412163, 0.000000000000000000 ) ) ;
#68573=CARTESIAN_POINT ( 'NONE',  ( -3.285556943749998737, -1.217708332855376607, 1.896917185911908499 ) ) ;
#68662=CARTESIAN_POINT ( 'NONE',  ( 1.642778471875000035, -1.276041666188710400, -2.845375778867859751 ) ) ;
#68834=AXIS2_PLACEMENT_3D ( 'NONE', #113915, #198260, #32583 ) ;
#68847=EDGE_CURVE ( 'NONE', #65209, #5754, #171525, .T. ) ;
#68865=CARTESIAN_POINT ( 'NONE',  ( 1.642778471875000035, -3.726041666188707691, -2.845375778867859751 ) ) ;
#68872=DIRECTION ( 'NONE',  ( -0.6483454320283800199, 0.000000000000000000, 0.7613463080411787542 ) ) ;
#68939=ORIENTED_EDGE ( 'NONE', *, *, #196923, .T. ) ;
#68946=CARTESIAN_POINT ( 'NONE',  ( 0.000000000000000000, 6.999999999999999112, 0.000000000000000000 ) ) ;
#68949=EDGE_CURVE ( 'NONE', #169163, #71477, #146637, .T. ) ;
#68979=ORIENTED_EDGE ( 'NONE', *, *, #25018, .T. ) ;
#68994=PLANE ( 'NONE',  #26266 ) ;
#69017=CARTESIAN_POINT ( 'NONE',  ( -3.475000000000000533, -0.3499999999999996447, 0.000000000000000000 ) ) ;
#69057=CARTESIAN_POINT ( 'NONE',  ( 0.000000000000000000, -3.237499999999997602, -4.012584370867899430 ) ) ;
#69059=CARTESIAN_POINT ( 'NONE',  ( 3.285556943749998737, -0.9552083328553737651, -1.896917185911906500 ) ) ;
#69116=CARTESIAN_POINT ( 'NONE',  ( 0.000000000000000000, 6.999999999999999112, 0.000000000000000000 ) ) ;
#69121=CARTESIAN_POINT ( 'NONE',  ( -3.285556943749998737, -1.217708332855376607, 1.896917185911908499 ) ) ;
#69195=EDGE_LOOP ( 'NONE', ( #33188, #13487, #140415, #126451 ) ) ;
#69246=ORIENTED_EDGE ( 'NONE', *, *, #208932, .F. ) ;
#69282=ORIENTED_EDGE ( 'NONE', *, *, #17805, .T. ) ;
#69309=CARTESIAN_POINT ( 'NONE',  ( -1.642778471874998480, -2.501041666188707158, 2.845375778867863303 ) ) ;
#69315=DIRECTION ( 'NONE',  ( -0.6483454320283799088, 0.000000000000000000, 0.7613463080411786432 ) ) ;
#69339=ORIENTED_EDGE ( 'NONE', *, *, #168924, .F. ) ;
#69404=EDGE_CURVE ( 'NONE', #170914, #40241, #90349, .T. ) ;
#69433=ORIENTED_EDGE ( 'NONE', *, *, #21052, .T. ) ;
#69586=EDGE_CURVE ( 'NONE', #187007, #88193, #46292, .T. ) ;
#69594=AXIS2_PLACEMENT_3D ( 'NONE', #197029, #114783, #115844 ) ;
#69606=CARTESIAN_POINT ( 'NONE',  ( 0.000000000000000000, -1.246874999522042948, -3.793834371823813445 ) ) ;
#69640=CARTESIAN_POINT ( 'NONE',  ( -3.285556943750000514, -0.2260416661887102996, -1.896917185911906500 ) ) ;
#69697=CIRCLE ( 'NONE', #42074, 3.475000000000000089 ) ;
#69704=CARTESIAN_POINT ( 'NONE',  ( -3.475000000000000533, -1.049999999999998934, 0.000000000000000000 ) ) ;
#69730=CARTESIAN_POINT ( 'NONE',  ( -3.285556943750000514, -3.988541666188710089, -1.896917185911906500 ) ) ;
#69791=DIRECTION ( 'NONE',  ( 0.000000000000000000, 0.000000000000000000, 1.000000000000000000 ) ) ;
#69805=VECTOR ( 'NONE', #158681, 1000.000000000000000 ) ;
#69849=B_SPLINE_CURVE_WITH_KNOTS ( 'NONE', 3,
 ( #136523, #120331, #186307, #109149, #37943, #92850, #104016 ),
 .UNSPECIFIED., .F., .F.,
 ( 4, 3, 4 ),
 ( 0.001837494195021906022, 0.002395020826491690066, 0.002588355962777570424 ),
 .UNSPECIFIED. ) ;
#69880=CARTESIAN_POINT ( 'NONE',  ( -3.285556943749999625, -0.1103036037021430799, -0.06039377925050889995 ) ) ;
#69927=CARTESIAN_POINT ( 'NONE',  ( -1.499999999999964029, 8.500000000000000000, 9.886859966642596476 ) ) ;
#69950=CARTESIAN_POINT ( 'NONE',  ( 1.737499999999999378, -1.472916665710751527, -3.009438278150925683 ) ) ;
#70082=CARTESIAN_POINT ( 'NONE',  ( 1.001543065824772753E-15, -0.2624999999999988454, 4.012584370867899430 ) ) ;
#70125=CARTESIAN_POINT ( 'NONE',  ( 1.001543065824772753E-15, -1.771874999522040861, 3.793834371823811669 ) ) ;
#70187=CARTESIAN_POINT ( 'NONE',  ( 1.642778471875000035, -2.413541666188709911, -2.845375778867859751 ) ) ;
#70374=CARTESIAN_POINT ( 'NONE',  ( 1.642778471875001811, -3.142708332855375986, 2.845375778867859751 ) ) ;
#70379=CARTESIAN_POINT ( 'NONE',  ( 1.394453263437886604E-15, -1.312499999999999556, 3.474999999999999645 ) ) ;
#70413=CARTESIAN_POINT ( 'NONE',  ( -0.9311234436981532525, -1.984380368602567835, 3.474999999999999201 ) ) ;
#70506=VECTOR ( 'NONE', #56718, 1000.000000000000000 ) ;
#70645=CARTESIAN_POINT ( 'NONE',  ( -3.285556943750000514, -0.2260416661887102996, -1.896917185911906500 ) ) ;
#70696=VERTEX_POINT ( 'NONE', #61708 ) ;
#70700=CARTESIAN_POINT ( 'NONE',  ( 0.000000000000000000, -1.334374999522042859, -3.793834371823813001 ) ) ;
#70760=CARTESIAN_POINT ( 'NONE',  ( 7.204675194429079505E-15, -1.137499999999999512, -3.475000000000000089 ) ) ;
#70791=CARTESIAN_POINT ( 'NONE',  ( 1.642778471875000035, -3.726041666188707691, -2.845375778867859751 ) ) ;
#70872=AXIS2_PLACEMENT_3D ( 'NONE', #100459, #214166, #64760 ) ;
#70903=DIRECTION ( 'NONE',  ( 0.000000000000000000, -1.000000000000000000, -0.000000000000000000 ) ) ;
#71003=EDGE_LOOP ( 'NONE', ( #112281, #122181, #83097, #35722 ) ) ;
#71060=CARTESIAN_POINT ( 'NONE',  ( 0.000000000000000000, 1.000000000000000888, 0.000000000000000000 ) ) ;
#71101=ORIENTED_EDGE ( 'NONE', *, *, #41850, .T. ) ;
#71127=CARTESIAN_POINT ( 'NONE',  ( 1.001543065824772753E-15, -1.159374999522043703, 3.793834371823810780 ) ) ;
#71193=CARTESIAN_POINT ( 'NONE',  ( -1.642778471874998480, -2.151041666188707957, 2.845375778867863303 ) ) ;
#71257=CARTESIAN_POINT ( 'NONE',  ( 3.285556943750000514, -2.851041666188706802, 1.896917185911906500 ) ) ;
#71338=CARTESIAN_POINT ( 'NONE',  ( 1.683015768249133348, -0.9661576380125261876, 2.984288236375972403 ) ) ;
#71349=EDGE_CURVE ( 'NONE', #24990, #82008, #125069, .T. ) ;
#71447=CARTESIAN_POINT ( 'NONE',  ( 0.000000000000000000, -0.4374999999999981126, -4.012584370867899430 ) ) ;
#71473=EDGE_CURVE ( 'NONE', #145305, #897, #114544, .T. ) ;
#71477=VERTEX_POINT ( 'NONE', #134200 ) ;
#71494=AXIS2_PLACEMENT_3D ( 'NONE', #5925, #200924, #21103 ) ;
#71536=VERTEX_POINT ( 'NONE', #117984 ) ;
#71602=ORIENTED_EDGE ( 'NONE', *, *, #169931, .F. ) ;
#71672=EDGE_CURVE ( 'NONE', #22347, #12842, #201016, .T. ) ;
#71684=FACE_OUTER_BOUND ( 'NONE', #113054, .T. ) ;
#71715=DIRECTION ( 'NONE',  ( 0.000000000000000000, -1.000000000000000000, 0.000000000000000000 ) ) ;
#71716=CARTESIAN_POINT ( 'NONE',  ( -1.642778471875000035, -1.655208332855377051, -2.845375778867859751 ) ) ;
#71740=CARTESIAN_POINT ( 'NONE',  ( -3.285556943749998737, -1.480208332855375453, 1.896917185911908721 ) ) ;
#71773=CARTESIAN_POINT ( 'NONE',  ( 3.285556943750000514, -0.4010416661887095113, 1.896917185911906500 ) ) ;
#71805=CARTESIAN_POINT ( 'NONE',  ( 1.782949938078044916, -3.499999999999999556, -2.093702347113241213 ) ) ;
#71832=ORIENTED_EDGE ( 'NONE', *, *, #189245, .T. ) ;
#71840=CARTESIAN_POINT ( 'NONE',  ( 1.249999999999999334, 8.500000000000000000, -3.469446951953614189E-15 ) ) ;
#71855=ADVANCED_FACE ( 'NONE', ( #120128 ), #28033, .T. ) ;
#71861=CARTESIAN_POINT ( 'NONE',  ( 1.642778471875001811, -3.842708332855375275, 2.845375778867859751 ) ) ;
#71930=CIRCLE ( 'NONE', #161809, 11.00000000000000000 ) ;
#72150=ORIENTED_EDGE ( 'NONE', *, *, #180401, .T. ) ;
#72158=CYLINDRICAL_SURFACE ( 'NONE', #153857, 2.250000000000000444 ) ;
#72197=CARTESIAN_POINT ( 'NONE',  ( 1.001543065824772753E-15, -1.509374999522042016, 3.793834371823810780 ) ) ;
#72264=CARTESIAN_POINT ( 'NONE',  ( 1.642778471875000035, -1.276041666188710400, -2.845375778867859751 ) ) ;
#72290=VECTOR ( 'NONE', #77691, 1000.000000000000000 ) ;
#72329=CARTESIAN_POINT ( 'NONE',  ( 1.642778471875000035, -3.113541666188709200, -2.845375778867859751 ) ) ;
#72338=ORIENTED_EDGE ( 'NONE', *, *, #7876, .T. ) ;
#72384=CARTESIAN_POINT ( 'NONE',  ( 1.734723475976807094E-15, 2.499999999999998668, 0.000000000000000000 ) ) ;
#72416=CARTESIAN_POINT ( 'NONE',  ( 3.361659061299089313, -0.9420306218829536116, 0.2814501367822265787 ) ) ;
#72461=PRODUCT_DEFINITION_CONTEXT ( 'detailed design', #132313, 'design' ) ;
#72525=CARTESIAN_POINT ( 'NONE',  ( -3.475000000000000533, -0.02916666666666653876, -2.006292185433948827 ) ) ;
#72642=EDGE_CURVE ( 'NONE', #197916, #51499, #35329, .T. ) ;
#72778=CARTESIAN_POINT ( 'NONE',  ( 3.475000000000000533, -2.274999999999999467, 0.000000000000000000 ) ) ;
#72798=CARTESIAN_POINT ( 'NONE',  ( -3.285556943750000514, -2.326041666188709112, -1.896917185911906500 ) ) ;
#72841=EDGE_CURVE ( 'NONE', #121330, #59550, #207901, .T. ) ;
#72850=CARTESIAN_POINT ( 'NONE',  ( 3.285556943749998737, -0.3427083328553764408, -1.896917185911906500 ) ) ;
#72941=CARTESIAN_POINT ( 'NONE',  ( -3.285556943750000070, -3.609374999522043659, 0.000000000000000000 ) ) ;
#72947=DIRECTION ( 'NONE',  ( -0.6483454320283800199, 0.000000000000000000, 0.7613463080411787542 ) ) ;
#73016=LINE ( 'NONE', #173766, #127427 ) ;
#73047=CARTESIAN_POINT ( 'NONE',  ( -3.475000000000000533, -1.385416665710749839, -2.006292185433948827 ) ) ;
#73135=LINE ( 'NONE', #74236, #66859 ) ;
#73144=ORIENTED_EDGE ( 'NONE', *, *, #116234, .F. ) ;
#73159=FACE_OUTER_BOUND ( 'NONE', #13632, .T. ) ;
#73220=VERTEX_POINT ( 'NONE', #45776 ) ;
#73228=CARTESIAN_POINT ( 'NONE',  ( 0.000000000000000000, 0.000000000000000000, 0.000000000000000000 ) ) ;
#73264=DIRECTION ( 'NONE',  ( 0.000000000000000000, 0.000000000000000000, -1.000000000000000000 ) ) ;
#73272=CARTESIAN_POINT ( 'NONE',  ( -3.285556943750000514, -1.976041666188710577, -1.896917185911906722 ) ) ;
#73321=ADVANCED_FACE ( 'NONE', ( #14289 ), #161651, .F. ) ;
#73340=CARTESIAN_POINT ( 'NONE',  ( 1.642778471875000035, -3.376041666188708046, -2.845375778867859751 ) ) ;
#73345=EDGE_CURVE ( 'NONE', #213437, #37457, #156787, .T. ) ;
#73363=TOROIDAL_SURFACE ( 'NONE', #11054, 2.349999999999999645, 0.1000000000000000056 ) ;
#73372=EDGE_LOOP ( 'NONE', ( #118335, #130533, #77896, #33959 ) ) ;
#73405=CARTESIAN_POINT ( 'NONE',  ( -3.285556943749998737, -4.017708332855375986, 1.896917185911908499 ) ) ;
#73487=EDGE_CURVE ( 'NONE', #197566, #184334, #83438, .T. ) ;
#73494=CARTESIAN_POINT ( 'NONE',  ( 0.000000000000000000, -0.8934598047668927956, -3.291472234583660672 ) ) ;
#73498=CARTESIAN_POINT ( 'NONE',  ( -1.556029036868112447, 0.5000000000000007772, 1.827231139298829632 ) ) ;
#73504=DIRECTION ( 'NONE',  ( -1.000000000000000000, 0.000000000000000000, 3.491481338843133355E-15 ) ) ;
#73513=DIRECTION ( 'NONE',  ( -0.6483454320283800199, 0.000000000000000000, 0.7613463080411787542 ) ) ;
#73533=ORIENTED_EDGE ( 'NONE', *, *, #102642, .T. ) ;
#73537=AXIS2_PLACEMENT_3D ( 'NONE', #190384, #172022, #8434 ) ;
#73565=CARTESIAN_POINT ( 'NONE',  ( 3.285556943749998737, -0.6052083328553753416, -1.896917185911906500 ) ) ;
#73600=CARTESIAN_POINT ( 'NONE',  ( 1.001543065824772753E-15, -0.6125000000000012657, 4.012584370867899430 ) ) ;
#73605=EDGE_CURVE ( 'NONE', #182913, #202980, #165900, .T. ) ;
#73682=CIRCLE ( 'NONE', #194731, 10.25000000000000000 ) ;
#73758=CARTESIAN_POINT ( 'NONE',  ( -3.420146311865638555, -0.02861402253355461306, -0.3000856501258975517 ) ) ;
#73827=ORIENTED_EDGE ( 'NONE', *, *, #73345, .F. ) ;
#73870=ADVANCED_FACE ( 'NONE', ( #22815 ), #149150, .T. ) ;
#73883=CARTESIAN_POINT ( 'NONE',  ( 1.642778471875001811, -0.7802083328553761632, 2.845375778867859751 ) ) ;
#73895=( BOUNDED_CURVE ( )  B_SPLINE_CURVE ( 2, ( #65340, #31817, #163953, #16592, #212666, #48085, #47009 ),
 .UNSPECIFIED., .F., .T. ) 
 B_SPLINE_CURVE_WITH_KNOTS ( ( 3, 2, 2, 3 ),
 ( 0.1612917726641805993, 0.1666666666666666574, 0.1805555555555555525, 0.1875000000000000000 ),
 .UNSPECIFIED. ) 
 CURVE ( )  GEOMETRIC_REPRESENTATION_ITEM ( )  RATIONAL_B_SPLINE_CURVE ( ( 0.9364346073024809591, 0.9481528537347150287, 1.000000000000000000, 0.8660254037844387076, 1.000000000000000000, 0.9330127018922194093, 0.9330127018922194093 ) ) 
 REPRESENTATION_ITEM ( '' )  );
#73938=CARTESIAN_POINT ( 'NONE',  ( 1.001543065824772753E-15, -2.209374999522042859, 3.793834371823811669 ) ) ;
#74031=CARTESIAN_POINT ( 'NONE',  ( -3.474999999999998312, -0.3208333333333319715, 2.006292185433951047 ) ) ;
#74107=CARTESIAN_POINT ( 'NONE',  ( 0.000000000000000000, 0.5000000000000004441, 0.000000000000000000 ) ) ;
#74119=CARTESIAN_POINT ( 'NONE',  ( 1.001543065824772753E-15, -1.312499999999998224, 4.012584370867899430 ) ) ;
#74188=AXIS2_PLACEMENT_3D ( 'NONE', #109704, #196219, #63006 ) ;
#74199=CARTESIAN_POINT ( 'NONE',  ( -3.475000000000000533, -1.385416665710749617, -2.006292185433948827 ) ) ;
#74224=AXIS2_PLACEMENT_3D ( 'NONE', #95277, #128895, #94208 ) ;
#74236=CARTESIAN_POINT ( 'NONE',  ( 2.550000000000000266, -7.105553651663779391, 1.849324200890695824 ) ) ;
#74240=ORIENTED_EDGE ( 'NONE', *, *, #186277, .F. ) ;
#74259=FACE_OUTER_BOUND ( 'NONE', #56252, .T. ) ;
#74316=ORIENTED_EDGE ( 'NONE', *, *, #132981, .F. ) ;
#74363=CARTESIAN_POINT ( 'NONE',  ( 3.475000000000000533, -2.231249999044084831, 0.000000000000000000 ) ) ;
#74385=VERTEX_POINT ( 'NONE', #170448 ) ;
#74432=CARTESIAN_POINT ( 'NONE',  ( -1.642778471874998480, -3.901041666188709289, 2.845375778867863303 ) ) ;
#74491=CARTESIAN_POINT ( 'NONE',  ( 1.642778471875001811, -0.3427083328553758301, 2.845375778867859751 ) ) ;
#74613=DIRECTION ( 'NONE',  ( -0.000000000000000000, -1.000000000000000000, -0.000000000000000000 ) ) ;
#74640=CARTESIAN_POINT ( 'NONE',  ( 3.285556943750000514, -1.013541666188710888, 1.896917185911906500 ) ) ;
#74644=EDGE_CURVE ( 'NONE', #71536, #110540, #38613, .T. ) ;
#74677=CARTESIAN_POINT ( 'NONE',  ( -3.285556943750000070, -3.959374999522043304, 0.000000000000000000 ) ) ;
#74706=CARTESIAN_POINT ( 'NONE',  ( 4.255647627037052709E-16, 0.5000000000000004441, 3.475000000000000089 ) ) ;
#74708=CARTESIAN_POINT ( 'NONE',  ( 1.500000000000039524, 6.999999999999999112, 10.89724735885167561 ) ) ;
#74866=CARTESIAN_POINT ( 'NONE',  ( -1.737499999999997824, -2.347916665710752415, 3.009438278150925683 ) ) ;
#74887=CARTESIAN_POINT ( 'NONE',  ( 3.475000000000000533, -2.581249999044084475, 0.000000000000000000 ) ) ;
#74908=CARTESIAN_POINT ( 'NONE',  ( 1.347111479062088405E-15, 6.999999999999999112, 11.00000000000000000 ) ) ;
#74948=CARTESIAN_POINT ( 'NONE',  ( 3.285556943750000070, -1.771874999522041083, 0.000000000000000000 ) ) ;
#75002=FACE_OUTER_BOUND ( 'NONE', #159534, .T. ) ;
#75007=CARTESIAN_POINT ( 'NONE',  ( -3.285556943750000070, -2.646874999522041971, 0.000000000000000000 ) ) ;
#75097=CARTESIAN_POINT ( 'NONE',  ( 3.475000000000000533, -0.5250000000000011324, 0.000000000000000000 ) ) ;
#75171=CARTESIAN_POINT ( 'NONE',  ( 1.642778471875000035, -2.676041666188708756, -2.845375778867859751 ) ) ;
#75187=CARTESIAN_POINT ( 'NONE',  ( 0.000000000000000000, -1.837499999999999911, -4.012584370867899430 ) ) ;
#75258=CARTESIAN_POINT ( 'NONE',  ( -3.474999999999998312, -0.6270833323774197554, 2.006292185433951047 ) ) ;
#75300=EDGE_LOOP ( 'NONE', ( #161082, #103614, #105795, #152290 ) ) ;
#75364=DIRECTION ( 'NONE',  ( 0.7613463080411785322, -0.000000000000000000, 0.6483454320283801309 ) ) ;
#75454=CARTESIAN_POINT ( 'NONE',  ( 3.673940397442059868E-16, -3.517800438942085606, -3.000000000000000000 ) ) ;
#75492=CARTESIAN_POINT ( 'NONE',  ( -3.285556943749998737, -2.530208332855374831, 1.896917185911908499 ) ) ;
#75555=CARTESIAN_POINT ( 'NONE',  ( -3.285556943749998737, -0.4302083328553760744, 1.896917185911908499 ) ) ;
#75662=VERTEX_POINT ( 'NONE', #141408 ) ;
#75713=CARTESIAN_POINT ( 'NONE',  ( -3.380278471875000523, -0.05468749976102194044, 0.000000000000000000 ) ) ;
#75740=CARTESIAN_POINT ( 'NONE',  ( -3.475000000000000533, -0.3499999999999996447, 0.000000000000000000 ) ) ;
#75822=ORIENTED_EDGE ( 'NONE', *, *, #171420, .T. ) ;
#75868=DIRECTION ( 'NONE',  ( 0.000000000000000000, 0.000000000000000000, 1.000000000000000000 ) ) ;
#75948=CARTESIAN_POINT ( 'NONE',  ( 0.9311234436981579154, -2.509380368602567302, -3.474999999999996536 ) ) ;
#75988=EDGE_CURVE ( 'NONE', #12413, #60185, #111058, .T. ) ;
#76012=CARTESIAN_POINT ( 'NONE',  ( -3.285556943750000070, -0.8968749995220438587, 0.000000000000000000 ) ) ;
#76068=CARTESIAN_POINT ( 'NONE',  ( -1.642778471874998480, -2.938541666188707602, 2.845375778867863303 ) ) ;
#76157=CARTESIAN_POINT ( 'NONE',  ( -1.737500000000000266, -1.108333333333332726, -3.009438278150923907 ) ) ;
#76204=ORIENTED_EDGE ( 'NONE', *, *, #214167, .F. ) ;
#76247=CARTESIAN_POINT ( 'NONE',  ( -3.474999999999998312, -1.370833333333331350, 2.006292185433951047 ) ) ;
#76271=CARTESIAN_POINT ( 'NONE',  ( 1.500000000000053291, 7.750000000000000000, 15.74999999999999289 ) ) ;
#76321=CARTESIAN_POINT ( 'NONE',  ( 0.000000000000000000, -0.7437499990440860076, -4.012584370867899430 ) ) ;
#76329=LINE ( 'NONE', #9195, #209570 ) ;
#76333=CARTESIAN_POINT ( 'NONE',  ( 0.000000000000000000, 0.5000000000000004441, 0.000000000000000000 ) ) ;
#76375=CARTESIAN_POINT ( 'NONE',  ( -0.9311234436981564722, -2.728130369558482204, 3.474999999999996536 ) ) ;
#76403=CARTESIAN_POINT ( 'NONE',  ( 3.285556943749998737, -0.2552083328553768071, -1.896917185911906500 ) ) ;
#76484=CARTESIAN_POINT ( 'NONE',  ( -1.642778471875000035, -2.705208332855375986, -2.845375778867859751 ) ) ;
#76547=CARTESIAN_POINT ( 'NONE',  ( -3.285556943750000514, -3.988541666188710089, -1.896917185911906500 ) ) ;
#76582=AXIS2_PLACEMENT_3D ( 'NONE', #140719, #109316, #57297 ) ;
#76610=CARTESIAN_POINT ( 'NONE',  ( 3.285556943750000514, -0.6635416661887083567, 1.896917185911906500 ) ) ;
#76714=CARTESIAN_POINT ( 'NONE',  ( 0.000000000000000000, 0.000000000000000000, 0.000000000000000000 ) ) ;
#76754=CARTESIAN_POINT ( 'NONE',  ( 3.285556943750000514, -0.3135416661887098777, 1.896917185911906500 ) ) ;
#76792=CARTESIAN_POINT ( 'NONE',  ( 1.737500000000001155, -2.683333333333332682, 3.009438278150922130 ) ) ;
#76825=DIRECTION ( 'NONE',  ( -0.6483454320283799088, 0.000000000000000000, 0.7613463080411786432 ) ) ;
#76834=CARTESIAN_POINT ( 'NONE',  ( 0.000000000000000000, -3.517800438942085606, 3.000000000000000000 ) ) ;
#76889=VERTEX_POINT ( 'NONE', #9763 ) ;
#76921=CIRCLE ( 'NONE', #104624, 0.5000000000000000000 ) ;
#77034=CARTESIAN_POINT ( 'NONE',  ( 4.255647627037052709E-16, 0.5000000000000004441, 3.475000000000000089 ) ) ;
#77052=CARTESIAN_POINT ( 'NONE',  ( 1.642778471875001811, -0.3427083328553758301, 2.845375778867859751 ) ) ;
#77062=CARTESIAN_POINT ( 'NONE',  ( 0.000000000000000000, 6.999999999999999112, 0.000000000000000000 ) ) ;
#77066=CARTESIAN_POINT ( 'NONE',  ( 3.285556943749998737, -3.142708332855375986, -1.896917185911906500 ) ) ;
#77088=EDGE_LOOP ( 'NONE', ( #49667, #125371, #47953, #15559 ) ) ;
#77126=CARTESIAN_POINT ( 'NONE',  ( 3.285556943750000514, -3.201041666188709112, 1.896917185911906500 ) ) ;
#77130=CIRCLE ( 'NONE', #132528, 3.475000000000000089 ) ;
#77153=CARTESIAN_POINT ( 'NONE',  ( -1.458777222063855294, 0.5999999999999998668, 1.713029193092652225 ) ) ;
#77156=ORIENTED_EDGE ( 'NONE', *, *, #112217, .F. ) ;
#77179=CARTESIAN_POINT ( 'NONE',  ( -0.9311234436981514762, -1.821869630441516952, -3.474999999999999645 ) ) ;
#77217=CARTESIAN_POINT ( 'NONE',  ( -3.474999999999998312, -1.720833333333333881, 2.006292185433951047 ) ) ;
#77314=CARTESIAN_POINT ( 'NONE',  ( -3.474999999999998312, -2.420833333333334725, 2.006292185433951047 ) ) ;
#77350=DIRECTION ( 'NONE',  ( -2.345077562848782505E-16, 0.000000000000000000, -1.000000000000000000 ) ) ;
#77385=CARTESIAN_POINT ( 'NONE',  ( -3.474999999999998312, -1.327083332377416713, 2.006292185433951047 ) ) ;
#77428=ORIENTED_EDGE ( 'NONE', *, *, #23742, .F. ) ;
#77472=CARTESIAN_POINT ( 'NONE',  ( -1.642778471875000035, -0.5177083328553738761, -2.845375778867859751 ) ) ;
#77494=DIRECTION ( 'NONE',  ( 0.000000000000000000, 1.000000000000000000, 0.000000000000000000 ) ) ;
#77617=CARTESIAN_POINT ( 'NONE',  ( -3.285556943749998737, -3.580208332855374653, 1.896917185911908499 ) ) ;
#77680=CARTESIAN_POINT ( 'NONE',  ( 1.642778471875000035, -1.626041666188710044, -2.845375778867859751 ) ) ;
#77691=DIRECTION ( 'NONE',  ( -0.000000000000000000, -1.000000000000000000, -0.000000000000000000 ) ) ;
#77799=CARTESIAN_POINT ( 'NONE',  ( 1.467871227757891193E-11, -3.138498625356828775, -3.379301813585260383 ) ) ;
#77811=DIRECTION ( 'NONE',  ( 0.000000000000000000, 0.000000000000000000, 1.000000000000000000 ) ) ;
#77818=DIRECTION ( 'NONE',  ( 0.000000000000000000, 0.000000000000000000, -1.000000000000000000 ) ) ;
#77826=CARTESIAN_POINT ( 'NONE',  ( -3.285556943749998737, -2.180208332855376518, 1.896917185911908499 ) ) ;
#77852=DIRECTION ( 'NONE',  ( -0.000000000000000000, -1.000000000000000000, -0.000000000000000000 ) ) ;
#77864=CARTESIAN_POINT ( 'NONE',  ( 1.737499999999999378, -2.566666666666668650, -3.009438278150925683 ) ) ;
#77896=ORIENTED_EDGE ( 'NONE', *, *, #41175, .T. ) ;
#78070=PLANE ( 'NONE',  #121818 ) ;
#78072=EDGE_CURVE ( 'NONE', #157226, #27240, #125579, .T. ) ;
#78080=CIRCLE ( 'NONE', #105796, 10.25000000000000000 ) ;
#78107=FACE_OUTER_BOUND ( 'NONE', #41746, .T. ) ;
#78235=AXIS2_PLACEMENT_3D ( 'NONE', #150309, #1875, #164412 ) ;
#78285=CARTESIAN_POINT ( 'NONE',  ( -1.737499999999997824, -2.041666666666667407, 3.009438278150925683 ) ) ;
#78359=CARTESIAN_POINT ( 'NONE',  ( -1.642778471874998480, -2.851041666188706802, 2.845375778867863303 ) ) ;
#78378=CARTESIAN_POINT ( 'NONE',  ( -3.475000000000000533, -1.429166666666668251, -2.006292185433948827 ) ) ;
#78452=CARTESIAN_POINT ( 'NONE',  ( 1.737500000000001155, -0.5395833323774169576, 3.009438278150922130 ) ) ;
#78463=DIRECTION ( 'NONE',  ( -0.000000000000000000, 1.000000000000000000, -0.000000000000000000 ) ) ;
#78508=CARTESIAN_POINT ( 'NONE',  ( -0.9311234436981514762, -2.871869630441517884, -3.474999999999999645 ) ) ;
#78576=LINE ( 'NONE', #176100, #183667 ) ;
#78615=CARTESIAN_POINT ( 'NONE',  ( 0.000000000000000000, -2.384374999522042238, -3.793834371823813445 ) ) ;
#78740=CARTESIAN_POINT ( 'NONE',  ( 1.001543065824772753E-15, -1.071874999522043792, 3.793834371823811669 ) ) ;
#78882=CARTESIAN_POINT ( 'NONE',  ( 1.001543065824772753E-15, -1.771874999522040861, 3.793834371823811669 ) ) ;
#78921=CARTESIAN_POINT ( 'NONE',  ( -3.475000000000000533, -1.779166666666666785, -2.006292185433948827 ) ) ;
#78927=( NAMED_UNIT ( * ) SI_UNIT ( $, .STERADIAN. ) SOLID_ANGLE_UNIT ( ) );
#79084=VECTOR ( 'NONE', #211849, 1000.000000000000000 ) ;
#79120=CARTESIAN_POINT ( 'NONE',  ( -1.500000000000035971, 6.999999999999999112, -9.886859966642587594 ) ) ;
#79131=VERTEX_POINT ( 'NONE', #36192 ) ;
#79138=CARTESIAN_POINT ( 'NONE',  ( -0.7497020852614554309, -3.031334926134804153, 3.474999999999997424 ) ) ;
#79195=CARTESIAN_POINT ( 'NONE',  ( 0.000000000000000000, -0.5468749995220422155, -3.793834371823813001 ) ) ;
#79269=CARTESIAN_POINT ( 'NONE',  ( -3.285556943750000070, -3.346874999522041261, 0.000000000000000000 ) ) ;
#79319=CARTESIAN_POINT ( 'NONE',  ( -0.9311234436981496998, -1.328130369558482293, 3.475000000000000977 ) ) ;
#79351=CARTESIAN_POINT ( 'NONE',  ( 0.000000000000000000, 0.5000000000000004441, 0.000000000000000000 ) ) ;
#79355=ORIENTED_EDGE ( 'NONE', *, *, #9768, .T. ) ;
#79363=CARTESIAN_POINT ( 'NONE',  ( -3.474999999999998312, -2.070833333333331971, 2.006292185433951047 ) ) ;
#79449=CARTESIAN_POINT ( 'NONE',  ( 1.737499999999999378, -3.266666666666667496, -3.009438278150925683 ) ) ;
#79524=CARTESIAN_POINT ( 'NONE',  ( 3.475000000000000533, -1.910416665710751305, 2.006292185433948827 ) ) ;
#79591=AXIS2_PLACEMENT_3D ( 'NONE', #141108, #58744, #172508 ) ;
#79629=CARTESIAN_POINT ( 'NONE',  ( 0.000000000000000000, 0.5999999999999998668, 0.000000000000000000 ) ) ;
#79647=DIRECTION ( 'NONE',  ( -0.7613463080411786432, 0.000000000000000000, -0.6483454320283800199 ) ) ;
#79689=CARTESIAN_POINT ( 'NONE',  ( -3.285556943750000070, -2.646874999522041971, 0.000000000000000000 ) ) ;
#79810=CARTESIAN_POINT ( 'NONE',  ( 3.285556943750000514, -2.063541666188710266, 1.896917185911906500 ) ) ;
#79955=CARTESIAN_POINT ( 'NONE',  ( 0.000000000000000000, -1.596874999522041705, -3.793834371823813001 ) ) ;
#79995=CARTESIAN_POINT ( 'NONE',  ( -1.737499999999997824, -1.341666666666668117, 3.009438278150925683 ) ) ;
#80012=EDGE_CURVE ( 'NONE', #6228, #212297, #81109, .T. ) ;
#80067=CARTESIAN_POINT ( 'NONE',  ( 1.173530994449854870, -3.042800438942089514, 3.270848514539542506 ) ) ;
#80187=CARTESIAN_POINT ( 'NONE',  ( 0.000000000000000000, -0.5000000000000005551, 3.099999999999999201 ) ) ;
#80237=ORIENTED_EDGE ( 'NONE', *, *, #170444, .T. ) ;
#80240=CARTESIAN_POINT ( 'NONE',  ( 0.000000000000000000, 1.000000000000000888, 0.000000000000000000 ) ) ;
#80243=( BOUNDED_SURFACE ( )  B_SPLINE_SURFACE ( 1, 2, ( 
 ( #45001, #178190, #29806, #95892, #161945, #76403, #145726, #42874, #63364, #175001, #26587, #126312, #11394, #127384, #77472, #111111, #129520, #47136, #30880, #163007, #177115, #14589, #59090, #176061, #191211, #158734, #160868, #143591, #147824, #52444, #1522, #212792, #115376, #116430, #99071, #81742, #98020, #117505, #131612, #118570, #68662, #167266, #164075, #17774, #102253, #197611, #64430, #213842, #65461, #18851, #168327, #49255, #101177, #133731, #449, #80686, #67586, #181370, #146777, #183497, #184556, #200793, #82800, #148876, #32994, #165124, #130574, #199738, #51384, #16715, #48206, #132660, #35106, #66517, #198664, #31936, #84935, #151024, #134786, #50312, #196564, #114318, #182423, #36177, #34050, #100123, #166185, #83862, #149953, #180316, #2593, #15655, #6862, #170449, #137970, #41550, #202931, #169389, #135834, #171519, #203989, #54574, #155281, #20974, #120722, #87071, #185623, #19922, #38324, #56712, #37256, #186695, #104400, #22034, #153141, #7941, #122881, #106579, #3652, #55637, #72941, #88145, #86008, #4716, #70791, #154212, #136904, #5784, #71861, #121793, #189905, #152082, #139044, #69730, #201859, #188839, #53505, #172607, #187761 ),
 ( #119640, #39391, #105486, #23112, #24183, #89229, #205070, #40475, #90287, #156356, #206148, #74031, #140122, #57776, #123937, #107663, #103326, #210414, #75097, #95646, #141207, #58841, #158484, #43684, #159543, #126059, #11140, #144412, #176866, #62056, #194173, #93502, #13290, #177941, #10083, #94569, #124998, #127132, #76157, #26331, #145481, #160613, #91368, #208273, #209330, #192022, #129278, #174757, #45818, #193103, #92445, #111939, #211477, #142262, #190955, #42620, #59905, #29555, #60978, #77217, #27404, #157429, #28478, #63113, #109802, #44753, #12214, #110860, #128211, #207218, #78285, #79363, #161697, #195252, #46888, #173691, #143336, #25267, #175811, #9022, #108730, #150775, #200546, #68414, #134541, #31692, #147574, #197366, #47961, #182171, #81496, #15405, #33800, #132418, #113001, #163827, #65217, #16467, #80429, #131369, #32741, #200, #199482, #114077, #213593, #50063, #116186, #97767, #84688, #82547, #165941, #99879, #17526, #83614, #180068, #149696, #14340, #34852, #146529, #212546, #49007, #115125, #98823, #181121, #164872, #1277, #67335, #133480, #51128, #148634, #167015, #117250, #66270, #183249, #64187, #198419, #100927, #18608, #2337 ) ),
 .UNSPECIFIED., .F., .F., .F. ) 
 B_SPLINE_SURFACE_WITH_KNOTS ( ( 2, 2 ),
 ( 3, 2, 2, 2, 2, 2, 2, 2, 2, 2, 2, 2, 2, 2, 2, 2, 2, 2, 2, 2, 2, 2, 2, 2, 2, 2, 2, 2, 2, 2, 2, 2, 2, 2, 2, 2, 2, 2, 2, 2, 2, 2, 2, 2, 2, 2, 2, 2, 2, 2, 2, 2, 2, 2, 2, 2, 2, 2, 2, 2, 2, 2, 2, 2, 2, 2, 2, 2, 2, 3 ),
 ( 0.000000000000000000, 1.000000000000000000 ),
 ( 0.000000000000000000, 0.01388888888888888812, 0.02777777777777777624, 0.04166666666666666435, 0.05555555555555555247, 0.06944444444444444753, 0.08333333333333332871, 0.09722222222222222376, 0.1111111111111111049, 0.1250000000000000000, 0.1388888888888888951, 0.1527777777777777901, 0.1666666666666666574, 0.1805555555555555525, 0.1944444444444444475, 0.2083333333333333426, 0.2222222222222222099, 0.2361111111111111049, 0.2500000000000000000, 0.2638888888888888951, 0.2777777777777777901, 0.2916666666666666852, 0.3055555555555555802, 0.3194444444444444198, 0.3333333333333333148, 0.3472222222222222099, 0.3611111111111111049, 0.3750000000000000000, 0.3888888888888888951, 0.4027777777777777901, 0.4166666666666666852, 0.4305555555555555802, 0.4444444444444444198, 0.4583333333333333148, 0.4722222222222222099, 0.4861111111111111049, 0.5000000000000000000, 0.5138888888888888395, 0.5277777777777777901, 0.5416666666666666297, 0.5555555555555555802, 0.5694444444444444198, 0.5833333333333333703, 0.5972222222222222099, 0.6111111111111111605, 0.6250000000000000000, 0.6388888888888888395, 0.6527777777777777901, 0.6666666666666666297, 0.6805555555555555802, 0.6944444444444444198, 0.7083333333333333703, 0.7222222222222222099, 0.7361111111111111605, 0.7500000000000000000, 0.7638888888888888395, 0.7777777777777777901, 0.7916666666666666297, 0.8055555555555555802, 0.8194444444444444198, 0.8333333333333333703, 0.8472222222222222099, 0.8611111111111111605, 0.8750000000000000000, 0.8888888888888888395, 0.9027777777777777901, 0.9166666666666666297, 0.9305555555555555802, 0.9444444444444444198, 0.9523586252412667985 ),
 .UNSPECIFIED. ) 
 GEOMETRIC_REPRESENTATION_ITEM ( )  RATIONAL_B_SPLINE_SURFACE ( (
 ( 1.000000000000000000, 0.8660254037844387076, 1.000000000000000000, 0.8660254037844387076, 1.000000000000000000, 0.8660254037844387076, 1.000000000000000000, 0.8660254037844387076, 1.000000000000000000, 0.8660254037844387076, 1.000000000000000000, 0.8660254037844387076, 1.000000000000000000, 0.8660254037844387076, 1.000000000000000000, 0.8660254037844387076, 1.000000000000000000, 0.8660254037844387076, 1.000000000000000000, 0.8660254037844387076, 1.000000000000000000, 0.8660254037844387076, 1.000000000000000000, 0.8660254037844387076, 1.000000000000000000, 0.8660254037844387076, 1.000000000000000000, 0.8660254037844387076, 1.000000000000000000, 0.8660254037844387076, 1.000000000000000000, 0.8660254037844387076, 1.000000000000000000, 0.8660254037844387076, 1.000000000000000000, 0.8660254037844387076, 1.000000000000000000, 0.8660254037844387076, 1.000000000000000000, 0.8660254037844387076, 1.000000000000000000, 0.8660254037844387076, 1.000000000000000000, 0.8660254037844387076, 1.000000000000000000, 0.8660254037844387076, 1.000000000000000000, 0.8660254037844387076, 1.000000000000000000, 0.8660254037844387076, 1.000000000000000000, 0.8660254037844387076, 1.000000000000000000, 0.8660254037844387076, 1.000000000000000000, 0.8660254037844387076, 1.000000000000000000, 0.8660254037844387076, 1.000000000000000000, 0.8660254037844387076, 1.000000000000000000, 0.8660254037844387076, 1.000000000000000000, 0.8660254037844387076, 1.000000000000000000, 0.8660254037844387076, 1.000000000000000000, 0.8660254037844387076, 1.000000000000000000, 0.8660254037844387076, 1.000000000000000000, 0.8660254037844387076, 1.000000000000000000, 0.8660254037844387076, 1.000000000000000000, 0.8660254037844387076, 1.000000000000000000, 0.8660254037844387076, 1.000000000000000000, 0.8660254037844387076, 1.000000000000000000, 0.8660254037844387076, 1.000000000000000000, 0.8660254037844387076, 1.000000000000000000, 0.8660254037844387076, 1.000000000000000000, 0.8660254037844387076, 1.000000000000000000, 0.8660254037844387076, 1.000000000000000000, 0.8660254037844387076, 1.000000000000000000, 0.8660254037844387076, 1.000000000000000000, 0.8660254037844387076, 1.000000000000000000, 0.8660254037844387076, 1.000000000000000000, 0.8660254037844387076, 1.000000000000000000, 0.8660254037844387076, 1.000000000000000000, 0.8660254037844387076, 1.000000000000000000, 0.8660254037844387076, 1.000000000000000000, 0.8660254037844387076, 1.000000000000000000, 0.8660254037844387076, 1.000000000000000000, 0.8660254037844387076, 1.000000000000000000, 0.8660254037844387076, 1.000000000000000000, 0.8660254037844387076, 1.000000000000000000, 0.8660254037844387076, 1.000000000000000000, 0.8660254037844387076, 1.000000000000000000, 0.8660254037844387076, 1.000000000000000000, 0.8660254037844387076, 1.000000000000000000, 0.8660254037844387076, 1.000000000000000000, 0.8660254037844387076, 1.000000000000000000, 0.8660254037844387076, 1.000000000000000000, 0.8660254037844387076, 1.000000000000000000, 0.8660254037844387076, 1.000000000000000000, 0.8660254037844387076, 1.000000000000000000, 0.9236584592825519691, 0.9343189473637074638),
 ( 1.000000000000000000, 0.8660254037844387076, 1.000000000000000000, 0.8660254037844387076, 1.000000000000000000, 0.8660254037844387076, 1.000000000000000000, 0.8660254037844387076, 1.000000000000000000, 0.8660254037844387076, 1.000000000000000000, 0.8660254037844387076, 1.000000000000000000, 0.8660254037844387076, 1.000000000000000000, 0.8660254037844387076, 1.000000000000000000, 0.8660254037844387076, 1.000000000000000000, 0.8660254037844387076, 1.000000000000000000, 0.8660254037844387076, 1.000000000000000000, 0.8660254037844387076, 1.000000000000000000, 0.8660254037844387076, 1.000000000000000000, 0.8660254037844387076, 1.000000000000000000, 0.8660254037844387076, 1.000000000000000000, 0.8660254037844387076, 1.000000000000000000, 0.8660254037844387076, 1.000000000000000000, 0.8660254037844387076, 1.000000000000000000, 0.8660254037844387076, 1.000000000000000000, 0.8660254037844387076, 1.000000000000000000, 0.8660254037844387076, 1.000000000000000000, 0.8660254037844387076, 1.000000000000000000, 0.8660254037844387076, 1.000000000000000000, 0.8660254037844387076, 1.000000000000000000, 0.8660254037844387076, 1.000000000000000000, 0.8660254037844387076, 1.000000000000000000, 0.8660254037844387076, 1.000000000000000000, 0.8660254037844387076, 1.000000000000000000, 0.8660254037844387076, 1.000000000000000000, 0.8660254037844387076, 1.000000000000000000, 0.8660254037844387076, 1.000000000000000000, 0.8660254037844387076, 1.000000000000000000, 0.8660254037844387076, 1.000000000000000000, 0.8660254037844387076, 1.000000000000000000, 0.8660254037844387076, 1.000000000000000000, 0.8660254037844387076, 1.000000000000000000, 0.8660254037844387076, 1.000000000000000000, 0.8660254037844387076, 1.000000000000000000, 0.8660254037844387076, 1.000000000000000000, 0.8660254037844387076, 1.000000000000000000, 0.8660254037844387076, 1.000000000000000000, 0.8660254037844387076, 1.000000000000000000, 0.8660254037844387076, 1.000000000000000000, 0.8660254037844387076, 1.000000000000000000, 0.8660254037844387076, 1.000000000000000000, 0.8660254037844387076, 1.000000000000000000, 0.8660254037844387076, 1.000000000000000000, 0.8660254037844387076, 1.000000000000000000, 0.8660254037844387076, 1.000000000000000000, 0.8660254037844387076, 1.000000000000000000, 0.8660254037844387076, 1.000000000000000000, 0.8660254037844387076, 1.000000000000000000, 0.8660254037844387076, 1.000000000000000000, 0.8660254037844387076, 1.000000000000000000, 0.8660254037844387076, 1.000000000000000000, 0.8660254037844387076, 1.000000000000000000, 0.8660254037844387076, 1.000000000000000000, 0.8660254037844387076, 1.000000000000000000, 0.8660254037844387076, 1.000000000000000000, 0.8660254037844387076, 1.000000000000000000, 0.8660254037844387076, 1.000000000000000000, 0.8660254037844387076, 1.000000000000000000, 0.8660254037844387076, 1.000000000000000000, 0.8660254037844387076, 1.000000000000000000, 0.8660254037844387076, 1.000000000000000000, 0.8660254037844387076, 1.000000000000000000, 0.8660254037844387076, 1.000000000000000000, 0.8660254037844387076, 1.000000000000000000, 0.9236584592825519691, 0.9343189473637074638) ) ) 
 REPRESENTATION_ITEM ( '' )  SURFACE ( )  );
#80272=CARTESIAN_POINT ( 'NONE',  ( 0.000000000000000000, -0.8934598047668927956, -3.291472234583660672 ) ) ;
#80331=CARTESIAN_POINT ( 'NONE',  ( 1.001543065824772753E-15, -3.959374999522043304, 3.793834371823811669 ) ) ;
#80335=VERTEX_POINT ( 'NONE', #195935 ) ;
#80387=DIRECTION ( 'NONE',  ( -0.000000000000000000, 1.000000000000000000, -0.000000000000000000 ) ) ;
#80390=CARTESIAN_POINT ( 'NONE',  ( -1.737500000000000266, -1.808333333333332016, -3.009438278150923907 ) ) ;
#80402=CARTESIAN_POINT ( 'NONE',  ( 2.331613029862944941, -3.165258756643079430, -2.416022285627570820 ) ) ;
#80419=CARTESIAN_POINT ( 'NONE',  ( 1.499999999999959588, 7.750000000000000000, -10.86128356754324820 ) ) ;
#80429=CARTESIAN_POINT ( 'NONE',  ( -1.737500000000000266, -2.858333333333334281, -3.009438278150923907 ) ) ;
#80435=( BOUNDED_CURVE ( )  B_SPLINE_CURVE ( 2, ( #4346, #70413, #87764, #68288, #19550, #67216, #134421, #101883, #35804 ),
 .UNSPECIFIED., .F., .T. ) 
 B_SPLINE_CURVE_WITH_KNOTS ( ( 3, 2, 2, 2, 3 ),
 ( 0.3958333333333333703, 0.4027777777777777901, 0.4166666666666666852, 0.4305555555555555802, 0.4375000000000000000 ),
 .UNSPECIFIED. ) 
 CURVE ( )  GEOMETRIC_REPRESENTATION_ITEM ( )  RATIONAL_B_SPLINE_CURVE ( ( 0.9330127018922194093, 0.9330127018922196314, 1.000000000000000000, 0.8660254037844387076, 1.000000000000000000, 0.8660254037844387076, 1.000000000000000000, 0.9330127018922194093, 0.9330127018922194093 ) ) 
 REPRESENTATION_ITEM ( '' )  );
#80500=CARTESIAN_POINT ( 'NONE',  ( 1.737500000000001155, -2.989583332377417690, 3.009438278150922130 ) ) ;
#80517=CARTESIAN_POINT ( 'NONE',  ( 3.130865642711470276, -4.000192543527539613, -1.507748429708645199 ) ) ;
#80593=CARTESIAN_POINT ( 'NONE',  ( -3.474999999999998312, -3.427083332377419467, 2.006292185433951047 ) ) ;
#80609=VECTOR ( 'NONE', #23110, 1000.000000000000000 ) ;
#80686=CARTESIAN_POINT ( 'NONE',  ( 3.285556943750000514, -1.713541666188707735, 1.896917185911906500 ) ) ;
#80756=CARTESIAN_POINT ( 'NONE',  ( 0.000000000000000000, -0.8934598047668927956, -3.291472234583660672 ) ) ;
#80763=CARTESIAN_POINT ( 'NONE',  ( 0.9311234436981489226, -2.303119629485602005, 3.475000000000000533 ) ) ;
#80805=CARTESIAN_POINT ( 'NONE',  ( -1.499999999999946709, 7.750000000000000000, 15.75000000000000711 ) ) ;
#80826=AXIS2_PLACEMENT_3D ( 'NONE', #60867, #58739, #206044 ) ;
#80888=CARTESIAN_POINT ( 'NONE',  ( 3.285556943749998737, -2.355208332855375453, -1.896917185911906500 ) ) ;
#81029=CARTESIAN_POINT ( 'NONE',  ( -1.642778471874998480, -2.501041666188707158, 2.845375778867863303 ) ) ;
#81069=CARTESIAN_POINT ( 'NONE',  ( -3.475000000000000533, -1.750000000000001554, 0.000000000000000000 ) ) ;
#81071=CARTESIAN_POINT ( 'NONE',  ( 3.285556943750000514, -3.551041666188707424, 1.896917185911906500 ) ) ;
#81106=CARTESIAN_POINT ( 'NONE',  ( 0.000000000000000000, 0.9000000000000014655, 0.000000000000000000 ) ) ;
#81109=LINE ( 'NONE', #12890, #187646 ) ;
#81136=CARTESIAN_POINT ( 'NONE',  ( -1.432719062495390716, -3.042800438942089514, 3.165902886691621010 ) ) ;
#81214=EDGE_LOOP ( 'NONE', ( #33614, #200569, #203589, #69433, #197196 ) ) ;
#81245=CARTESIAN_POINT ( 'NONE',  ( -1.499999999999964029, 6.999999999999999112, 9.886859966642596476 ) ) ;
#81274=DIRECTION ( 'NONE',  ( 0.000000000000000000, 0.000000000000000000, 1.000000000000000000 ) ) ;
#81328=CARTESIAN_POINT ( 'NONE',  ( 0.000000000000000000, -0.1968749995220437643, -3.793834371823813001 ) ) ;
#81453=CARTESIAN_POINT ( 'NONE',  ( -3.475000000000000533, -1.429166666666668473, -2.006292185433948827 ) ) ;
#81496=CARTESIAN_POINT ( 'NONE',  ( 3.475000000000000533, -2.624999999999998668, 0.000000000000000000 ) ) ;
#81517=ORIENTED_EDGE ( 'NONE', *, *, #125041, .T. ) ;
#81581=CARTESIAN_POINT ( 'NONE',  ( 1.001543065824772753E-15, -3.412500000000000977, 4.012584370867899430 ) ) ;
#81594=CARTESIAN_POINT ( 'NONE',  ( 0.000000000000000000, 5.999999999999998224, 0.000000000000000000 ) ) ;
#81599=FILL_AREA_STYLE_COLOUR ( '', #28867 ) ;
#81650=CARTESIAN_POINT ( 'NONE',  ( -1.737500000000000266, -2.464583332377416447, -3.009438278150923907 ) ) ;
#81728=AXIS2_PLACEMENT_3D ( 'NONE', #79351, #15391, #145468 ) ;
#81742=CARTESIAN_POINT ( 'NONE',  ( -3.285556943749998737, -1.130208332855377140, 1.896917185911908499 ) ) ;
#81783=CARTESIAN_POINT ( 'NONE',  ( 2.550000000000000266, 2.499999999999998668, -1.849324200890695824 ) ) ;
#81793=VERTEX_POINT ( 'NONE', #3615 ) ;
#81842=VECTOR ( 'NONE', #139063, 1000.000000000000000 ) ;
#81945=CARTESIAN_POINT ( 'NONE',  ( -1.642778471874998480, -2.501041666188707158, 2.845375778867863303 ) ) ;
#82008=VERTEX_POINT ( 'NONE', #7902 ) ;
#82044=ORIENTED_EDGE ( 'NONE', *, *, #93974, .F. ) ;
#82056=EDGE_CURVE ( 'NONE', #169163, #210464, #108555, .T. ) ;
#82083=CARTESIAN_POINT ( 'NONE',  ( -3.285556943750000514, -2.588541666188707513, -1.896917185911906500 ) ) ;
#82123=CARTESIAN_POINT ( 'NONE',  ( -1.737500000000000266, -3.908333333333333215, -3.009438278150923907 ) ) ;
#82125=CARTESIAN_POINT ( 'NONE',  ( 1.642778471875000035, -2.763541666188709556, -2.845375778867859751 ) ) ;
#82243=CARTESIAN_POINT ( 'NONE',  ( -2.365690013115477441, -0.8887487162373138849, -2.290443095882321423 ) ) ;
#82344=ORIENTED_EDGE ( 'NONE', *, *, #51928, .F. ) ;
#82354=CARTESIAN_POINT ( 'NONE',  ( -3.387811967423835835, -0.9606458502256096654, 0.3526910777686760312 ) ) ;
#82382=CARTESIAN_POINT ( 'NONE',  ( -3.285556943750000070, -1.859374999522041882, 0.000000000000000000 ) ) ;
#82452=CARTESIAN_POINT ( 'NONE',  ( 3.285556943749998737, -3.842708332855377051, -1.896917185911906500 ) ) ;
#82468=DIRECTION ( 'NONE',  ( 0.000000000000000000, 0.000000000000000000, 1.000000000000000000 ) ) ;
#82484=EDGE_CURVE ( 'NONE', #145929, #9969, #41005, .T. ) ;
#82500=ORIENTED_EDGE ( 'NONE', *, *, #33740, .F. ) ;
#82502=CARTESIAN_POINT ( 'NONE',  ( -1.737500000000000266, -1.458333333333332371, -3.009438278150923907 ) ) ;
#82536=CARTESIAN_POINT ( 'NONE',  ( -3.427332196402439468, -0.01934385360880741186, -0.4151528345443494805 ) ) ;
#82547=CARTESIAN_POINT ( 'NONE',  ( -3.475000000000000533, -3.179166666666664476, -2.006292185433948827 ) ) ;
#82560=CIRCLE ( 'NONE', #134555, 2.600000000000000533 ) ;
#82637=CARTESIAN_POINT ( 'NONE',  ( 1.737500000000001155, -3.383333333333331971, 3.009438278150922130 ) ) ;
#82650=CARTESIAN_POINT ( 'NONE',  ( -1.642778471874998480, -0.4885416661887104217, 2.845375778867863303 ) ) ;
#82653=LINE ( 'NONE', #150881, #98966 ) ;
#82711=CARTESIAN_POINT ( 'NONE',  ( 3.475000000000000533, -2.931249999044084120, 0.000000000000000000 ) ) ;
#82755=ORIENTED_EDGE ( 'NONE', *, *, #170444, .F. ) ;
#82775=( BOUNDED_CURVE ( )  B_SPLINE_CURVE ( 2, ( #214283, #135245, #119032, #50766, #181816, #200195, #116895, #150420, #36641 ),
 .UNSPECIFIED., .F., .T. ) 
 B_SPLINE_CURVE_WITH_KNOTS ( ( 3, 2, 2, 2, 3 ),
 ( 0.3541666666666666852, 0.3611111111111111049, 0.3750000000000000000, 0.3888888888888888951, 0.3958333333333333703 ),
 .UNSPECIFIED. ) 
 CURVE ( )  GEOMETRIC_REPRESENTATION_ITEM ( )  RATIONAL_B_SPLINE_CURVE ( ( 0.9330127018922194093, 0.9330127018922196314, 1.000000000000000000, 0.8660254037844387076, 1.000000000000000000, 0.8660254037844387076, 1.000000000000000000, 0.9330127018922190762, 0.9330127018922194093 ) ) 
 REPRESENTATION_ITEM ( '' )  );
#82800=CARTESIAN_POINT ( 'NONE',  ( -1.642778471875000035, -1.917708332855375897, -2.845375778867859751 ) ) ;
#82814=ADVANCED_FACE ( 'NONE', ( #4431 ), #164838, .T. ) ;
#82992=CARTESIAN_POINT ( 'NONE',  ( -3.294361253650757604, -0.1042918288308124219, 0.000000000000000000 ) ) ;
#82999=CARTESIAN_POINT ( 'NONE',  ( -3.285556943749998737, -2.880208332855377584, 1.896917185911908499 ) ) ;
#83014=ORIENTED_EDGE ( 'NONE', *, *, #88762, .F. ) ;
#83097=ORIENTED_EDGE ( 'NONE', *, *, #55534, .F. ) ;
#83147=CARTESIAN_POINT ( 'NONE',  ( 1.001543065824772753E-15, -3.521874999522041083, 3.793834371823811669 ) ) ;
#83185=CARTESIAN_POINT ( 'NONE',  ( -3.475000000000000533, -3.529166666666667229, -2.006292185433948827 ) ) ;
#83187=CARTESIAN_POINT ( 'NONE',  ( 3.285556943749998737, -3.492708332855374742, -1.896917185911906500 ) ) ;
#83252=CARTESIAN_POINT ( 'NONE',  ( 0.000000000000000000, -1.334374999522042859, -3.793834371823813001 ) ) ;
#83328=AXIS2_PLACEMENT_3D ( 'NONE', #187790, #169418, #55664 ) ;
#83379=VECTOR ( 'NONE', #140646, 1000.000000000000000 ) ;
#83400=DIRECTION ( 'NONE',  ( 0.000000000000000000, 1.000000000000000000, 0.000000000000000000 ) ) ;
#83438=CIRCLE ( 'NONE', #385, 2.750000000000000444 ) ;
#83448=CARTESIAN_POINT ( 'NONE',  ( 3.285556943750000070, -2.384374999522043126, 0.000000000000000000 ) ) ;
#83454=CARTESIAN_POINT ( 'NONE',  ( 0.9311234436981525864, -1.296869630441517707, 3.474999999999998757 ) ) ;
#83478=PLANE ( 'NONE',  #133991 ) ;
#83539=TOROIDAL_SURFACE ( 'NONE', #204575, 2.649999999999999911, 0.1000000000000000056 ) ;
#83547=EDGE_CURVE ( 'NONE', #164595, #111991, #122692, .T. ) ;
#83567=( BOUNDED_CURVE ( )  B_SPLINE_CURVE ( 2, ( #191286, #92768, #168916, #86604, #10409, #44009, #174022, #152670, #202456 ),
 .UNSPECIFIED., .F., .T. ) 
 B_SPLINE_CURVE_WITH_KNOTS ( ( 3, 2, 2, 2, 3 ),
 ( 0.4375000000000000000, 0.4444444444444444198, 0.4583333333333333148, 0.4722222222222222099, 0.4791666666666666852 ),
 .UNSPECIFIED. ) 
 CURVE ( )  GEOMETRIC_REPRESENTATION_ITEM ( )  RATIONAL_B_SPLINE_CURVE ( ( 0.9330127018922194093, 0.9330127018922194093, 1.000000000000000000, 0.8660254037844387076, 1.000000000000000000, 0.8660254037844387076, 1.000000000000000000, 0.9330127018922190762, 0.9330127018922194093 ) ) 
 REPRESENTATION_ITEM ( '' )  );
#83587=CARTESIAN_POINT ( 'NONE',  ( 2.862582142408669927, -3.212557612082180825, 1.662679547930521640 ) ) ;
#83612=CARTESIAN_POINT ( 'NONE',  ( 1.734723475976807094E-15, -7.105553651663779391, 0.000000000000000000 ) ) ;
#83614=CARTESIAN_POINT ( 'NONE',  ( 3.475000000000000533, -3.295833333333334725, -2.006292185433951047 ) ) ;
#83703=CARTESIAN_POINT ( 'NONE',  ( -3.474999999999998312, -3.470833333333334103, 2.006292185433951047 ) ) ;
#83739=CARTESIAN_POINT ( 'NONE',  ( -1.642778471875000035, -1.567708332855376252, -2.845375778867859751 ) ) ;
#83746=B_SPLINE_CURVE_WITH_KNOTS ( 'NONE', 3,
 ( #48898, #196214, #181014, #147471, #145376, #162654 ),
 .UNSPECIFIED., .F., .F.,
 ( 4, 2, 4 ),
 ( 0.000000000000000000, 0.0007995527602724504957, 0.001599105520544900991 ),
 .UNSPECIFIED. ) ;
#83774=CARTESIAN_POINT ( 'NONE',  ( 1.737499999999999378, -2.172916665710750816, -3.009438278150925683 ) ) ;
#83798=CARTESIAN_POINT ( 'NONE',  ( 1.737499999999999378, -1.516666666666666163, -3.009438278150925683 ) ) ;
#83832=ORIENTED_EDGE ( 'NONE', *, *, #132234, .F. ) ;
#83862=CARTESIAN_POINT ( 'NONE',  ( 0.000000000000000000, -2.646874999522040639, -3.793834371823813001 ) ) ;
#84072=CARTESIAN_POINT ( 'NONE',  ( 0.000000000000000000, -2.996874999522043392, -3.793834371823813001 ) ) ;
#84073=AXIS2_PLACEMENT_3D ( 'NONE', #77062, #44595, #95494 ) ;
#84085=MANIFOLD_SOLID_BREP ( 'Fillet1', #212477 ) ;
#84089=AXIS2_PLACEMENT_3D ( 'NONE', #188742, #121703, #204972 ) ;
#84112=DIRECTION ( 'NONE',  ( -0.6483454320283799088, 0.000000000000000000, 0.7613463080411786432 ) ) ;
#84205=CIRCLE ( 'NONE', #80826, 3.017800438942085606 ) ;
#84223=CARTESIAN_POINT ( 'NONE',  ( 3.475000000000000533, -0.4958333333333350690, -2.006292185433951047 ) ) ;
#84266=CARTESIAN_POINT ( 'NONE',  ( -1.737500000000000266, -3.208333333333333925, -3.009438278150923907 ) ) ;
#84268=CARTESIAN_POINT ( 'NONE',  ( 3.285556943750000070, -2.821874999522043570, 0.000000000000000000 ) ) ;
#84330=CARTESIAN_POINT ( 'NONE',  ( 3.285556943749998737, -2.442708332855375364, -1.896917185911906500 ) ) ;
#84346=EDGE_CURVE ( 'NONE', #160528, #70696, #189005, .T. ) ;
#84359=AXIS2_PLACEMENT_3D ( 'NONE', #30226, #96310, #76825 ) ;
#84488=CARTESIAN_POINT ( 'NONE',  ( -3.330162143076817571, -0.9219660286950489558, 0.1033982544314127755 ) ) ;
#84498=CARTESIAN_POINT ( 'NONE',  ( 1.782949938078045582, -1.600000000000000755, -2.093702347113241213 ) ) ;
#84520=CARTESIAN_POINT ( 'NONE',  ( 3.285556943750000070, -3.084374999522042415, 0.000000000000000000 ) ) ;
#84565=CIRCLE ( 'NONE', #74224, 10.25000000000000000 ) ;
#84590=CARTESIAN_POINT ( 'NONE',  ( 1.255262969126037241E-15, 2.000000000000001776, -10.25000000000000000 ) ) ;
#84592=CARTESIAN_POINT ( 'NONE',  ( 2.550000000000000266, -7.105553651663779391, -1.849324200890695824 ) ) ;
#84656=( BOUNDED_CURVE ( )  B_SPLINE_CURVE ( 3, ( #60753, #10920, #63954, #126916 ),
 .UNSPECIFIED., .F., .T. ) 
 B_SPLINE_CURVE_WITH_KNOTS ( ( 4, 4 ),
 ( 1.576609981660940463, 1.599396078175049585 ),
 .UNSPECIFIED. ) 
 CURVE ( )  GEOMETRIC_REPRESENTATION_ITEM ( )  RATIONAL_B_SPLINE_CURVE ( ( 1.000000000000000000, 0.9999567332851475587, 0.9999567332851475587, 1.000000000000000000 ) ) 
 REPRESENTATION_ITEM ( '' )  );
#84676=CARTESIAN_POINT ( 'NONE',  ( -3.424027514449416554, -0.02102871867356865404, -0.4191108859519457885 ) ) ;
#84688=CARTESIAN_POINT ( 'NONE',  ( -3.475000000000000533, -3.149999999999999911, 0.000000000000000000 ) ) ;
#84693=VECTOR ( 'NONE', #47029, 1000.000000000000000 ) ;
#84706=DIRECTION ( 'NONE',  ( 0.000000000000000000, -1.000000000000000000, -0.000000000000000000 ) ) ;
#84813=CARTESIAN_POINT ( 'NONE',  ( 1.642778471875001811, -1.392708332855374653, 2.845375778867859751 ) ) ;
#84848=CARTESIAN_POINT ( 'NONE',  ( 1.642778471875001811, -1.130208332855375808, 2.845375778867859751 ) ) ;
#84859=TOROIDAL_SURFACE ( 'NONE', #147182, 2.600000000000000089, 0.1000000000000000056 ) ;
#84870=CARTESIAN_POINT ( 'NONE',  ( 1.737500000000001155, -1.633333333333333748, 3.009438278150922130 ) ) ;
#84935=CARTESIAN_POINT ( 'NONE',  ( 1.642778471875000035, -2.326041666188709112, -2.845375778867859751 ) ) ;
#85026=CIRCLE ( 'NONE', #168075, 11.00000000000000000 ) ;
#85061=DIRECTION ( 'NONE',  ( 0.000000000000000000, -1.000000000000000000, 0.000000000000000000 ) ) ;
#85130=VERTEX_POINT ( 'NONE', #198273 ) ;
#85138=CARTESIAN_POINT ( 'NONE',  ( -1.642778471874998480, -3.551041666188709645, 2.845375778867863303 ) ) ;
#85181=DIRECTION ( 'NONE',  ( 0.000000000000000000, -1.000000000000000000, 0.000000000000000000 ) ) ;
#85261=CARTESIAN_POINT ( 'NONE',  ( -1.737500000000000266, -2.158333333333331439, -3.009438278150923907 ) ) ;
#85266=CARTESIAN_POINT ( 'NONE',  ( 0.000000000000000000, 8.500000000000000000, 0.000000000000000000 ) ) ;
#85290=CARTESIAN_POINT ( 'NONE',  ( -3.475000000000000533, -0.6999999999999992895, 0.000000000000000000 ) ) ;
#85336=CARTESIAN_POINT ( 'NONE',  ( 3.285556943750000514, -2.063541666188710266, 1.896917185911906500 ) ) ;
#85396=CARTESIAN_POINT ( 'NONE',  ( -3.285556943750000514, -1.976041666188710577, -1.896917185911906500 ) ) ;
#85478=VERTEX_POINT ( 'NONE', #189801 ) ;
#85482=CARTESIAN_POINT ( 'NONE',  ( 0.8710647801728804707, -0.9715519045938938447, 3.328597978068449148 ) ) ;
#85531=CARTESIAN_POINT ( 'NONE',  ( 0.9311234436981512541, -2.159380368602565881, -3.475000000000000977 ) ) ;
#85545=CIRCLE ( 'NONE', #130484, 0.09999999999999982514 ) ;
#85582=CARTESIAN_POINT ( 'NONE',  ( -1.642778471875000035, -2.967708332855374831, -2.845375778867859751 ) ) ;
#85587=EDGE_CURVE ( 'NONE', #179285, #132336, #131738, .T. ) ;
#85589=CARTESIAN_POINT ( 'NONE',  ( 3.475000000000000533, -1.195833333333332194, -2.006292185433951047 ) ) ;
#85609=CIRCLE ( 'NONE', #189509, 11.00000000000000000 ) ;
#85615=ORIENTED_EDGE ( 'NONE', *, *, #3232, .F. ) ;
#85669=ORIENTED_EDGE ( 'NONE', *, *, #209595, .F. ) ;
#85701=ORIENTED_EDGE ( 'NONE', *, *, #164027, .T. ) ;
#85746=ORIENTED_EDGE ( 'NONE', *, *, #179232, .F. ) ;
#85859=CARTESIAN_POINT ( 'NONE',  ( 0.000000000000000000, 8.500000000000000000, 0.000000000000000000 ) ) ;
#85863=DIRECTION ( 'NONE',  ( -0.000000000000000000, 1.000000000000000000, -0.000000000000000000 ) ) ;
#85885=CARTESIAN_POINT ( 'NONE',  ( 3.285556943750000070, -2.384374999522043126, 0.000000000000000000 ) ) ;
#85921=CARTESIAN_POINT ( 'NONE',  ( -1.737499999999997824, -4.097916665710750195, 3.009438278150925683 ) ) ;
#85978=EDGE_LOOP ( 'NONE', ( #44412, #6603, #115593, #27985, #103134, #55412, #111147 ) ) ;
#86008=CARTESIAN_POINT ( 'NONE',  ( -1.642778471875000035, -3.667708332855373676, -2.845375778867859751 ) ) ;
#86030=ORIENTED_EDGE ( 'NONE', *, *, #21279, .F. ) ;
#86054=ORIENTED_EDGE ( 'NONE', *, *, #93974, .T. ) ;
#86071=CARTESIAN_POINT ( 'NONE',  ( 0.000000000000000000, 6.999999999999999112, 0.000000000000000000 ) ) ;
#86079=CARTESIAN_POINT ( 'NONE',  ( -0.2190597442376090720, -0.9782633227147815580, 3.454112556983322424 ) ) ;
#86107=EDGE_CURVE ( 'NONE', #182913, #211538, #84565, .T. ) ;
#86135=EDGE_CURVE ( 'NONE', #80335, #9969, #161325, .T. ) ;
#86194=LINE ( 'NONE', #3838, #172568 ) ;
#86209=CARTESIAN_POINT ( 'NONE',  ( 2.960184520039609524, -4.109567588314592790, -1.425549731837409961 ) ) ;
#86219=EDGE_LOOP ( 'NONE', ( #69282, #144710, #197279, #11202 ) ) ;
#86223=DIRECTION ( 'NONE',  ( 0.000000000000000000, 0.000000000000000000, 1.000000000000000000 ) ) ;
#86259=DIRECTION ( 'NONE',  ( 0.000000000000000000, 1.000000000000000000, 0.000000000000000000 ) ) ;
#86336=CARTESIAN_POINT ( 'NONE',  ( -0.9311234436981447038, -2.171869630441516374, -3.475000000000004086 ) ) ;
#86338=CARTESIAN_POINT ( 'NONE',  ( -1.642778471875000035, -2.005208332855376696, -2.845375778867859751 ) ) ;
#86362=CARTESIAN_POINT ( 'NONE',  ( 1.737499999999999378, -0.4666666666666673402, -3.009438278150925683 ) ) ;
#86398=ADVANCED_FACE ( 'NONE', ( #201252 ), #48646, .T. ) ;
#86408=CARTESIAN_POINT ( 'NONE',  ( 3.285556943749998737, -1.305208332855376296, -1.896917185911906500 ) ) ;
#86469=CARTESIAN_POINT ( 'NONE',  ( -3.285556943750000070, -2.296874999522042327, 0.000000000000000000 ) ) ;
#86604=CARTESIAN_POINT ( 'NONE',  ( 3.475000000000000533, -1.895833333333332815, -2.006292185433951047 ) ) ;
#86653=CARTESIAN_POINT ( 'NONE',  ( 3.285556943750000514, -3.113541666188709645, 1.896917185911906500 ) ) ;
#86657=LINE ( 'NONE', #150612, #52916 ) ;
#86683=CARTESIAN_POINT ( 'NONE',  ( 0.000000000000000000, 0.5000000000000004441, -3.475000000000000089 ) ) ;
#86746=DIRECTION ( 'NONE',  ( 0.000000000000000000, 0.000000000000000000, -1.000000000000000000 ) ) ;
#86811=CARTESIAN_POINT ( 'NONE',  ( -3.419573553597315296, -0.02497503617633969886, -0.3927721855967285514 ) ) ;
#86847=ORIENTED_EDGE ( 'NONE', *, *, #180401, .F. ) ;
#86862=DIRECTION ( 'NONE',  ( 0.000000000000000000, 1.000000000000000000, 0.000000000000000000 ) ) ;
#86896=CARTESIAN_POINT ( 'NONE',  ( 0.000000000000000000, 2.499999999999998668, 0.000000000000000000 ) ) ;
#86982=CARTESIAN_POINT ( 'NONE',  ( 1.642778471875001811, -0.7802083328553761632, 2.845375778867859751 ) ) ;
#87016=ORIENTED_EDGE ( 'NONE', *, *, #20202, .T. ) ;
#87042=ORIENTED_EDGE ( 'NONE', *, *, #68949, .T. ) ;
#87071=CARTESIAN_POINT ( 'NONE',  ( 1.001543065824772753E-15, -3.171874999522042327, 3.793834371823811669 ) ) ;
#87106=( BOUNDED_CURVE ( )  B_SPLINE_CURVE ( 2, ( #198985, #136167, #166519, #19186, #168647, #201125, #85261, #86336, #119974 ),
 .UNSPECIFIED., .F., .T. ) 
 B_SPLINE_CURVE_WITH_KNOTS ( ( 3, 2, 2, 2, 3 ),
 ( 0.4791666666666666852, 0.4861111111111111049, 0.5000000000000000000, 0.5138888888888888395, 0.5208333333333333703 ),
 .UNSPECIFIED. ) 
 CURVE ( )  GEOMETRIC_REPRESENTATION_ITEM ( )  RATIONAL_B_SPLINE_CURVE ( ( 0.9330127018922194093, 0.9330127018922196314, 1.000000000000000000, 0.8660254037844387076, 1.000000000000000000, 0.8660254037844387076, 1.000000000000000000, 0.9330127018922187432, 0.9330127018922192983 ) ) 
 REPRESENTATION_ITEM ( '' )  );
#87235=DIRECTION ( 'NONE',  ( 0.3162277660168373861, -0.9486832980505139901, 0.000000000000000000 ) ) ;
#87298=CARTESIAN_POINT ( 'NONE',  ( 0.000000000000000000, 5.999999999999998224, 0.000000000000000000 ) ) ;
#87359=ORIENTED_EDGE ( 'NONE', *, *, #120662, .T. ) ;
#87415=CARTESIAN_POINT ( 'NONE',  ( -3.285556943750000514, -1.276041666188709511, -1.896917185911906722 ) ) ;
#87481=CARTESIAN_POINT ( 'NONE',  ( 1.642778471875000035, -0.5760416661887077794, -2.845375778867859751 ) ) ;
#87541=CARTESIAN_POINT ( 'NONE',  ( 0.000000000000000000, -2.734374999522040550, -3.793834371823813001 ) ) ;
#87549=DIRECTION ( 'NONE',  ( 0.000000000000000000, 0.000000000000000000, 1.000000000000000000 ) ) ;
#87722=CARTESIAN_POINT ( 'NONE',  ( 1.642778471875000035, -4.076041666188710444, -2.845375778867859751 ) ) ;
#87724=DIRECTION ( 'NONE',  ( 0.000000000000000000, 0.000000000000000000, -1.000000000000000000 ) ) ;
#87725=ORIENTED_EDGE ( 'NONE', *, *, #95039, .F. ) ;
#87750=LINE ( 'NONE', #74706, #105964 ) ;
#87764=CARTESIAN_POINT ( 'NONE',  ( -1.737499999999997824, -1.997916665710752770, 3.009438278150925683 ) ) ;
#87975=CARTESIAN_POINT ( 'NONE',  ( 3.475000000000000533, -2.245833333333331350, -2.006292185433951047 ) ) ;
#87998=CARTESIAN_POINT ( 'NONE',  ( -1.642778471874998480, -2.238541666188708312, 2.845375778867863303 ) ) ;
#88020=CARTESIAN_POINT ( 'NONE',  ( -1.642778471875000035, -1.917708332855375897, -2.845375778867859751 ) ) ;
#88054=CARTESIAN_POINT ( 'NONE',  ( 1.737499999999999378, -4.272916665710751793, -3.009438278150925683 ) ) ;
#88062=VERTEX_POINT ( 'NONE', #145254 ) ;
#88145=CARTESIAN_POINT ( 'NONE',  ( -3.285556943750000514, -3.638541666188706891, -1.896917185911906500 ) ) ;
#88180=CARTESIAN_POINT ( 'NONE',  ( -1.456858692995781412, -3.148926244281702314, 3.052706761563094950 ) ) ;
#88193=VERTEX_POINT ( 'NONE', #127996 ) ;
#88204=ADVANCED_FACE ( 'NONE', ( #62883 ), #157208, .T. ) ;
#88228=CIRCLE ( 'NONE', #171257, 2.500000000000000888 ) ;
#88263=VERTEX_POINT ( 'NONE', #190742 ) ;
#88437=EDGE_CURVE ( 'NONE', #6228, #74385, #137792, .T. ) ;
#88489=CARTESIAN_POINT ( 'NONE',  ( -3.285556943750000070, -1.596874999522043037, 0.000000000000000000 ) ) ;
#88555=CARTESIAN_POINT ( 'NONE',  ( 3.285556943750000070, -0.9843749995220412163, 0.000000000000000000 ) ) ;
#88618=CARTESIAN_POINT ( 'NONE',  ( 3.285556943750000070, -3.521874999522042859, 0.000000000000000000 ) ) ;
#88701=CARTESIAN_POINT ( 'NONE',  ( 2.912612998216587368, -0.9539908294626121554, 1.749314886574315331 ) ) ;
#88753=CIRCLE ( 'NONE', #102505, 11.00000000000000000 ) ;
#88762=EDGE_CURVE ( 'NONE', #7256, #135209, #40041, .T. ) ;
#88771=CARTESIAN_POINT ( 'NONE',  ( 3.285556943750000070, -0.2843749995220419269, 0.000000000000000000 ) ) ;
#88780=LINE ( 'NONE', #75713, #20147 ) ;
#88806=CARTESIAN_POINT ( 'NONE',  ( -3.474999999999998312, -1.020833333333332815, 2.006292185433951047 ) ) ;
#88976=CARTESIAN_POINT ( 'NONE',  ( -1.500000000000039524, 7.378742179571327497, -10.87908636427990139 ) ) ;
#88990=ORIENTED_EDGE ( 'NONE', *, *, #30234, .T. ) ;
#89074=VERTEX_POINT ( 'NONE', #139639 ) ;
#89081=CARTESIAN_POINT ( 'NONE',  ( 1.001543065824772753E-15, -2.559374999522041172, 3.793834371823811669 ) ) ;
#89140=CARTESIAN_POINT ( 'NONE',  ( -1.642778471875000035, -0.9552083328553742092, -2.845375778867859751 ) ) ;
#89229=CARTESIAN_POINT ( 'NONE',  ( 3.475000000000000533, -0.1458333333333326765, -2.006292185433951047 ) ) ;
#89345=ORIENTED_EDGE ( 'NONE', *, *, #94477, .F. ) ;
#89629=CARTESIAN_POINT ( 'NONE',  ( -3.285556943750000070, -0.8093749995220431703, 0.000000000000000000 ) ) ;
#89661=ORIENTED_EDGE ( 'NONE', *, *, #153552, .T. ) ;
#89692=CARTESIAN_POINT ( 'NONE',  ( 3.285556943749998737, -3.842708332855377051, -1.896917185911906500 ) ) ;
#89695=( BOUNDED_CURVE ( )  B_SPLINE_CURVE ( 2, ( #152303, #3878, #69950, #136062, #202075, #53735, #119866, #106803, #24404 ),
 .UNSPECIFIED., .F., .T. ) 
 B_SPLINE_CURVE_WITH_KNOTS ( ( 3, 2, 2, 2, 3 ),
 ( 0.2708333333333333703, 0.2777777777777777901, 0.2916666666666666852, 0.3055555555555555802, 0.3125000000000000000 ),
 .UNSPECIFIED. ) 
 CURVE ( )  GEOMETRIC_REPRESENTATION_ITEM ( )  RATIONAL_B_SPLINE_CURVE ( ( 0.9330127018922194093, 0.9330127018922196314, 1.000000000000000000, 0.8660254037844387076, 1.000000000000000000, 0.8660254037844387076, 1.000000000000000000, 0.9330127018922194093, 0.9330127018922194093 ) ) 
 REPRESENTATION_ITEM ( '' )  );
#89702=ORIENTED_EDGE ( 'NONE', *, *, #60337, .T. ) ;
#89781=CARTESIAN_POINT ( 'NONE',  ( 1.689998555091125843, -0.9101070431196979227, -2.859088409908076667 ) ) ;
#89881=CARTESIAN_POINT ( 'NONE',  ( 3.475000000000000533, -0.5541666666666681396, 2.006292185433948827 ) ) ;
#89993=ADVANCED_FACE ( 'NONE', ( #22379 ), #68994, .T. ) ;
#90007=DIRECTION ( 'NONE',  ( -0.000000000000000000, 1.000000000000000000, -0.000000000000000000 ) ) ;
#90021=ORIENTED_EDGE ( 'NONE', *, *, #53239, .F. ) ;
#90146=CARTESIAN_POINT ( 'NONE',  ( 3.285556943750000070, -2.121874999522044281, 0.000000000000000000 ) ) ;
#90205=CARTESIAN_POINT ( 'NONE',  ( 3.285556943750000070, -1.771874999522041083, 0.000000000000000000 ) ) ;
#90259=ORIENTED_EDGE ( 'NONE', *, *, #139074, .F. ) ;
#90265=DIRECTION ( 'NONE',  ( 3.491481338843133355E-15, 0.000000000000000000, 1.000000000000000000 ) ) ;
#90287=CARTESIAN_POINT ( 'NONE',  ( 1.737500000000001155, -0.2333333333333319215, 3.009438278150922130 ) ) ;
#90303=AXIS2_PLACEMENT_3D ( 'NONE', #68946, #150242, #118855 ) ;
#90349=( BOUNDED_CURVE ( )  B_SPLINE_CURVE ( 2, ( #208065, #75948, #122665, #23982, #74887, #204850, #8809, #56504, #205939 ),
 .UNSPECIFIED., .F., .T. ) 
 B_SPLINE_CURVE_WITH_KNOTS ( ( 3, 2, 2, 2, 3 ),
 ( 0.5208333333333333703, 0.5277777777777777901, 0.5416666666666666297, 0.5555555555555555802, 0.5625000000000000000 ),
 .UNSPECIFIED. ) 
 CURVE ( )  GEOMETRIC_REPRESENTATION_ITEM ( )  RATIONAL_B_SPLINE_CURVE ( ( 0.9330127018922192983, 0.9330127018922198534, 1.000000000000000000, 0.8660254037844387076, 1.000000000000000000, 0.8660254037844387076, 1.000000000000000000, 0.9330127018922194093, 0.9330127018922194093 ) ) 
 REPRESENTATION_ITEM ( '' )  );
#90376=CARTESIAN_POINT ( 'NONE',  ( 0.000000000000000000, -3.696874999522040017, -3.793834371823813001 ) ) ;
#90424=FACE_OUTER_BOUND ( 'NONE', #38454, .T. ) ;
#90454=CARTESIAN_POINT ( 'NONE',  ( 1.737499999999999378, -0.4229166657107527594, -3.009438278150925683 ) ) ;
#90504=DIRECTION ( 'NONE',  ( 0.000000000000000000, 0.000000000000000000, -1.000000000000000000 ) ) ;
#90535=DIRECTION ( 'NONE',  ( 0.000000000000000000, 0.000000000000000000, 1.000000000000000000 ) ) ;
#90557=DIRECTION ( 'NONE',  ( 0.000000000000000000, 1.000000000000000000, 0.000000000000000000 ) ) ;
#90632=CARTESIAN_POINT ( 'NONE',  ( 3.285556943749998737, -1.042708332855377451, -1.896917185911906722 ) ) ;
#90697=CARTESIAN_POINT ( 'NONE',  ( 1.001543065824772753E-15, -3.871874999522043836, 3.793834371823811669 ) ) ;
#90758=CARTESIAN_POINT ( 'NONE',  ( 0.000000000000000000, -0.1968749995220437643, -3.793834371823813001 ) ) ;
#90840=CARTESIAN_POINT ( 'NONE',  ( 3.028508906271001777, -0.9278780887907630559, -1.428417487556953525 ) ) ;
#90848=ADVANCED_FACE ( 'NONE', ( #181924 ), #43705, .F. ) ;
#90850=CARTESIAN_POINT ( 'NONE',  ( -2.324088772396477673E-16, -2.143749999044084031, -3.475000000000000089 ) ) ;
#90907=CARTESIAN_POINT ( 'NONE',  ( 3.285556943749998737, -0.2552083328553768071, -1.896917185911906500 ) ) ;
#90916=CARTESIAN_POINT ( 'NONE',  ( -1.499999999999946709, 7.750000000000000000, 15.75000000000000711 ) ) ;
#90943=CARTESIAN_POINT ( 'NONE',  ( -1.642778471875000035, -4.017708332855376874, -2.845375778867859751 ) ) ;
#91100=CARTESIAN_POINT ( 'NONE',  ( -3.420040343843560926, -0.02845264914099391793, -0.3063276076694415595 ) ) ;
#91115=CARTESIAN_POINT ( 'NONE',  ( -1.500000000000039524, 6.999999999999999112, -10.89724735885167739 ) ) ;
#91125=ORIENTED_EDGE ( 'NONE', *, *, #118482, .F. ) ;
#91171=EDGE_LOOP ( 'NONE', ( #52566, #200084, #176905, #202778 ) ) ;
#91185=CARTESIAN_POINT ( 'NONE',  ( 0.000000000000000000, -0.5000000000000004441, 0.000000000000000000 ) ) ;
#91219=CARTESIAN_POINT ( 'NONE',  ( 0.000000000000000000, -0.9843749995220403282, -3.793834371823813001 ) ) ;
#91227=CARTESIAN_POINT ( 'NONE',  ( 1.250000000000037526, 8.500000000000000000, 10.85702537530423406 ) ) ;
#91258=EDGE_CURVE ( 'NONE', #93052, #3985, #117328, .T. ) ;
#91279=CARTESIAN_POINT ( 'NONE',  ( 0.000000000000000000, -2.384374999522042238, -3.793834371823813001 ) ) ;
#91290=AXIS2_PLACEMENT_3D ( 'NONE', #174764, #105493, #72947 ) ;
#91368=CARTESIAN_POINT ( 'NONE',  ( 3.475000000000000533, -1.225000000000000311, 0.000000000000000000 ) ) ;
#91455=CARTESIAN_POINT ( 'NONE',  ( -3.474999999999998312, -1.720833333333333881, 2.006292185433951047 ) ) ;
#91634=FACE_BOUND ( 'NONE', #192858, .T. ) ;
#91769=CARTESIAN_POINT ( 'NONE',  ( 1.001543065824772753E-15, -2.821874999522044458, 3.793834371823811669 ) ) ;
#91832=CARTESIAN_POINT ( 'NONE',  ( -3.285556943750000070, -3.346874999522041261, 0.000000000000000000 ) ) ;
#91855=FACE_BOUND ( 'NONE', #129037, .T. ) ;
#91952=FACE_OUTER_BOUND ( 'NONE', #69195, .T. ) ;
#91981=CARTESIAN_POINT ( 'NONE',  ( -1.642778471875000035, -1.217708332855376607, -2.845375778867859751 ) ) ;
#91990=DIRECTION ( 'NONE',  ( -0.8660254037844397068, 0.4999999999999978906, 0.000000000000000000 ) ) ;
#92018=CARTESIAN_POINT ( 'NONE',  ( 3.475000000000000533, -0.5250000000000011324, 0.000000000000000000 ) ) ;
#92020=DIRECTION ( 'NONE',  ( 0.000000000000000000, -1.000000000000000000, 0.000000000000000000 ) ) ;
#92048=ORIENTED_EDGE ( 'NONE', *, *, #95890, .F. ) ;
#92054=DIRECTION ( 'NONE',  ( -0.000000000000000000, -1.000000000000000000, -0.000000000000000000 ) ) ;
#92234=ADVANCED_FACE ( 'NONE', ( #186984 ), #132938, .F. ) ;
#92299=CARTESIAN_POINT ( 'NONE',  ( -3.285556943750000070, -2.296874999522042327, 0.000000000000000000 ) ) ;
#92350=CARTESIAN_POINT ( 'NONE',  ( 0.000000000000000000, 12.31951671548121219, 0.000000000000000000 ) ) ;
#92355=CARTESIAN_POINT ( 'NONE',  ( 3.285556943750000070, -2.821874999522043570, 0.000000000000000000 ) ) ;
#92445=CARTESIAN_POINT ( 'NONE',  ( -1.737500000000000266, -1.458333333333332371, -3.009438278150923907 ) ) ;
#92478=CARTESIAN_POINT ( 'NONE',  ( 0.000000000000000000, -3.042800438942089514, 0.000000000000000000 ) ) ;
#92516=CARTESIAN_POINT ( 'NONE',  ( 1.001543065824772753E-15, -2.821874999522044458, 3.793834371823810780 ) ) ;
#92534=CARTESIAN_POINT ( 'NONE',  ( -1.737499999999997824, -2.391666666666667052, 3.009438278150925683 ) ) ;
#92604=CARTESIAN_POINT ( 'NONE',  ( 1.001543065824772753E-15, -0.5687499990440827435, 4.012584370867899430 ) ) ;
#92762=CARTESIAN_POINT ( 'NONE',  ( 0.000000000000000000, 0.06547992991065912372, 0.000000000000000000 ) ) ;
#92765=ORIENTED_EDGE ( 'NONE', *, *, #85587, .F. ) ;
#92768=CARTESIAN_POINT ( 'NONE',  ( 0.9311234436981512541, -1.853130369558481538, -3.475000000000000977 ) ) ;
#92827=EDGE_LOOP ( 'NONE', ( #146830, #197033, #190471, #130600 ) ) ;
#92833=CARTESIAN_POINT ( 'NONE',  ( 3.285556943750000514, -2.413541666188708579, 1.896917185911906500 ) ) ;
#92850=CARTESIAN_POINT ( 'NONE',  ( 1.499999999999959588, 7.064371086078063300, -10.89416074946470836 ) ) ;
#92865=VERTEX_POINT ( 'NONE', #11945 ) ;
#92896=CARTESIAN_POINT ( 'NONE',  ( -1.642778471874998480, -3.988541666188710089, 2.845375778867863303 ) ) ;
#92904=EDGE_LOOP ( 'NONE', ( #40239, #89661, #162516, #87359, #203533 ) ) ;
#92926=VECTOR ( 'NONE', #1269, 1000.000000000000000 ) ;
#92943=CARTESIAN_POINT ( 'NONE',  ( -1.737499999999997824, -1.647916665710749573, 3.009438278150925683 ) ) ;
#93044=CARTESIAN_POINT ( 'NONE',  ( -3.285556943750000070, -0.8093749995220431703, 0.000000000000000000 ) ) ;
#93052=VERTEX_POINT ( 'NONE', #3433 ) ;
#93053=AXIS2_PLACEMENT_3D ( 'NONE', #196238, #113994, #82468 ) ;
#93080=CARTESIAN_POINT ( 'NONE',  ( -3.475000000000000533, -2.129166666666665542, -2.006292185433948827 ) ) ;
#93216=AXIS2_PLACEMENT_3D ( 'NONE', #155491, #205284, #90504 ) ;
#93343=CARTESIAN_POINT ( 'NONE',  ( -1.642778471874998480, -0.4010416661887096224, 2.845375778867863303 ) ) ;
#93355=CARTESIAN_POINT ( 'NONE',  ( -3.285556943750000070, -0.1093749995220438809, 0.000000000000000000 ) ) ;
#93363=AXIS2_PLACEMENT_3D ( 'NONE', #72384, #135289, #101698 ) ;
#93411=CARTESIAN_POINT ( 'NONE',  ( -1.642778471874998480, -1.538541666188709245, 2.845375778867863303 ) ) ;
#93461=DIRECTION ( 'NONE',  ( -1.224646799147353454E-16, 0.000000000000000000, -1.000000000000000000 ) ) ;
#93466=CARTESIAN_POINT ( 'NONE',  ( 1.393942678861017637, 0.9000000000000014655, -1.636894562288534472 ) ) ;
#93502=CARTESIAN_POINT ( 'NONE',  ( 3.475000000000000533, -0.9041666666666666741, 2.006292185433948827 ) ) ;
#93573=CARTESIAN_POINT ( 'NONE',  ( 3.285556943750000514, -2.763541666188706891, 1.896917185911906722 ) ) ;
#93594=CARTESIAN_POINT ( 'NONE',  ( 3.475000000000000533, -2.274999999999999467, 0.000000000000000000 ) ) ;
#93624=ORIENTED_EDGE ( 'NONE', *, *, #198470, .T. ) ;
#93759=CARTESIAN_POINT ( 'NONE',  ( 0.000000000000000000, -0.02876672507444791305, 0.000000000000000000 ) ) ;
#93777=ADVANCED_FACE ( 'NONE', ( #15166 ), #84859, .T. ) ;
#93822=ADVANCED_FACE ( 'NONE', ( #28242 ), #176631, .T. ) ;
#93829=DIRECTION ( 'NONE',  ( -0.000000000000000000, -1.000000000000000000, -0.000000000000000000 ) ) ;
#93838=CARTESIAN_POINT ( 'NONE',  ( 0.000000000000000000, -2.734374999522040550, -3.793834371823813445 ) ) ;
#93841=AXIS2_PLACEMENT_3D ( 'NONE', #128165, #12174, #97723 ) ;
#93903=CARTESIAN_POINT ( 'NONE',  ( 1.642778471875000035, -2.326041666188709112, -2.845375778867859751 ) ) ;
#93957=ORIENTED_EDGE ( 'NONE', *, *, #129593, .T. ) ;
#93964=CARTESIAN_POINT ( 'NONE',  ( 3.285556943749998737, -1.305208332855376296, -1.896917185911906500 ) ) ;
#93974=EDGE_CURVE ( 'NONE', #204603, #7595, #205921, .T. ) ;
#94066=VERTEX_POINT ( 'NONE', #200309 ) ;
#94113=CARTESIAN_POINT ( 'NONE',  ( -1.642778471874998480, -1.451041666188708446, 2.845375778867863303 ) ) ;
#94150=CARTESIAN_POINT ( 'NONE',  ( 3.475000000000000533, -1.604166666666667629, 2.006292185433948827 ) ) ;
#94174=( BOUNDED_CURVE ( )  B_SPLINE_CURVE ( 2, ( #27165, #125828, #74866, #121562, #23958, #39163, #158261, #206979, #171287 ),
 .UNSPECIFIED., .F., .T. ) 
 B_SPLINE_CURVE_WITH_KNOTS ( ( 3, 2, 2, 2, 3 ),
 ( 0.4791666666666666852, 0.4861111111111111049, 0.5000000000000000000, 0.5138888888888888395, 0.5208333333333333703 ),
 .UNSPECIFIED. ) 
 CURVE ( )  GEOMETRIC_REPRESENTATION_ITEM ( )  RATIONAL_B_SPLINE_CURVE ( ( 0.9330127018922194093, 0.9330127018922196314, 1.000000000000000000, 0.8660254037844387076, 1.000000000000000000, 0.8660254037844387076, 1.000000000000000000, 0.9330127018922187432, 0.9330127018922192983 ) ) 
 REPRESENTATION_ITEM ( '' )  );
#94186=FACE_OUTER_BOUND ( 'NONE', #197922, .T. ) ;
#94187=DIRECTION ( 'NONE',  ( -0.000000000000000000, -1.000000000000000000, -0.000000000000000000 ) ) ;
#94208=DIRECTION ( 'NONE',  ( 0.000000000000000000, 0.000000000000000000, 1.000000000000000000 ) ) ;
#94212=CARTESIAN_POINT ( 'NONE',  ( 3.285556943750000514, -0.4010416661887095113, 1.896917185911906500 ) ) ;
#94296=VERTEX_POINT ( 'NONE', #144472 ) ;
#94333=AXIS2_PLACEMENT_3D ( 'NONE', #148694, #167078, #166003 ) ;
#94409=CARTESIAN_POINT ( 'NONE',  ( -1.642778471875000035, -1.217708332855376607, -2.845375778867859751 ) ) ;
#94477=EDGE_CURVE ( 'NONE', #88062, #56290, #175875, .T. ) ;
#94478=CARTESIAN_POINT ( 'NONE',  ( -1.642778471875000035, -2.355208332855376341, -2.845375778867859751 ) ) ;
#94543=AXIS2_PLACEMENT_3D ( 'NONE', #87298, #168547, #137127 ) ;
#94569=CARTESIAN_POINT ( 'NONE',  ( -3.474999999999998312, -1.020833333333332815, 2.006292185433951047 ) ) ;
#94661=CARTESIAN_POINT ( 'NONE',  ( -3.475000000000000533, -2.129166666666665542, -2.006292185433948827 ) ) ;
#94682=SURFACE_STYLE_USAGE ( .BOTH. , #43798 ) ;
#94733=CARTESIAN_POINT ( 'NONE',  ( -3.475000000000000533, -1.735416665710752371, -2.006292185433948827 ) ) ;
#94773=ORIENTED_EDGE ( 'NONE', *, *, #20473, .T. ) ;
#94778=ORIENTED_EDGE ( 'NONE', *, *, #153278, .F. ) ;
#94839=DIRECTION ( 'NONE',  ( 0.000000000000000000, 0.000000000000000000, 1.000000000000000000 ) ) ;
#94899=CARTESIAN_POINT ( 'NONE',  ( 1.642778471875000035, -3.113541666188709200, -2.845375778867859751 ) ) ;
#94956=VERTEX_POINT ( 'NONE', #43443 ) ;
#95025=CARTESIAN_POINT ( 'NONE',  ( 3.285556943749998737, -2.005208332855377140, -1.896917185911906500 ) ) ;
#95032=ORIENTED_EDGE ( 'NONE', *, *, #128454, .T. ) ;
#95039=EDGE_CURVE ( 'NONE', #22324, #3985, #98791, .T. ) ;
#95173=CARTESIAN_POINT ( 'NONE',  ( 1.001543065824772753E-15, -2.471874999522041705, 3.793834371823811669 ) ) ;
#95211=CARTESIAN_POINT ( 'NONE',  ( -3.474999999999998312, -2.770833333333333037, 2.006292185433951047 ) ) ;
#95216=CARTESIAN_POINT ( 'NONE',  ( 0.000000000000000000, 0.000000000000000000, 0.000000000000000000 ) ) ;
#95274=DIRECTION ( 'NONE',  ( 0.000000000000000000, 0.000000000000000000, -1.000000000000000000 ) ) ;
#95277=CARTESIAN_POINT ( 'NONE',  ( 0.000000000000000000, 5.000000000000000888, 0.000000000000000000 ) ) ;
#95281=CARTESIAN_POINT ( 'NONE',  ( -1.642778471875000035, -0.2552083328553750308, -2.845375778867859751 ) ) ;
#95282=CARTESIAN_POINT ( 'NONE',  ( -3.231971923028420957, -3.070585806845580024, 1.214571025355801304 ) ) ;
#95347=CARTESIAN_POINT ( 'NONE',  ( 1.416814887940403445, 7.999555336178682197, -9.899480522462175358 ) ) ;
#95426=CARTESIAN_POINT ( 'NONE',  ( -1.347971487989957070E-14, -3.018749999044084475, 3.475000000000000089 ) ) ;
#95484=CARTESIAN_POINT ( 'NONE',  ( -3.285556943750000514, -0.1385416661887106660, -1.896917185911906500 ) ) ;
#95494=DIRECTION ( 'NONE',  ( 1.000000000000000000, 0.000000000000000000, -3.491481338843133355E-15 ) ) ;
#95550=CARTESIAN_POINT ( 'NONE',  ( -3.285556943750000514, -3.726041666188710799, -1.896917185911906500 ) ) ;
#95646=CARTESIAN_POINT ( 'NONE',  ( 3.475000000000000533, -0.5541666666666681396, 2.006292185433948827 ) ) ;
#95713=CARTESIAN_POINT ( 'NONE',  ( 1.642778471875001811, -2.792708332855376785, 2.845375778867859751 ) ) ;
#95715=FACE_OUTER_BOUND ( 'NONE', #48237, .T. ) ;
#95732=CARTESIAN_POINT ( 'NONE',  ( 3.475000000000000533, -2.945833333333332416, -2.006292185433951047 ) ) ;
#95802=CARTESIAN_POINT ( 'NONE',  ( -1.737499999999997824, -2.347916665710752415, 3.009438278150925683 ) ) ;
#95860=CARTESIAN_POINT ( 'NONE',  ( -3.475000000000000533, -2.800000000000000266, 0.000000000000000000 ) ) ;
#95890=EDGE_CURVE ( 'NONE', #22324, #153466, #181937, .T. ) ;
#95892=CARTESIAN_POINT ( 'NONE',  ( 0.000000000000000000, -0.1968749995220437643, -3.793834371823813001 ) ) ;
#95971=CARTESIAN_POINT ( 'NONE',  ( -3.285556943750000070, -2.296874999522042327, 0.000000000000000000 ) ) ;
#95989=ORIENTED_EDGE ( 'NONE', *, *, #175486, .F. ) ;
#96020=AXIS2_PLACEMENT_3D ( 'NONE', #56449, #188572, #189637 ) ;
#96095=CARTESIAN_POINT ( 'NONE',  ( 1.642778471875001811, -1.742708332855374298, 2.845375778867859751 ) ) ;
#96117=CIRCLE ( 'NONE', #61596, 4.500000000000000000 ) ;
#96127=TOROIDAL_SURFACE ( 'NONE', #58059, 2.149999999999999911, 0.1000000000000000056 ) ;
#96239=CARTESIAN_POINT ( 'NONE',  ( 3.285556943750000070, -2.734374999522042771, 0.000000000000000000 ) ) ;
#96279=CARTESIAN_POINT ( 'NONE',  ( 3.475000000000000533, -1.225000000000000311, 0.000000000000000000 ) ) ;
#96284=( NAMED_UNIT ( * ) SI_UNIT ( $, .STERADIAN. ) SOLID_ANGLE_UNIT ( ) );
#96310=DIRECTION ( 'NONE',  ( -0.000000000000000000, -1.000000000000000000, -0.000000000000000000 ) ) ;
#96346=CARTESIAN_POINT ( 'NONE',  ( -3.112320638501687053, -3.098081249360057132, -1.430203574381059495 ) ) ;
#96471=AXIS2_PLACEMENT_3D ( 'NONE', #174163, #191428, #204466 ) ;
#96472=DIRECTION ( 'NONE',  ( 0.000000000000000000, -1.000000000000000000, 0.000000000000000000 ) ) ;
#96492=CARTESIAN_POINT ( 'NONE',  ( 0.000000000000000000, -3.517800438942085606, 0.000000000000000000 ) ) ;
#96730=DIRECTION ( 'NONE',  ( -0.6483454320283800199, 0.000000000000000000, 0.7613463080411787542 ) ) ;
#96736=ORIENTED_EDGE ( 'NONE', *, *, #99699, .T. ) ;
#96774=CIRCLE ( 'NONE', #93363, 3.150000000000000799 ) ;
#96800=CARTESIAN_POINT ( 'NONE',  ( -3.474999999999998312, -3.820833333333332416, 2.006292185433951047 ) ) ;
#96871=CARTESIAN_POINT ( 'NONE',  ( 3.475000000000000533, -2.902083332377417779, -2.006292185433951047 ) ) ;
#96996=DIRECTION ( 'NONE',  ( -0.6483454320283789096, 0.000000000000000000, 0.7613463080411795314 ) ) ;
#97055=ORIENTED_EDGE ( 'NONE', *, *, #73345, .T. ) ;
#97157=EDGE_LOOP ( 'NONE', ( #206117, #150568, #210240, #201106 ) ) ;
#97160=CARTESIAN_POINT ( 'NONE',  ( 1.001543065824772753E-15, -1.421874999522042327, 3.793834371823811669 ) ) ;
#97199=CYLINDRICAL_SURFACE ( 'NONE', #18051, 10.25000000000000000 ) ;
#97268=EDGE_CURVE ( 'NONE', #13166, #128202, #14358, .T. ) ;
#97297=FACE_OUTER_BOUND ( 'NONE', #5828, .T. ) ;
#97299=CARTESIAN_POINT ( 'NONE',  ( 1.642778471875000035, -2.676041666188708756, -2.845375778867859751 ) ) ;
#97318=PLANE ( 'NONE',  #196990 ) ;
#97340=CARTESIAN_POINT ( 'NONE',  ( 1.737499999999999378, -1.516666666666666163, -3.009438278150925683 ) ) ;
#97343=CARTESIAN_POINT ( 'NONE',  ( 3.285556943750000514, -0.3135416661887098777, 1.896917185911906500 ) ) ;
#97408=CARTESIAN_POINT ( 'NONE',  ( -1.642778471874998480, -0.8385416661887100664, 2.845375778867863303 ) ) ;
#97490=CARTESIAN_POINT ( 'NONE',  ( 0.000000000000000000, 2.999999999999999112, 0.000000000000000000 ) ) ;
#97582=EDGE_CURVE ( 'NONE', #42744, #211199, #112767, .T. ) ;
#97600=CARTESIAN_POINT ( 'NONE',  ( -3.285556943750000070, -0.4593749995220435256, 0.000000000000000000 ) ) ;
#97609=FACE_OUTER_BOUND ( 'NONE', #149725, .T. ) ;
#97684=CARTESIAN_POINT ( 'NONE',  ( 3.475000000000000533, -1.152083332377417335, -2.006292185433951047 ) ) ;
#97699=ORIENTED_EDGE ( 'NONE', *, *, #209026, .T. ) ;
#97723=DIRECTION ( 'NONE',  ( 0.000000000000000000, 0.000000000000000000, -1.000000000000000000 ) ) ;
#97734=ADVANCED_FACE ( 'NONE', ( #12230 ), #15423, .F. ) ;
#97740=CARTESIAN_POINT ( 'NONE',  ( 3.183171797643657097, -3.183434840866198545, -1.009552839968071325 ) ) ;
#97757=FACE_OUTER_BOUND ( 'NONE', #28476, .T. ) ;
#97767=CARTESIAN_POINT ( 'NONE',  ( -3.474999999999998312, -3.120833333333331350, 2.006292185433951047 ) ) ;
#97858=EDGE_CURVE ( 'NONE', #71477, #42744, #200565, .T. ) ;
#97930=CARTESIAN_POINT ( 'NONE',  ( 0.000000000000000000, -2.843749999044084653, -4.012584370867899430 ) ) ;
#98020=CARTESIAN_POINT ( 'NONE',  ( -3.285556943750000070, -1.159374999522042815, 0.000000000000000000 ) ) ;
#98183=DIRECTION ( 'NONE',  ( 1.000000000000000000, 0.000000000000000000, 1.224646799147353207E-16 ) ) ;
#98218=CARTESIAN_POINT ( 'NONE',  ( -1.642778471874998480, -1.451041666188708446, 2.845375778867863303 ) ) ;
#98348=CARTESIAN_POINT ( 'NONE',  ( 3.285556943750000514, -1.713541666188707735, 1.896917185911906500 ) ) ;
#98389=CARTESIAN_POINT ( 'NONE',  ( 3.475000000000000533, -3.004166666666665542, 2.006292185433948827 ) ) ;
#98391=CARTESIAN_POINT ( 'NONE',  ( -1.642778471875000035, -4.105208332855374564, -2.845375778867859751 ) ) ;
#98456=CARTESIAN_POINT ( 'NONE',  ( -3.285556943750000514, -0.2260416661887102996, -1.896917185911906500 ) ) ;
#98482=EDGE_CURVE ( 'NONE', #174327, #31992, #26402, .T. ) ;
#98511=CARTESIAN_POINT ( 'NONE',  ( -1.496707356397872557, -0.8887487162373141070, -2.932808216565309767 ) ) ;
#98593=CIRCLE ( 'NONE', #109016, 9.999999999999996447 ) ;
#98652=CARTESIAN_POINT ( 'NONE',  ( 0.000000000000000000, -2.996874999522043392, -3.793834371823813001 ) ) ;
#98733=ORIENTED_EDGE ( 'NONE', *, *, #64021, .F. ) ;
#98743=DIRECTION ( 'NONE',  ( -0.000000000000000000, -1.000000000000000000, -0.000000000000000000 ) ) ;
#98791=CIRCLE ( 'NONE', #50381, 0.4999999999999995559 ) ;
#98809=CARTESIAN_POINT ( 'NONE',  ( -3.423460510979340121, -0.02136329652385748901, -0.4189541688200317804 ) ) ;
#98823=CARTESIAN_POINT ( 'NONE',  ( -1.737500000000000266, -3.558333333333333570, -3.009438278150923907 ) ) ;
#98910=CARTESIAN_POINT ( 'NONE',  ( 1.737499999999999378, -3.966666666666666785, -3.009438278150925683 ) ) ;
#98925=DIRECTION ( 'NONE',  ( 2.345077562848777574E-16, -0.000000000000000000, 1.000000000000000000 ) ) ;
#98966=VECTOR ( 'NONE', #98925, 1000.000000000000000 ) ;
#98982=CARTESIAN_POINT ( 'NONE',  ( -1.737500000000000266, -3.164583332377419289, -3.009438278150923907 ) ) ;
#99071=CARTESIAN_POINT ( 'NONE',  ( -1.642778471874998480, -1.101041666188708801, 2.845375778867863303 ) ) ;
#99204=VECTOR ( 'NONE', #192160, 1000.000000000000000 ) ;
#99259=CIRCLE ( 'NONE', #5817, 9.999999999999998224 ) ;
#99277=CARTESIAN_POINT ( 'NONE',  ( 1.642778471875000035, -3.376041666188708046, -2.845375778867859751 ) ) ;
#99315=DIRECTION ( 'NONE',  ( 0.000000000000000000, 1.000000000000000000, 0.000000000000000000 ) ) ;
#99418=CARTESIAN_POINT ( 'NONE',  ( 3.285556943750000070, -3.434374999522042060, 0.000000000000000000 ) ) ;
#99430=DIRECTION ( 'NONE',  ( -3.491481338843133750E-15, -0.000000000000000000, -1.000000000000000000 ) ) ;
#99460=CARTESIAN_POINT ( 'NONE',  ( 3.285556943750000070, -3.171874999522043215, 0.000000000000000000 ) ) ;
#99524=CARTESIAN_POINT ( 'NONE',  ( 3.285556943750000070, -1.421874999522041660, 0.000000000000000000 ) ) ;
#99627=DIRECTION ( 'NONE',  ( -0.000000000000000000, 1.000000000000000000, -0.000000000000000000 ) ) ;
#99661=CARTESIAN_POINT ( 'NONE',  ( 1.737499999999999378, -2.566666666666668650, -3.009438278150925683 ) ) ;
#99699=EDGE_CURVE ( 'NONE', #25653, #108029, #175315, .T. ) ;
#99709=CARTESIAN_POINT ( 'NONE',  ( -3.285556943749998737, -3.230208332855375897, 1.896917185911908499 ) ) ;
#99879=CARTESIAN_POINT ( 'NONE',  ( 0.000000000000000000, -3.237499999999997602, -4.012584370867899430 ) ) ;
#99907=ORIENTED_EDGE ( 'NONE', *, *, #38982, .F. ) ;
#100002=CARTESIAN_POINT ( 'NONE',  ( 1.642778471875000035, -0.9260416661887073131, -2.845375778867859751 ) ) ;
#100038=CARTESIAN_POINT ( 'NONE',  ( 1.737499999999999378, -2.872916665710750106, -3.009438278150925683 ) ) ;
#100071=ORIENTED_EDGE ( 'NONE', *, *, #168924, .T. ) ;
#100123=CARTESIAN_POINT ( 'NONE',  ( -3.285556943750000514, -2.588541666188707513, -1.896917185911906500 ) ) ;
#100303=CARTESIAN_POINT ( 'NONE',  ( -3.285556943750000070, -0.1112512837626866702, 0.000000000000000000 ) ) ;
#100325=CARTESIAN_POINT ( 'NONE',  ( -1.642778471875000035, -3.667708332855373676, -2.845375778867859751 ) ) ;
#100355=AXIS2_PLACEMENT_3D ( 'NONE', #144734, #194500, #46145 ) ;
#100459=CARTESIAN_POINT ( 'NONE',  ( 1.718115394875207702, -1.600000000000000755, -2.017567716309123682 ) ) ;
#100465=ORIENTED_EDGE ( 'NONE', *, *, #97582, .T. ) ;
#100471=CARTESIAN_POINT ( 'NONE',  ( 1.001543065824772753E-15, -3.871874999522043836, 3.793834371823811669 ) ) ;
#100517=CARTESIAN_POINT ( 'NONE',  ( 1.642778471875000035, -3.813541666188708490, -2.845375778867859751 ) ) ;
#100554=DIRECTION ( 'NONE',  ( 0.000000000000000000, -1.000000000000000000, 0.000000000000000000 ) ) ;
#100582=CARTESIAN_POINT ( 'NONE',  ( 3.285556943750000070, -2.821874999522043570, 0.000000000000000000 ) ) ;
#100765=CARTESIAN_POINT ( 'NONE',  ( -3.285556943749998737, -2.530208332855374831, 1.896917185911908499 ) ) ;
#100768=ORIENTED_EDGE ( 'NONE', *, *, #108161, .T. ) ;
#100771=DIRECTION ( 'NONE',  ( -0.000000000000000000, -1.000000000000000000, -0.000000000000000000 ) ) ;
#100918=CARTESIAN_POINT ( 'NONE',  ( -3.433841370118181580, -0.01667935949903331938, -0.3944899663380890265 ) ) ;
#100927=CARTESIAN_POINT ( 'NONE',  ( 1.737499999999999378, -3.966666666666666785, -3.009438278150925683 ) ) ;
#101010=( BOUNDED_CURVE ( )  B_SPLINE_CURVE ( 2, ( #121, #31609, #66188, #97684, #117170, #198339, #64103, #116097, #18529 ),
 .UNSPECIFIED., .F., .T. ) 
 B_SPLINE_CURVE_WITH_KNOTS ( ( 3, 2, 2, 2, 3 ),
 ( 0.1875000000000000000, 0.1944444444444444475, 0.2083333333333333426, 0.2222222222222222099, 0.2291666666666666574 ),
 .UNSPECIFIED. ) 
 CURVE ( )  GEOMETRIC_REPRESENTATION_ITEM ( )  RATIONAL_B_SPLINE_CURVE ( ( 0.9330127018922194093, 0.9330127018922194093, 1.000000000000000000, 0.8660254037844387076, 1.000000000000000000, 0.8660254037844387076, 1.000000000000000000, 0.9330127018922194093, 0.9330127018922194093 ) ) 
 REPRESENTATION_ITEM ( '' )  );
#101022=ORIENTED_EDGE ( 'NONE', *, *, #182167, .T. ) ;
#101029=CARTESIAN_POINT ( 'NONE',  ( 3.285556943750000070, -0.7218749995220423710, 0.000000000000000000 ) ) ;
#101055=CARTESIAN_POINT ( 'NONE',  ( -3.285556943750000514, -1.888541666188711110, -1.896917185911906722 ) ) ;
#101088=CARTESIAN_POINT ( 'NONE',  ( 0.000000000000000000, -0.9843749995220403282, -3.793834371823813001 ) ) ;
#101128=ORIENTED_EDGE ( 'NONE', *, *, #71473, .F. ) ;
#101177=CARTESIAN_POINT ( 'NONE',  ( 1.642778471875000035, -1.626041666188710044, -2.845375778867859751 ) ) ;
#101213=VECTOR ( 'NONE', #77852, 1000.000000000000000 ) ;
#101255=CARTESIAN_POINT ( 'NONE',  ( -1.081945585493433448, -0.9830613892718149671, 3.305300248233959515 ) ) ;
#101274=VERTEX_POINT ( 'NONE', #44701 ) ;
#101389=CARTESIAN_POINT ( 'NONE',  ( 1.642778471875000035, -2.676041666188708756, -2.845375778867859751 ) ) ;
#101460=VECTOR ( 'NONE', #135222, 1000.000000000000000 ) ;
#101544=CARTESIAN_POINT ( 'NONE',  ( 1.642778471875000035, -3.376041666188708046, -2.845375778867859751 ) ) ;
#101584=CARTESIAN_POINT ( 'NONE',  ( 1.737500000000001155, -3.733333333333331616, 3.009438278150922130 ) ) ;
#101586=CARTESIAN_POINT ( 'NONE',  ( 0.000000000000000000, -1.596874999522041705, -3.793834371823813001 ) ) ;
#101650=CARTESIAN_POINT ( 'NONE',  ( -1.642778471875000035, -2.005208332855376696, -2.845375778867859751 ) ) ;
#101698=DIRECTION ( 'NONE',  ( 0.000000000000000000, 0.000000000000000000, 1.000000000000000000 ) ) ;
#101792=FACE_OUTER_BOUND ( 'NONE', #159593, .T. ) ;
#101798=ORIENTED_EDGE ( 'NONE', *, *, #125041, .F. ) ;
#101840=CARTESIAN_POINT ( 'NONE',  ( -3.285556943750000514, -2.588541666188707513, -1.896917185911906500 ) ) ;
#101883=CARTESIAN_POINT ( 'NONE',  ( -0.9311234436981514762, -2.128119629485601738, -3.474999999999999645 ) ) ;
#101902=ADVANCED_FACE ( 'NONE', ( #16369 ), #49962, .T. ) ;
#101919=EDGE_LOOP ( 'NONE', ( #197709, #38911, #189222, #106315 ) ) ;
#101972=CARTESIAN_POINT ( 'NONE',  ( 1.734723475976807094E-15, -7.105553651663779391, 0.000000000000000000 ) ) ;
#101983=DIRECTION ( 'NONE',  ( 0.000000000000000000, -1.000000000000000000, 0.000000000000000000 ) ) ;
#101995=CARTESIAN_POINT ( 'NONE',  ( -3.422577805355617730, -0.02192484962740117241, -0.4179650480824659842 ) ) ;
#101996=CARTESIAN_POINT ( 'NONE',  ( -1.499999999999960476, 7.378742179571331938, 10.87908636427991205 ) ) ;
#102033=DIRECTION ( 'NONE',  ( -0.000000000000000000, 1.000000000000000000, 0.000000000000000000 ) ) ;
#102047=CARTESIAN_POINT ( 'NONE',  ( 1.500000000000039524, 7.564371094685074404, 10.87018506808106899 ) ) ;
#102079=PLANE ( 'NONE',  #129600 ) ;
#102133=CARTESIAN_POINT ( 'NONE',  ( 1.001543065824772753E-15, -1.421874999522042549, 3.793834371823810780 ) ) ;
#102169=CARTESIAN_POINT ( 'NONE',  ( -3.285556943750000514, -1.276041666188709511, -1.896917185911906500 ) ) ;
#102253=CARTESIAN_POINT ( 'NONE',  ( 1.642778471875001811, -1.392708332855374653, 2.845375778867859751 ) ) ;
#102320=AXIS2_PLACEMENT_3D ( 'NONE', #163844, #127149, #96730 ) ;
#102459=CARTESIAN_POINT ( 'NONE',  ( 0.000000000000000000, -4.046874999522043659, -3.793834371823813001 ) ) ;
#102473=CARTESIAN_POINT ( 'NONE',  ( 0.000000000000000000, 0.5000000000000004441, -3.475000000000000089 ) ) ;
#102505=AXIS2_PLACEMENT_3D ( 'NONE', #156968, #20536, #4268 ) ;
#102593=CARTESIAN_POINT ( 'NONE',  ( -3.285556943750000514, -1.626041666188708046, -1.896917185911906722 ) ) ;
#102597=AXIS2_PLACEMENT_3D ( 'NONE', #163962, #129406, #145613 ) ;
#102619=CARTESIAN_POINT ( 'NONE',  ( -3.475000000000000533, -0.7291666666666675178, -2.006292185433948827 ) ) ;
#102642=EDGE_CURVE ( 'NONE', #94956, #135209, #145114, .T. ) ;
#102661=CARTESIAN_POINT ( 'NONE',  ( 3.285556943750000514, -0.6635416661887083567, 1.896917185911906500 ) ) ;
#102718=EDGE_CURVE ( 'NONE', #187973, #104308, #85609, .T. ) ;
#102723=CARTESIAN_POINT ( 'NONE',  ( 3.285556943750000514, -2.151041666188709733, 1.896917185911906500 ) ) ;
#102765=DIRECTION ( 'NONE',  ( 0.000000000000000000, -1.000000000000000000, 0.000000000000000000 ) ) ;
#102907=CARTESIAN_POINT ( 'NONE',  ( 0.000000000000000000, -2.646874999522040639, -3.793834371823813001 ) ) ;
#102939=ORIENTED_EDGE ( 'NONE', *, *, #66694, .F. ) ;
#102958=VERTEX_POINT ( 'NONE', #80067 ) ;
#103056=FACE_OUTER_BOUND ( 'NONE', #111065, .T. ) ;
#103134=ORIENTED_EDGE ( 'NONE', *, *, #151508, .T. ) ;
#103143=DIRECTION ( 'NONE',  ( 0.000000000000000000, 1.000000000000000000, 0.000000000000000000 ) ) ;
#103176=ORIENTED_EDGE ( 'NONE', *, *, #189245, .F. ) ;
#103205=CARTESIAN_POINT ( 'NONE',  ( -1.642778471875000035, -2.267708332855375541, -2.845375778867859751 ) ) ;
#103241=CARTESIAN_POINT ( 'NONE',  ( 1.642778471875000035, -0.6635416661887084677, -2.845375778867859751 ) ) ;
#103326=CARTESIAN_POINT ( 'NONE',  ( 1.737499999999999378, -0.4666666666666673402, -3.009438278150925683 ) ) ;
#103372=EDGE_CURVE ( 'NONE', #82008, #24990, #37226, .T. ) ;
#103500=AXIS2_PLACEMENT_3D ( 'NONE', #117090, #100771, #69315 ) ;
#103565=AXIS2_PLACEMENT_3D ( 'NONE', #192355, #12541, #44012 ) ;
#103614=ORIENTED_EDGE ( 'NONE', *, *, #124593, .T. ) ;
#103670=CARTESIAN_POINT ( 'NONE',  ( -3.285556943749998737, -1.217708332855376607, 1.896917185911908721 ) ) ;
#103675=EDGE_CURVE ( 'NONE', #24541, #153164, #44975, .T. ) ;
#103692=CARTESIAN_POINT ( 'NONE',  ( -1.642778471875000035, -4.017708332855376874, -2.845375778867859751 ) ) ;
#103733=CARTESIAN_POINT ( 'NONE',  ( -3.285556943749998737, -1.130208332855377140, 1.896917185911908499 ) ) ;
#103796=CARTESIAN_POINT ( 'NONE',  ( 1.642778471875000035, -2.063541666188710266, -2.845375778867859751 ) ) ;
#103890=CARTESIAN_POINT ( 'NONE',  ( 0.000000000000000000, 8.500000000000000000, 0.000000000000000000 ) ) ;
#103930=EDGE_CURVE ( 'NONE', #31992, #56290, #121398, .T. ) ;
#103933=CARTESIAN_POINT ( 'NONE',  ( -2.324088772396477673E-16, -2.143749999044084031, -3.475000000000000089 ) ) ;
#103985=CARTESIAN_POINT ( 'NONE',  ( 3.285556943750000070, -3.784374999522041705, 0.000000000000000000 ) ) ;
#104016=CARTESIAN_POINT ( 'NONE',  ( 1.499999999999959588, 6.999999999999999112, -10.89724735885168805 ) ) ;
#104063=VECTOR ( 'NONE', #117796, 1000.000000000000000 ) ;
#104169=DIRECTION ( 'NONE',  ( 0.000000000000000000, 0.000000000000000000, 1.000000000000000000 ) ) ;
#104254=CARTESIAN_POINT ( 'NONE',  ( 1.642778471875000035, -1.713541666188707291, -2.845375778867859751 ) ) ;
#104279=CARTESIAN_POINT ( 'NONE',  ( 3.285556943749998737, -1.655208332855374609, -1.896917185911906722 ) ) ;
#104308=VERTEX_POINT ( 'NONE', #8722 ) ;
#104310=CARTESIAN_POINT ( 'NONE',  ( 1.001543065824772753E-15, -4.068749999044083410, 4.012584370867899430 ) ) ;
#104371=CARTESIAN_POINT ( 'NONE',  ( 1.249999999999961142, 8.500000000000000000, -10.85702537530424472 ) ) ;
#104372=EDGE_LOOP ( 'NONE', ( #85701, #155889 ) ) ;
#104400=CARTESIAN_POINT ( 'NONE',  ( 1.642778471875000035, -3.376041666188708046, -2.845375778867859751 ) ) ;
#104611=ORIENTED_EDGE ( 'NONE', *, *, #198277, .T. ) ;
#104624=AXIS2_PLACEMENT_3D ( 'NONE', #153490, #169727, #20264 ) ;
#104740=CARTESIAN_POINT ( 'NONE',  ( 1.642778471875000035, -1.363541666188707646, -2.845375778867859751 ) ) ;
#104809=CARTESIAN_POINT ( 'NONE',  ( -3.285556943750000070, -1.159374999522042815, 0.000000000000000000 ) ) ;
#104868=CARTESIAN_POINT ( 'NONE',  ( 1.642778471875000035, -3.813541666188708490, -2.845375778867859751 ) ) ;
#104890=B_SPLINE_CURVE_WITH_KNOTS ( 'NONE', 3,
 ( #81136, #64877, #193806, #147222, #213246, #161330, #145110, #45455, #95282, #128900, #28119, #178649, #111571, #208977, #126773, #177579, #160253, #96346, #192731, #194881, #44385, #46517, #12914, #112640, #30260, #110507, #162401, #176507, #212042, #126638, #46383, #77799 ),
 .UNSPECIFIED., .F., .F.,
 ( 4, 2, 2, 2, 2, 2, 2, 2, 2, 2, 2, 2, 2, 2, 2, 4 ),
 ( 2.873115300368997076E-17, 0.001171507007196520090, 0.001757260510794765715, 0.002343014014393011990, 0.002928767517991258482, 0.003514521021589504975, 0.004100274525187751901, 0.004686028028785998827, 0.005271781532384244885, 0.005857535035982492679, 0.006443288539580738737, 0.007029042043178984796, 0.007614795546777232589, 0.008200549050375479515, 0.008786302553973725574, 0.009372056057571971632 ),
 .UNSPECIFIED. ) ;
#105025=CARTESIAN_POINT ( 'NONE',  ( -1.642778471875000035, -0.8677083328553769626, -2.845375778867859751 ) ) ;
#105064=CARTESIAN_POINT ( 'NONE',  ( -1.737499999999997824, -0.9916666666666684726, 3.009438278150925683 ) ) ;
#105066=CARTESIAN_POINT ( 'NONE',  ( 0.000000000000000000, 5.999999999999998224, 0.000000000000000000 ) ) ;
#105069=CARTESIAN_POINT ( 'NONE',  ( 1.737499999999999378, -1.166666666666666519, -3.009438278150925683 ) ) ;
#105184=DIRECTION ( 'NONE',  ( -0.000000000000000000, -1.000000000000000000, -0.000000000000000000 ) ) ;
#105255=EDGE_LOOP ( 'NONE', ( #85746, #117314 ) ) ;
#105329=CIRCLE ( 'NONE', #167602, 10.25000000000000000 ) ;
#105336=CARTESIAN_POINT ( 'NONE',  ( -3.285556943749998737, -0.8677083328553740760, 1.896917185911908499 ) ) ;
#105397=CARTESIAN_POINT ( 'NONE',  ( -1.642778471875000035, -0.2552083328553750308, -2.845375778867859751 ) ) ;
#105420=CARTESIAN_POINT ( 'NONE',  ( -1.159304781898771619, -3.232243495192086424, 3.077805119331097572 ) ) ;
#105486=CARTESIAN_POINT ( 'NONE',  ( -1.737500000000000266, -0.05833333333333384774, -3.009438278150923907 ) ) ;
#105493=DIRECTION ( 'NONE',  ( -0.000000000000000000, -1.000000000000000000, -0.000000000000000000 ) ) ;
#105574=CARTESIAN_POINT ( 'NONE',  ( -1.347971487989957070E-14, -2.712500000000000355, 3.475000000000000089 ) ) ;
#105737=CIRCLE ( 'NONE', #129899, 3.150000000000000799 ) ;
#105795=ORIENTED_EDGE ( 'NONE', *, *, #86135, .T. ) ;
#105796=AXIS2_PLACEMENT_3D ( 'NONE', #81594, #183357, #182279 ) ;
#105828=EDGE_LOOP ( 'NONE', ( #47917, #197164, #167685, #21026 ) ) ;
#105832=CARTESIAN_POINT ( 'NONE',  ( 1.642778471875000035, -1.713541666188707291, -2.845375778867859751 ) ) ;
#105903=CARTESIAN_POINT ( 'NONE',  ( -1.642778471875000035, -0.5177083328553738761, -2.845375778867859751 ) ) ;
#105964=VECTOR ( 'NONE', #122484, 1000.000000000000000 ) ;
#105966=FACE_OUTER_BOUND ( 'NONE', #186162, .T. ) ;
#105968=ORIENTED_EDGE ( 'NONE', *, *, #144738, .T. ) ;
#105971=CARTESIAN_POINT ( 'NONE',  ( 1.642778471875001811, -3.580208332855376430, 2.845375778867859751 ) ) ;
#106047=ORIENTED_EDGE ( 'NONE', *, *, #199503, .F. ) ;
#106049=CIRCLE ( 'NONE', #206333, 11.00000000000000000 ) ;
#106095=EDGE_LOOP ( 'NONE', ( #208194, #36482, #197459 ) ) ;
#106125=CARTESIAN_POINT ( 'NONE',  ( 3.285556943749998737, -0.9552083328553737651, -1.896917185911906500 ) ) ;
#106160=CARTESIAN_POINT ( 'NONE',  ( -1.737500000000000266, -0.4083333333333334370, -3.009438278150923907 ) ) ;
#106192=EDGE_LOOP ( 'NONE', ( #167904, #14241, #211233, #107286 ) ) ;
#106315=ORIENTED_EDGE ( 'NONE', *, *, #206779, .T. ) ;
#106412=CARTESIAN_POINT ( 'NONE',  ( 1.394453263437886604E-15, -2.362500000000000266, 3.474999999999999645 ) ) ;
#106433=CARTESIAN_POINT ( 'NONE',  ( 3.285556943749998737, -1.392708332855375764, -1.896917185911906500 ) ) ;
#106490=CARTESIAN_POINT ( 'NONE',  ( -3.285556943750000514, -3.026041666188709733, -1.896917185911906500 ) ) ;
#106501=CIRCLE ( 'NONE', #196431, 4.500000000000000000 ) ;
#106558=AXIS2_PLACEMENT_3D ( 'NONE', #214401, #132179, #64986 ) ;
#106576=LINE ( 'NONE', #4714, #80609 ) ;
#106577=ORIENTED_EDGE ( 'NONE', *, *, #42175, .T. ) ;
#106578=DIRECTION ( 'NONE',  ( -0.000000000000000000, 1.000000000000000000, -0.000000000000000000 ) ) ;
#106579=CARTESIAN_POINT ( 'NONE',  ( 1.001543065824772753E-15, -3.521874999522041083, 3.793834371823811669 ) ) ;
#106593=VECTOR ( 'NONE', #102765, 1000.000000000000000 ) ;
#106621=EDGE_CURVE ( 'NONE', #40241, #5998, #163080, .T. ) ;
#106628=ORIENTED_EDGE ( 'NONE', *, *, #52227, .T. ) ;
#106742=CARTESIAN_POINT ( 'NONE',  ( -1.737499999999997824, -0.5979166657107508609, 3.009438278150925683 ) ) ;
#106803=CARTESIAN_POINT ( 'NONE',  ( 0.9311234436981525864, -1.603119629485603825, 3.474999999999998757 ) ) ;
#106853=TOROIDAL_SURFACE ( 'NONE', #93053, 3.599999999999999201, 0.4999999999999998890 ) ;
#106920=CARTESIAN_POINT ( 'NONE',  ( 3.285556943750000070, -1.421874999522041660, 0.000000000000000000 ) ) ;
#106947=DIRECTION ( 'NONE',  ( 8.659560562354967371E-17, 0.7071067811865445751, -0.7071067811865504593 ) ) ;
#106984=CARTESIAN_POINT ( 'NONE',  ( 3.285556943749998737, -3.755208332855373587, -1.896917185911906500 ) ) ;
#107043=CARTESIAN_POINT ( 'NONE',  ( 0.000000000000000000, -4.134374999522041350, -3.793834371823813001 ) ) ;
#107080=ADVANCED_FACE ( 'NONE', ( #163750 ), #149621, .T. ) ;
#107125=ORIENTED_EDGE ( 'NONE', *, *, #170395, .T. ) ;
#107130=ORIENTED_EDGE ( 'NONE', *, *, #206779, .F. ) ;
#107201=CARTESIAN_POINT ( 'NONE',  ( 1.001543065824772753E-15, -0.3718749995220430038, 3.793834371823811669 ) ) ;
#107230=ADVANCED_FACE ( 'NONE', ( #132340 ), #185296, .T. ) ;
#107242=CARTESIAN_POINT ( 'NONE',  ( 3.475000000000000533, -0.4958333333333350690, -2.006292185433951047 ) ) ;
#107286=ORIENTED_EDGE ( 'NONE', *, *, #52227, .F. ) ;
#107324=EDGE_LOOP ( 'NONE', ( #43640, #213094 ) ) ;
#107462=CYLINDRICAL_SURFACE ( 'NONE', #141537, 10.25000000000000000 ) ;
#107513=CARTESIAN_POINT ( 'NONE',  ( 1.642778471875000035, -2.063541666188710266, -2.845375778867859751 ) ) ;
#107561=DIRECTION ( 'NONE',  ( 0.6483454320283789096, 0.000000000000000000, -0.7613463080411795314 ) ) ;
#107571=CARTESIAN_POINT ( 'NONE',  ( 3.285556943749998737, -2.092708332855377051, -1.896917185911906500 ) ) ;
#107663=CARTESIAN_POINT ( 'NONE',  ( 0.000000000000000000, -0.4374999999999981126, -4.012584370867899430 ) ) ;
#107683=LINE ( 'NONE', #123956, #81842 ) ;
#107754=CARTESIAN_POINT ( 'NONE',  ( -1.737499999999997824, -1.341666666666668117, 3.009438278150925683 ) ) ;
#107826=CARTESIAN_POINT ( 'NONE',  ( 3.475000000000000533, -0.8312499990440826991, 0.000000000000000000 ) ) ;
#107848=AXIS2_PLACEMENT_3D ( 'NONE', #186492, #173482, #119433 ) ;
#107877=FACE_OUTER_BOUND ( 'NONE', #189745, .T. ) ;
#107993=VERTEX_POINT ( 'NONE', #141894 ) ;
#107995=CARTESIAN_POINT ( 'NONE',  ( 3.475000000000000533, -2.260416665710749839, 2.006292185433948827 ) ) ;
#108029=VERTEX_POINT ( 'NONE', #174377 ) ;
#108062=CARTESIAN_POINT ( 'NONE',  ( 3.285556943749998737, -3.405208332855374831, -1.896917185911906500 ) ) ;
#108123=CARTESIAN_POINT ( 'NONE',  ( -1.642778471874998480, -3.288541666188707246, 2.845375778867863303 ) ) ;
#108161=EDGE_CURVE ( 'NONE', #153466, #22324, #25652, .T. ) ;
#108275=CARTESIAN_POINT ( 'NONE',  ( 3.285556943750000070, -0.6343749995220415716, 0.000000000000000000 ) ) ;
#108312=CARTESIAN_POINT ( 'NONE',  ( 1.642778471875001811, -3.492708332855375630, 2.845375778867859751 ) ) ;
#108496=CARTESIAN_POINT ( 'NONE',  ( -6.042630808230841359E-15, -2.318749999044084298, 3.474999999999999645 ) ) ;
#108502=EDGE_LOOP ( 'NONE', ( #30455, #211498 ) ) ;
#108532=FACE_OUTER_BOUND ( 'NONE', #149068, .T. ) ;
#108555=CIRCLE ( 'NONE', #35805, 0.09999999999999999167 ) ;
#108580=CARTESIAN_POINT ( 'NONE',  ( 0.000000000000000000, -1.334374999522042859, -3.793834371823813001 ) ) ;
#108599=ORIENTED_EDGE ( 'NONE', *, *, #142758, .F. ) ;
#108636=CARTESIAN_POINT ( 'NONE',  ( -1.642778471874998480, -1.888541666188708890, 2.845375778867863303 ) ) ;
#108651=FACE_OUTER_BOUND ( 'NONE', #2803, .T. ) ;
#108730=CARTESIAN_POINT ( 'NONE',  ( 1.737500000000001155, -2.333333333333333037, 3.009438278150922130 ) ) ;
#108769=ORIENTED_EDGE ( 'NONE', *, *, #199503, .T. ) ;
#108802=CARTESIAN_POINT ( 'NONE',  ( -1.642778471875000035, -2.617708332855375186, -2.845375778867859751 ) ) ;
#108820=CARTESIAN_POINT ( 'NONE',  ( -3.475000000000000533, -2.479166666666667851, -2.006292185433948827 ) ) ;
#109014=ORIENTED_EDGE ( 'NONE', *, *, #41171, .F. ) ;
#109016=AXIS2_PLACEMENT_3D ( 'NONE', #85859, #71715, #137828 ) ;
#109063=ADVANCED_FACE ( 'NONE', ( #11629 ), #112178, .F. ) ;
#109065=CARTESIAN_POINT ( 'NONE',  ( 1.001543065824772753E-15, -2.559374999522041172, 3.793834371823810780 ) ) ;
#109112=ADVANCED_FACE ( 'NONE', ( #91855, #46294 ), #144886, .T. ) ;
#109132=CARTESIAN_POINT ( 'NONE',  ( -3.285556943750000514, -3.288541666188709023, -1.896917185911906500 ) ) ;
#109149=CARTESIAN_POINT ( 'NONE',  ( 1.499999999999959588, 7.193113254731348327, -10.88798745763944353 ) ) ;
#109197=CARTESIAN_POINT ( 'NONE',  ( 0.000000000000000000, -0.5468749995220422155, -3.793834371823813001 ) ) ;
#109246=CARTESIAN_POINT ( 'NONE',  ( -0.9311234436981496998, -1.634380368602566636, 3.475000000000000977 ) ) ;
#109293=FACE_OUTER_BOUND ( 'NONE', #205359, .T. ) ;
#109316=DIRECTION ( 'NONE',  ( 0.000000000000000000, -1.000000000000000000, -0.000000000000000000 ) ) ;
#109354=DIRECTION ( 'NONE',  ( 0.3162277660168376636, 0.9486832980505138790, 0.000000000000000000 ) ) ;
#109382=CARTESIAN_POINT ( 'NONE',  ( 1.737499999999999378, -1.166666666666666519, -3.009438278150925683 ) ) ;
#109650=ORIENTED_EDGE ( 'NONE', *, *, #29015, .F. ) ;
#109659=CARTESIAN_POINT ( 'NONE',  ( -3.285556943750000514, -3.726041666188710799, -1.896917185911906500 ) ) ;
#109704=CARTESIAN_POINT ( 'NONE',  ( -1.499999999999946709, 7.750000000000000000, 15.75000000000000711 ) ) ;
#109708=ORIENTED_EDGE ( 'NONE', *, *, #32460, .F. ) ;
#109710=CARTESIAN_POINT ( 'NONE',  ( 3.285556943749998737, -3.142708332855375986, -1.896917185911906500 ) ) ;
#109780=ADVANCED_FACE ( 'NONE', ( #73159 ), #180846, .T. ) ;
#109802=CARTESIAN_POINT ( 'NONE',  ( 1.737499999999999378, -1.866666666666665808, -3.009438278150925683 ) ) ;
#109823=CARTESIAN_POINT ( 'NONE',  ( 1.734723475976807094E-15, -7.105553651663779391, 0.000000000000000000 ) ) ;
#109872=CARTESIAN_POINT ( 'NONE',  ( 1.642778471875000035, -3.026041666188708401, -2.845375778867859751 ) ) ;
#109890=CARTESIAN_POINT ( 'NONE',  ( 1.001543065824772753E-15, -2.012499999999999289, 4.012584370867899430 ) ) ;
#109904=EDGE_CURVE ( 'NONE', #111991, #36461, #89695, .T. ) ;
#109964=CARTESIAN_POINT ( 'NONE',  ( -1.737500000000000266, -0.7145833323774185564, -3.009438278150923907 ) ) ;
#110048=FACE_OUTER_BOUND ( 'NONE', #208598, .T. ) ;
#110054=DIRECTION ( 'NONE',  ( -0.6483454320283799088, 0.000000000000000000, 0.7613463080411786432 ) ) ;
#110087=AXIS2_PLACEMENT_3D ( 'NONE', #157258, #143174, #61875 ) ;
#110090=DIRECTION ( 'NONE',  ( 0.000000000000000000, 1.000000000000000000, 0.000000000000000000 ) ) ;
#110114=ORIENTED_EDGE ( 'NONE', *, *, #211811, .F. ) ;
#110132=CARTESIAN_POINT ( 'NONE',  ( -3.285556943750000070, -2.996874999522041616, 0.000000000000000000 ) ) ;
#110157=ADVANCED_FACE ( 'NONE', ( #74259 ), #59791, .F. ) ;
#110194=CARTESIAN_POINT ( 'NONE',  ( 1.642778471875001811, -2.792708332855376785, 2.845375778867859751 ) ) ;
#110257=CARTESIAN_POINT ( 'NONE',  ( 1.001543065824772753E-15, -0.7218749995220414828, 3.793834371823811669 ) ) ;
#110263=DIRECTION ( 'NONE',  ( 0.000000000000000000, 0.000000000000000000, 1.000000000000000000 ) ) ;
#110279=CARTESIAN_POINT ( 'NONE',  ( 0.000000000000000000, 1.000000000000000888, 0.000000000000000000 ) ) ;
#110330=CIRCLE ( 'NONE', #13316, 0.1000000000000000333 ) ;
#110405=CARTESIAN_POINT ( 'NONE',  ( -1.642778471874998480, -2.151041666188707957, 2.845375778867863303 ) ) ;
#110443=CARTESIAN_POINT ( 'NONE',  ( -3.475000000000000533, -2.829166666666666607, -2.006292185433948827 ) ) ;
#110446=CARTESIAN_POINT ( 'NONE',  ( 0.000000000000000000, 0.5000000000000004441, 0.000000000000000000 ) ) ;
#110507=CARTESIAN_POINT ( 'NONE',  ( -1.501780004532949908, -3.122141865171504271, -3.051664013761996141 ) ) ;
#110540=VERTEX_POINT ( 'NONE', #165903 ) ;
#110567=DIRECTION ( 'NONE',  ( 0.000000000000000000, -0.000000000000000000, -1.000000000000000000 ) ) ;
#110685=DIRECTION ( 'NONE',  ( 0.000000000000000000, 0.000000000000000000, 1.000000000000000000 ) ) ;
#110700=CARTESIAN_POINT ( 'NONE',  ( 1.642778471875000035, -1.276041666188710400, -2.845375778867859751 ) ) ;
#110734=DIRECTION ( 'NONE',  ( 0.000000000000000000, 1.000000000000000000, 0.000000000000000000 ) ) ;
#110742=CONICAL_SURFACE ( 'NONE', #162486, 10.92874649719719571, 0.04746665426984499059 ) ;
#110768=CARTESIAN_POINT ( 'NONE',  ( 3.285556943750000514, -1.451041666188708890, 1.896917185911906500 ) ) ;
#110860=CARTESIAN_POINT ( 'NONE',  ( 3.475000000000000533, -1.954166666666666163, 2.006292185433948827 ) ) ;
#110935=DIRECTION ( 'NONE',  ( -0.6483454320283799088, 0.000000000000000000, 0.7613463080411786432 ) ) ;
#110950=CARTESIAN_POINT ( 'NONE',  ( 3.475000000000000533, -1.225000000000000311, 0.000000000000000000 ) ) ;
#111024=CARTESIAN_POINT ( 'NONE',  ( 3.475000000000000533, -1.560416665710748996, 2.006292185433948827 ) ) ;
#111058=LINE ( 'NONE', #13481, #69805 ) ;
#111065=EDGE_LOOP ( 'NONE', ( #145193, #34101, #28938, #40514 ) ) ;
#111080=FACE_OUTER_BOUND ( 'NONE', #118880, .T. ) ;
#111082=CARTESIAN_POINT ( 'NONE',  ( -3.475000000000000533, -2.829166666666666163, -2.006292185433948827 ) ) ;
#111111=CARTESIAN_POINT ( 'NONE',  ( 0.000000000000000000, -0.5468749995220422155, -3.793834371823813001 ) ) ;
#111147=ORIENTED_EDGE ( 'NONE', *, *, #129564, .T. ) ;
#111155=CARTESIAN_POINT ( 'NONE',  ( 0.000000000000000000, 5.999999999999998224, -11.00000000000000000 ) ) ;
#111196=CARTESIAN_POINT ( 'NONE',  ( -1.642778471874998480, -2.238541666188708312, 2.845375778867863303 ) ) ;
#111260=CARTESIAN_POINT ( 'NONE',  ( -3.285556943750000514, -2.588541666188707513, -1.896917185911906500 ) ) ;
#111323=CARTESIAN_POINT ( 'NONE',  ( 3.285556943750000514, -1.713541666188707735, 1.896917185911906500 ) ) ;
#111387=AXIS2_PLACEMENT_3D ( 'NONE', #164308, #99315, #84112 ) ;
#111454=CARTESIAN_POINT ( 'NONE',  ( 1.734723475976807094E-15, 2.499999999999998668, 0.000000000000000000 ) ) ;
#111463=ORIENTED_EDGE ( 'NONE', *, *, #25018, .F. ) ;
#111469=CARTESIAN_POINT ( 'NONE',  ( -3.285556943749998737, -1.480208332855375453, 1.896917185911908499 ) ) ;
#111491=EDGE_CURVE ( 'NONE', #82008, #55892, #141842, .T. ) ;
#111506=CARTESIAN_POINT ( 'NONE',  ( -1.737500000000000266, -2.158333333333331439, -3.009438278150923907 ) ) ;
#111510=SURFACE_SIDE_STYLE ('',( #114709 ) ) ;
#111571=CARTESIAN_POINT ( 'NONE',  ( -3.440154425158069795, -3.082311296064041528, 0.07384894924763349411 ) ) ;
#111768=CARTESIAN_POINT ( 'NONE',  ( 1.642778471875000035, -0.2260416661887081069, -2.845375778867859751 ) ) ;
#111939=CARTESIAN_POINT ( 'NONE',  ( 0.000000000000000000, -1.487500000000001599, -4.012584370867899430 ) ) ;
#111955=CARTESIAN_POINT ( 'NONE',  ( -2.550000000000000266, 2.499999999999998668, -1.849324200890692271 ) ) ;
#111991=VERTEX_POINT ( 'NONE', #112557 ) ;
#112027=CARTESIAN_POINT ( 'NONE',  ( 1.737500000000001155, -1.983333333333333393, 3.009438278150922130 ) ) ;
#112101=CARTESIAN_POINT ( 'NONE',  ( -1.737500000000000266, -2.114583332377416802, -3.009438278150923907 ) ) ;
#112178=TOROIDAL_SURFACE ( 'NONE', #202037, 2.649999999999999911, 0.1000000000000000056 ) ;
#112210=ORIENTED_EDGE ( 'NONE', *, *, #2302, .T. ) ;
#112217=EDGE_CURVE ( 'NONE', #108029, #121330, #198294, .T. ) ;
#112260=CARTESIAN_POINT ( 'NONE',  ( 1.458777222063855739, 0.9000000000000014655, -1.713029193092652225 ) ) ;
#112263=CARTESIAN_POINT ( 'NONE',  ( 1.642778471875001811, -3.230208332855373676, 2.845375778867859751 ) ) ;
#112281=ORIENTED_EDGE ( 'NONE', *, *, #179232, .T. ) ;
#112323=DIRECTION ( 'NONE',  ( 0.000000000000000000, 1.000000000000000000, 0.000000000000000000 ) ) ;
#112376=CARTESIAN_POINT ( 'NONE',  ( 1.394453263437886604E-15, -2.668749999044085275, 3.474999999999999645 ) ) ;
#112387=CARTESIAN_POINT ( 'NONE',  ( -3.285556943749998737, -1.480208332855375453, 1.896917185911908499 ) ) ;
#112396=ADVANCED_FACE ( 'NONE', ( #168706 ), #21362, .T. ) ;
#112486=EDGE_LOOP ( 'NONE', ( #178247, #40594, #214035, #95032 ) ) ;
#112527=CARTESIAN_POINT ( 'NONE',  ( 3.285556943750000514, -2.413541666188708579, 1.896917185911906500 ) ) ;
#112557=CARTESIAN_POINT ( 'NONE',  ( 7.204675194429079505E-15, -1.443749999044083854, -3.475000000000000089 ) ) ;
#112570=CARTESIAN_POINT ( 'NONE',  ( -3.475000000000000533, -2.800000000000000266, 0.000000000000000000 ) ) ;
#112639=CARTESIAN_POINT ( 'NONE',  ( 0.000000000000000000, -0.2843749995220433702, -3.793834371823813001 ) ) ;
#112640=CARTESIAN_POINT ( 'NONE',  ( -2.004536931766795593, -3.116556058128074902, -2.754590913354557635 ) ) ;
#112694=CARTESIAN_POINT ( 'NONE',  ( -3.241630445535677918, -0.8887487162373168825, -0.5775286854858272534 ) ) ;
#112698=FACE_OUTER_BOUND ( 'NONE', #108502, .T. ) ;
#112700=CARTESIAN_POINT ( 'NONE',  ( 1.499999999999963141, 7.750000000000000000, -9.886859966642596476 ) ) ;
#112767=CIRCLE ( 'NONE', #102320, 2.250000000000000444 ) ;
#112833=CARTESIAN_POINT ( 'NONE',  ( 3.285556943750000514, -1.013541666188710888, 1.896917185911906500 ) ) ;
#112963=CARTESIAN_POINT ( 'NONE',  ( -1.737499999999997824, -1.691666666666667762, 3.009438278150925683 ) ) ;
#113001=CARTESIAN_POINT ( 'NONE',  ( -1.737499999999997824, -2.741666666666666696, 3.009438278150925683 ) ) ;
#113054=EDGE_LOOP ( 'NONE', ( #101128, #145510 ) ) ;
#113089=CARTESIAN_POINT ( 'NONE',  ( 3.475000000000000533, -3.645833333333333037, -2.006292185433951047 ) ) ;
#113160=EDGE_LOOP ( 'NONE', ( #203905, #59749, #25009 ) ) ;
#113164=CARTESIAN_POINT ( 'NONE',  ( 1.001543065824772753E-15, -2.668749999044085719, 4.012584370867899430 ) ) ;
#113295=DIRECTION ( 'NONE',  ( -2.345077562848777574E-16, -0.000000000000000000, -1.000000000000000000 ) ) ;
#113307=CIRCLE ( 'NONE', #182328, 0.4999999999999995559 ) ;
#113311=VERTEX_POINT ( 'NONE', #105574 ) ;
#113388=EDGE_LOOP ( 'NONE', ( #74240, #200269 ) ) ;
#113446=CARTESIAN_POINT ( 'NONE',  ( -0.9311234436981496998, -2.684380368602567568, 3.475000000000000977 ) ) ;
#113458=CARTESIAN_POINT ( 'NONE',  ( -3.285556943749998737, -2.180208332855376518, 1.896917185911908499 ) ) ;
#113497=FACE_OUTER_BOUND ( 'NONE', #73372, .T. ) ;
#113521=EDGE_CURVE ( 'NONE', #94066, #187973, #18333, .T. ) ;
#113535=LINE ( 'NONE', #14870, #40862 ) ;
#113601=CARTESIAN_POINT ( 'NONE',  ( -3.285556943750000514, -1.888541666188711110, -1.896917185911906500 ) ) ;
#113641=CARTESIAN_POINT ( 'NONE',  ( -3.474999999999998312, -1.720833333333333881, 2.006292185433951047 ) ) ;
#113643=CARTESIAN_POINT ( 'NONE',  ( 3.285556943749998737, -0.2552083328553768071, -1.896917185911906500 ) ) ;
#113715=DIRECTION ( 'NONE',  ( -0.000000000000000000, -1.000000000000000000, -0.000000000000000000 ) ) ;
#113717=ORIENTED_EDGE ( 'NONE', *, *, #142095, .T. ) ;
#113872=EDGE_LOOP ( 'NONE', ( #159386, #164266, #111463, #10119, #36712 ) ) ;
#113908=CARTESIAN_POINT ( 'NONE',  ( 3.285556943750000514, -0.3135416661887098777, 1.896917185911906500 ) ) ;
#113915=CARTESIAN_POINT ( 'NONE',  ( 0.000000000000000000, 1.000000000000000888, 0.000000000000000000 ) ) ;
#113985=AXIS2_PLACEMENT_3D ( 'NONE', #3619, #134752, #18816 ) ;
#113994=DIRECTION ( 'NONE',  ( -0.000000000000000000, 1.000000000000000000, -0.000000000000000000 ) ) ;
#114006=ORIENTED_EDGE ( 'NONE', *, *, #102642, .F. ) ;
#114028=ORIENTED_EDGE ( 'NONE', *, *, #106621, .F. ) ;
#114047=CARTESIAN_POINT ( 'NONE',  ( 2.978798704061872193, -3.177366733903203233, -1.522944741273397407 ) ) ;
#114056=ORIENTED_EDGE ( 'NONE', *, *, #21279, .T. ) ;
#114065=CARTESIAN_POINT ( 'NONE',  ( -3.425644128314343728, -0.02016143452187105223, -0.4179710227418531598 ) ) ;
#114074=CARTESIAN_POINT ( 'NONE',  ( -3.285556943750000070, -0.1112512837626866702, 0.000000000000000000 ) ) ;
#114077=CARTESIAN_POINT ( 'NONE',  ( 3.475000000000000533, -3.004166666666665542, 2.006292185433948827 ) ) ;
#114098=VERTEX_POINT ( 'NONE', #157265 ) ;
#114163=CARTESIAN_POINT ( 'NONE',  ( 0.000000000000000000, -2.887499999999999289, -4.012584370867899430 ) ) ;
#114233=CARTESIAN_POINT ( 'NONE',  ( 1.737500000000001155, -1.939583332377418978, 3.009438278150922130 ) ) ;
#114281=B_SPLINE_CURVE_WITH_KNOTS ( 'NONE', 3,
 ( #185658, #154251, #122913, #9059, #58878, #88180, #7976, #207251, #125034, #157464 ),
 .UNSPECIFIED., .F., .F.,
 ( 4, 2, 2, 2, 4 ),
 ( 0.000000000000000000, 0.0009122422346014731880, 0.001824484469202946376, 0.002736726703804419347, 0.003648968938405892752 ),
 .UNSPECIFIED. ) ;
#114318=CARTESIAN_POINT ( 'NONE',  ( 1.001543065824772753E-15, -2.471874999522041705, 3.793834371823811669 ) ) ;
#114453=CARTESIAN_POINT ( 'NONE',  ( 0.000000000000000000, 5.999999999999998224, -10.25000000000000000 ) ) ;
#114522=CARTESIAN_POINT ( 'NONE',  ( -3.285556943750000070, -1.159374999522042815, 0.000000000000000000 ) ) ;
#114544=CIRCLE ( 'NONE', #21042, 4.500000000000000000 ) ;
#114623=AXIS2_PLACEMENT_3D ( 'NONE', #73228, #110090, #62337 ) ;
#114664=CARTESIAN_POINT ( 'NONE',  ( -3.285556943750000070, -1.859374999522041882, 0.000000000000000000 ) ) ;
#114702=CARTESIAN_POINT ( 'NONE',  ( -3.474999999999998312, -3.470833333333334103, 2.006292185433951047 ) ) ;
#114704=CARTESIAN_POINT ( 'NONE',  ( -1.642778471874998480, -3.988541666188710089, 2.845375778867863303 ) ) ;
#114709=SURFACE_STYLE_FILL_AREA ( #193747 ) ;
#114753=ADVANCED_FACE ( 'NONE', ( #192931 ), #128361, .T. ) ;
#114783=DIRECTION ( 'NONE',  ( -0.000000000000000000, 1.000000000000000000, -0.000000000000000000 ) ) ;
#114792=TOROIDAL_SURFACE ( 'NONE', #183828, 3.399419719642636561, 0.1000000000000000056 ) ;
#114817=CARTESIAN_POINT ( 'NONE',  ( -2.511332776996739291, -0.8887487162373162164, -2.129472066838233868 ) ) ;
#114909=CARTESIAN_POINT ( 'NONE',  ( 3.475000000000000533, -2.654166666666667229, 2.006292185433948827 ) ) ;
#114953=CARTESIAN_POINT ( 'NONE',  ( 3.285556943750000070, -1.334374999522040861, 0.000000000000000000 ) ) ;
#114961=CYLINDRICAL_SURFACE ( 'NONE', #68834, 2.250000000000000444 ) ;
#114985=ORIENTED_EDGE ( 'NONE', *, *, #170070, .F. ) ;
#115098=CARTESIAN_POINT ( 'NONE',  ( 3.271045316616016940, -3.187365041801710763, -0.6525704249654357136 ) ) ;
#115115=CARTESIAN_POINT ( 'NONE',  ( -3.423866110619523173, -0.02112260055291484417, -0.4190911324384871683 ) ) ;
#115125=CARTESIAN_POINT ( 'NONE',  ( -3.475000000000000533, -3.529166666666667229, -2.006292185433948827 ) ) ;
#115175=ADVANCED_FACE ( 'NONE', ( #176734, #16329 ), #161564, .T. ) ;
#115221=ORIENTED_EDGE ( 'NONE', *, *, #19306, .T. ) ;
#115287=CARTESIAN_POINT ( 'NONE',  ( -3.474999999999998312, -2.027083332377417779, 2.006292185433951047 ) ) ;
#115376=CARTESIAN_POINT ( 'NONE',  ( 1.642778471875001811, -1.042708332855375009, 2.845375778867859751 ) ) ;
#115534=CARTESIAN_POINT ( 'NONE',  ( -3.410126044457033156, -0.03745499569612897872, 0.000000000000000000 ) ) ;
#115570=CARTESIAN_POINT ( 'NONE',  ( -1.642778471875000035, -4.017708332855376874, -2.845375778867859751 ) ) ;
#115593=ORIENTED_EDGE ( 'NONE', *, *, #167712, .F. ) ;
#115716=CARTESIAN_POINT ( 'NONE',  ( -3.475000000000000533, 0.000000000000000000, 0.000000000000000000 ) ) ;
#115758=CARTESIAN_POINT ( 'NONE',  ( 1.642778471875001811, -3.930208332855376074, 2.845375778867859751 ) ) ;
#115795=UNCERTAINTY_MEASURE_WITH_UNIT (LENGTH_MEASURE( 1.000000000000000082E-05 ), #164460, 'distance_accuracy_value', 'NONE');
#115805=TOROIDAL_SURFACE ( 'NONE', #205567, 3.599999999999999201, 0.4999999999999998890 ) ;
#115828=CARTESIAN_POINT ( 'NONE',  ( 1.001543065824772753E-15, -1.159374999522043481, 3.793834371823811669 ) ) ;
#115844=DIRECTION ( 'NONE',  ( 0.000000000000000000, 0.000000000000000000, 1.000000000000000000 ) ) ;
#115971=CARTESIAN_POINT ( 'NONE',  ( 3.475000000000000533, -2.624999999999998668, 0.000000000000000000 ) ) ;
#116019=CARTESIAN_POINT ( 'NONE',  ( 3.285556943749998737, -2.005208332855377140, -1.896917185911906500 ) ) ;
#116039=CARTESIAN_POINT ( 'NONE',  ( 1.394453263437886604E-15, -2.362500000000000266, 3.474999999999999645 ) ) ;
#116072=DIRECTION ( 'NONE',  ( -0.000000000000000000, -1.000000000000000000, -0.000000000000000000 ) ) ;
#116097=CARTESIAN_POINT ( 'NONE',  ( 0.9311234436981525864, -1.253119629485603070, 3.474999999999998757 ) ) ;
#116173=CARTESIAN_POINT ( 'NONE',  ( -3.451466477441916147, -0.01064274562824485404, -0.2975466414532820791 ) ) ;
#116184=AXIS2_PLACEMENT_3D ( 'NONE', #76333, #62225, #42798 ) ;
#116186=CARTESIAN_POINT ( 'NONE',  ( -1.737499999999997824, -3.091666666666666341, 3.009438278150925683 ) ) ;
#116234=EDGE_CURVE ( 'NONE', #63041, #197916, #198602, .T. ) ;
#116275=CARTESIAN_POINT ( 'NONE',  ( -3.475000000000000533, -2.829166666666666607, -2.006292185433948827 ) ) ;
#116343=CARTESIAN_POINT ( 'NONE',  ( 1.001543065824772753E-15, -3.718749999044085097, 4.012584370867899430 ) ) ;
#116406=CARTESIAN_POINT ( 'NONE',  ( -1.288108131580338211, -0.9841229182759280159, 3.227445187970915619 ) ) ;
#116430=CARTESIAN_POINT ( 'NONE',  ( 1.001543065824772753E-15, -1.071874999522043792, 3.793834371823811669 ) ) ;
#116557=AXIS2_PLACEMENT_3D ( 'NONE', #171475, #149905, #186650 ) ;
#116566=CARTESIAN_POINT ( 'NONE',  ( 2.520460663003311730, -4.091624451297095177, -2.338645729556988240 ) ) ;
#116635=CARTESIAN_POINT ( 'NONE',  ( 1.642778471875000035, -3.026041666188708401, -2.845375778867859751 ) ) ;
#116784=CARTESIAN_POINT ( 'NONE',  ( -1.737499999999997824, -0.2916666666666657415, 3.009438278150925683 ) ) ;
#116824=CARTESIAN_POINT ( 'NONE',  ( 3.475000000000000533, -3.675000000000001155, 0.000000000000000000 ) ) ;
#116826=CARTESIAN_POINT ( 'NONE',  ( -3.285556943750000514, -3.026041666188709733, -1.896917185911906500 ) ) ;
#116893=CARTESIAN_POINT ( 'NONE',  ( 1.642778471875001811, -2.530208332855374387, 2.845375778867859751 ) ) ;
#116895=CARTESIAN_POINT ( 'NONE',  ( 1.737500000000001155, -1.939583332377418978, 3.009438278150922130 ) ) ;
#116920=VECTOR ( 'NONE', #144180, 1000.000000000000227 ) ;
#116946=CARTESIAN_POINT ( 'NONE',  ( -0.8870621307506136866, -0.8887487162373149951, -3.171027839057565689 ) ) ;
#117056=CARTESIAN_POINT ( 'NONE',  ( 1.523611765266693174, 0.5000000000000001110, -1.789163823896770200 ) ) ;
#117058=CARTESIAN_POINT ( 'NONE',  ( -3.327716440918550234, -0.9205823139102755626, 0.1123605076546999176 ) ) ;
#117085=CARTESIAN_POINT ( 'NONE',  ( 3.285556943750000514, -2.413541666188708579, 1.896917185911906500 ) ) ;
#117090=CARTESIAN_POINT ( 'NONE',  ( 0.000000000000000000, 0.4000000000000010214, 0.000000000000000000 ) ) ;
#117170=CARTESIAN_POINT ( 'NONE',  ( 3.475000000000000533, -1.181249999044085897, 0.000000000000000000 ) ) ;
#117224=CARTESIAN_POINT ( 'NONE',  ( 2.890748560597784955, -3.175295894664973417, -1.688109688813533626 ) ) ;
#117239=CARTESIAN_POINT ( 'NONE',  ( -3.425394108783801794, -0.02028796577872097814, -0.4182871798345951797 ) ) ;
#117250=CARTESIAN_POINT ( 'NONE',  ( -3.474999999999998312, -3.820833333333332416, 2.006292185433951047 ) ) ;
#117314=ORIENTED_EDGE ( 'NONE', *, *, #86107, .F. ) ;
#117328=B_SPLINE_CURVE_WITH_KNOTS ( 'NONE', 3,
 ( #5262, #35656, #167804, #85482, #37803, #4203, #71338, #137455, #203470, #55124, #38871, #88701, #154760, #6344, #188307, #141748, #72416, #176342, #138517, #90840, #156903, #42094, #157974, #173158, #9564, #89781, #204541, #140677, #8491, #73494 ),
 .UNSPECIFIED., .F., .F.,
 ( 4, 2, 2, 2, 2, 2, 2, 2, 2, 2, 2, 2, 2, 2, 4 ),
 ( 0.001318931363626723533, 0.001984147519712246236, 0.002649363675797769373, 0.003314579831883291642, 0.003979795987968814779, 0.004645012144054337482, 0.005310228300139859317, 0.005975444456225382020, 0.006640660612310906458, 0.007971092924481951864, 0.008636309080567474566, 0.009301525236652995535, 0.009966741392738518238, 0.01063195754882404094, 0.01196238986099508982 ),
 .UNSPECIFIED. ) ;
#117344=CARTESIAN_POINT ( 'NONE',  ( -3.475000000000000533, -3.179166666666664476, -2.006292185433948827 ) ) ;
#117416=CARTESIAN_POINT ( 'NONE',  ( 0.000000000000000000, -0.6343749995220417937, -3.793834371823813001 ) ) ;
#117480=CARTESIAN_POINT ( 'NONE',  ( 7.204675194429079505E-15, -1.137499999999999512, -3.475000000000000089 ) ) ;
#117505=CARTESIAN_POINT ( 'NONE',  ( -3.285556943750000514, -1.188541666188710044, -1.896917185911906500 ) ) ;
#117585=EDGE_CURVE ( 'NONE', #5998, #6228, #164320, .T. ) ;
#117633=FACE_OUTER_BOUND ( 'NONE', #75300, .T. ) ;
#117650=ADVANCED_FACE ( 'NONE', ( #180137, #71684 ), #102079, .F. ) ;
#117714=CARTESIAN_POINT ( 'NONE',  ( -1.642778471875000035, -2.617708332855375186, -2.845375778867859751 ) ) ;
#117796=DIRECTION ( 'NONE',  ( -0.000000000000000000, 1.000000000000000000, -0.000000000000000000 ) ) ;
#117862=CARTESIAN_POINT ( 'NONE',  ( -1.737499999999997824, -0.6416666666666653862, 3.009438278150925683 ) ) ;
#117885=ORIENTED_EDGE ( 'NONE', *, *, #200871, .T. ) ;
#117902=CARTESIAN_POINT ( 'NONE',  ( 1.001543065824772753E-15, -3.062499999999998668, 4.012584370867899430 ) ) ;
#117904=CARTESIAN_POINT ( 'NONE',  ( 1.001543065824772753E-15, -0.7218749995220414828, 3.793834371823811669 ) ) ;
#117965=CARTESIAN_POINT ( 'NONE',  ( -3.285556943749998737, -1.917708332855377673, 1.896917185911908499 ) ) ;
#117984=CARTESIAN_POINT ( 'NONE',  ( 3.975693637526477975E-16, -3.499999999999999556, -3.017800438942085606 ) ) ;
#118046=CIRCLE ( 'NONE', #83328, 10.25000000000000000 ) ;
#118073=LINE ( 'NONE', #151588, #146067 ) ;
#118085=PRODUCT_DEFINITION_FORMATION_WITH_SPECIFIED_SOURCE ( 'ANY', '', #176864, .NOT_KNOWN. ) ;
#118126=CARTESIAN_POINT ( 'NONE',  ( -2.324088772396477673E-16, -2.887500000000000178, -3.475000000000000089 ) ) ;
#118128=CARTESIAN_POINT ( 'NONE',  ( -3.363224415809069612, -0.9755303453303005856, 0.7941732810802911713 ) ) ;
#118157=CARTESIAN_POINT ( 'NONE',  ( 0.000000000000000000, -2.296874999522042327, -3.793834371823813001 ) ) ;
#118259=ADVANCED_FACE ( 'NONE', ( #78107 ), #115805, .F. ) ;
#118307=CARTESIAN_POINT ( 'NONE',  ( -3.423586633568784787, -0.02128689224817647760, -0.4190252743465633922 ) ) ;
#118335=ORIENTED_EDGE ( 'NONE', *, *, #59714, .F. ) ;
#118359=FACE_OUTER_BOUND ( 'NONE', #112486, .T. ) ;
#118449=CARTESIAN_POINT ( 'NONE',  ( 1.642778471875000035, -2.326041666188709112, -2.845375778867859751 ) ) ;
#118482=EDGE_CURVE ( 'NONE', #187007, #153475, #123760, .T. ) ;
#118484=CARTESIAN_POINT ( 'NONE',  ( -3.285556943750000514, -0.9260416661887070910, -1.896917185911906500 ) ) ;
#118507=CARTESIAN_POINT ( 'NONE',  ( 3.475000000000000533, -1.604166666666667629, 2.006292185433948827 ) ) ;
#118518=EDGE_CURVE ( 'NONE', #35390, #130778, #10959, .T. ) ;
#118570=CARTESIAN_POINT ( 'NONE',  ( 0.000000000000000000, -1.246874999522042948, -3.793834371823813001 ) ) ;
#118614=CIRCLE ( 'NONE', #84073, 11.00000000000000000 ) ;
#118628=VERTEX_POINT ( 'NONE', #57601 ) ;
#118682=DIRECTION ( 'NONE',  ( -1.000000000000000000, 0.000000000000000000, 3.491481338843133355E-15 ) ) ;
#118723=DIRECTION ( 'NONE',  ( -1.000000000000000000, 0.000000000000000000, 0.000000000000000000 ) ) ;
#118769=CARTESIAN_POINT ( 'NONE',  ( -3.285556943750000514, -3.638541666188706891, -1.896917185911906500 ) ) ;
#118770=AXIS2_PLACEMENT_3D ( 'NONE', #69927, #136038, #53711 ) ;
#118827=CARTESIAN_POINT ( 'NONE',  ( 0.000000000000000000, 0.000000000000000000, 0.000000000000000000 ) ) ;
#118855=DIRECTION ( 'NONE',  ( 1.000000000000000000, 0.000000000000000000, -3.491481338843133355E-15 ) ) ;
#118880=EDGE_LOOP ( 'NONE', ( #92765, #13336, #72150, #104611 ) ) ;
#118928=CARTESIAN_POINT ( 'NONE',  ( -1.642778471874998480, -3.551041666188709645, 2.845375778867863303 ) ) ;
#118959=DIRECTION ( 'NONE',  ( 0.000000000000000000, 1.000000000000000000, 0.000000000000000000 ) ) ;
#118970=CARTESIAN_POINT ( 'NONE',  ( 1.642778471875001811, -0.6927083328553753638, 2.845375778867859751 ) ) ;
#119030=CARTESIAN_POINT ( 'NONE',  ( 3.285556943750000514, -1.451041666188708890, 1.896917185911906500 ) ) ;
#119032=CARTESIAN_POINT ( 'NONE',  ( 1.737499999999999378, -1.822916665710751172, -3.009438278150925683 ) ) ;
#119071=LINE ( 'NONE', #139551, #106593 ) ;
#119076=ADVANCED_FACE ( 'NONE', ( #189466, #173241 ), #158055, .T. ) ;
#119168=CARTESIAN_POINT ( 'NONE',  ( 0.000000000000000000, -1.399999999999998579, 0.000000000000000000 ) ) ;
#119218=CARTESIAN_POINT ( 'NONE',  ( 1.642778471875001811, -2.092708332855373943, 2.845375778867859751 ) ) ;
#119349=DIRECTION ( 'NONE',  ( 0.000000000000000000, 1.000000000000000000, 0.000000000000000000 ) ) ;
#119433=DIRECTION ( 'NONE',  ( 1.000000000000000000, 0.000000000000000000, -3.491481338843133355E-15 ) ) ;
#119515=CARTESIAN_POINT ( 'NONE',  ( -3.285556943750000070, -2.559374999522041172, 0.000000000000000000 ) ) ;
#119549=CARTESIAN_POINT ( 'NONE',  ( -1.642778471874998480, -0.8385416661887100664, 2.845375778867863303 ) ) ;
#119640=CARTESIAN_POINT ( 'NONE',  ( -3.475000000000000533, 0.000000000000000000, 0.000000000000000000 ) ) ;
#119648=DIRECTION ( 'NONE',  ( -0.000000000000000000, 1.000000000000000000, -0.000000000000000000 ) ) ;
#119866=CARTESIAN_POINT ( 'NONE',  ( 1.737500000000001155, -1.589583332377419334, 3.009438278150922130 ) ) ;
#119867=AXIS2_PLACEMENT_3D ( 'NONE', #210430, #161714, #144428 ) ;
#119964=ORIENTED_EDGE ( 'NONE', *, *, #3232, .T. ) ;
#119974=CARTESIAN_POINT ( 'NONE',  ( 1.464175926609780964E-14, -2.187499999999999112, -3.475000000000000533 ) ) ;
#120001=CARTESIAN_POINT ( 'NONE',  ( 3.285556943750000514, -3.463541666188707957, 1.896917185911906500 ) ) ;
#120045=CARTESIAN_POINT ( 'NONE',  ( -3.285556943750000514, -1.188541666188710044, -1.896917185911906500 ) ) ;
#120108=CARTESIAN_POINT ( 'NONE',  ( -3.285556943750000070, -2.646874999522041971, 0.000000000000000000 ) ) ;
#120128=FACE_OUTER_BOUND ( 'NONE', #45657, .T. ) ;
#120205=DIRECTION ( 'NONE',  ( 0.000000000000000000, -1.000000000000000000, -0.000000000000000000 ) ) ;
#120300=CARTESIAN_POINT ( 'NONE',  ( -3.285556943749998737, -2.880208332855377584, 1.896917185911908499 ) ) ;
#120331=CARTESIAN_POINT ( 'NONE',  ( 1.499999999999959810, 7.564371094685075292, -10.87018506808107965 ) ) ;
#120406=ORIENTED_EDGE ( 'NONE', *, *, #113521, .F. ) ;
#120576=CARTESIAN_POINT ( 'NONE',  ( -3.285556943750000514, -1.976041666188710577, -1.896917185911906500 ) ) ;
#120600=CARTESIAN_POINT ( 'NONE',  ( 3.285556943749998737, -1.305208332855376296, -1.896917185911906722 ) ) ;
#120633=CARTESIAN_POINT ( 'NONE',  ( 3.285556943750000070, -1.421874999522041660, 0.000000000000000000 ) ) ;
#120662=EDGE_CURVE ( 'NONE', #12413, #187007, #98593, .T. ) ;
#120688=DIRECTION ( 'NONE',  ( 0.000000000000000000, 0.000000000000000000, -1.000000000000000000 ) ) ;
#120722=CARTESIAN_POINT ( 'NONE',  ( 1.642778471875001811, -3.142708332855375986, 2.845375778867859751 ) ) ;
#121020=LINE ( 'NONE', #201081, #104063 ) ;
#121023=ORIENTED_EDGE ( 'NONE', *, *, #66779, .F. ) ;
#121034=ORIENTED_EDGE ( 'NONE', *, *, #142095, .F. ) ;
#121040=ORIENTED_EDGE ( 'NONE', *, *, #149738, .F. ) ;
#121131=CARTESIAN_POINT ( 'NONE',  ( -3.285556943750000070, -2.209374999522041527, 0.000000000000000000 ) ) ;
#121189=CARTESIAN_POINT ( 'NONE',  ( 3.285556943749998737, -3.492708332855374742, -1.896917185911906500 ) ) ;
#121330=VERTEX_POINT ( 'NONE', #200939 ) ;
#121374=CARTESIAN_POINT ( 'NONE',  ( 3.475000000000000533, -0.9041666666666666741, 2.006292185433948827 ) ) ;
#121398=( BOUNDED_CURVE ( )  B_SPLINE_CURVE ( 2, ( #116406, #168299, #49231, #52418, #69704, #19896, #17746, #35078, #117480 ),
 .UNSPECIFIED., .F., .T. ) 
 B_SPLINE_CURVE_WITH_KNOTS ( ( 3, 2, 2, 2, 3 ),
 ( 0.2341475240440091254, 0.2361111111111111049, 0.2500000000000000000, 0.2638888888888888951, 0.2708333333333333703 ),
 .UNSPECIFIED. ) 
 CURVE ( )  GEOMETRIC_REPRESENTATION_ITEM ( )  RATIONAL_B_SPLINE_CURVE ( ( 0.9674735258996458587, 0.9810589035196658481, 1.000000000000000000, 0.8660254037844387076, 1.000000000000000000, 0.8660254037844387076, 1.000000000000000000, 0.9330127018922190762, 0.9330127018922194093 ) ) 
 REPRESENTATION_ITEM ( '' )  );
#121507=CARTESIAN_POINT ( 'NONE',  ( 1.333315192109691072, 8.250054423670810877, -10.85938449304426356 ) ) ;
#121516=DIRECTION ( 'NONE',  ( 0.000000000000000000, 1.000000000000000000, 0.000000000000000000 ) ) ;
#121520=CARTESIAN_POINT ( 'NONE',  ( -2.128168088883454642E-12, -3.089410100848593466, 3.428390338093493028 ) ) ;
#121562=CARTESIAN_POINT ( 'NONE',  ( -3.474999999999997868, -2.377083332377420088, 2.006292185433951047 ) ) ;
#121649=CARTESIAN_POINT ( 'NONE',  ( 3.285556943750000070, -1.421874999522041660, 0.000000000000000000 ) ) ;
#121664=VECTOR ( 'NONE', #185687, 1000.000000000000000 ) ;
#121675=CARTESIAN_POINT ( 'NONE',  ( -3.285556943749998737, -1.130208332855376918, 1.896917185911908721 ) ) ;
#121703=DIRECTION ( 'NONE',  ( -0.000000000000000000, 1.000000000000000000, -0.000000000000000000 ) ) ;
#121709=CARTESIAN_POINT ( 'NONE',  ( -1.642778471874998480, -0.4885416661887104217, 2.845375778867863303 ) ) ;
#121758=DIRECTION ( 'NONE',  ( 0.7613463080411785322, -0.000000000000000000, 0.6483454320283801309 ) ) ;
#121793=CARTESIAN_POINT ( 'NONE',  ( 1.001543065824772753E-15, -3.871874999522043836, 3.793834371823811669 ) ) ;
#121818=AXIS2_PLACEMENT_3D ( 'NONE', #65001, #147351, #213378 ) ;
#121881=EDGE_CURVE ( 'NONE', #135098, #13166, #178794, .T. ) ;
#122131=CARTESIAN_POINT ( 'NONE',  ( 1.642778471875000035, -2.063541666188710266, -2.845375778867859751 ) ) ;
#122181=ORIENTED_EDGE ( 'NONE', *, *, #73605, .T. ) ;
#122201=CARTESIAN_POINT ( 'NONE',  ( 3.285556943750000070, -1.684374999522043836, 0.000000000000000000 ) ) ;
#122264=CARTESIAN_POINT ( 'NONE',  ( 1.642778471875000035, -0.2260416661887081069, -2.845375778867859751 ) ) ;
#122371=DIRECTION ( 'NONE',  ( 0.000000000000000000, 1.000000000000000000, 0.000000000000000000 ) ) ;
#122418=CARTESIAN_POINT ( 'NONE',  ( 1.642778471875001811, -0.6927083328553753638, 2.845375778867859751 ) ) ;
#122422=EDGE_CURVE ( 'NONE', #135209, #12134, #76329, .T. ) ;
#122455=CARTESIAN_POINT ( 'NONE',  ( -3.474999999999998312, -0.3208333333333319715, 2.006292185433951047 ) ) ;
#122484=DIRECTION ( 'NONE',  ( 0.000000000000000000, -1.000000000000000000, 0.000000000000000000 ) ) ;
#122665=CARTESIAN_POINT ( 'NONE',  ( 1.737499999999999378, -2.522916665710750461, -3.009438278150925683 ) ) ;
#122680=DIRECTION ( 'NONE',  ( 0.000000000000000000, 0.000000000000000000, -1.000000000000000000 ) ) ;
#122692=( BOUNDED_CURVE ( )  B_SPLINE_CURVE ( 2, ( #206257, #170556, #158594, #25376, #23222, #73047, #56816, #122986, #187867 ),
 .UNSPECIFIED., .F., .T. ) 
 B_SPLINE_CURVE_WITH_KNOTS ( ( 3, 2, 2, 2, 3 ),
 ( 0.2291666666666666574, 0.2361111111111111049, 0.2500000000000000000, 0.2638888888888888951, 0.2708333333333333703 ),
 .UNSPECIFIED. ) 
 CURVE ( )  GEOMETRIC_REPRESENTATION_ITEM ( )  RATIONAL_B_SPLINE_CURVE ( ( 0.9330127018922194093, 0.9330127018922194093, 1.000000000000000000, 0.8660254037844387076, 1.000000000000000000, 0.8660254037844387076, 1.000000000000000000, 0.9330127018922190762, 0.9330127018922194093 ) ) 
 REPRESENTATION_ITEM ( '' )  );
#122729=CARTESIAN_POINT ( 'NONE',  ( 1.001543065824772753E-15, -1.509374999522041794, 3.793834371823811669 ) ) ;
#122776=ORIENTED_EDGE ( 'NONE', *, *, #108161, .F. ) ;
#122788=CARTESIAN_POINT ( 'NONE',  ( 3.285556943750000070, -2.121874999522044281, 0.000000000000000000 ) ) ;
#122842=DIRECTION ( 'NONE',  ( 0.6483454320283812411, 0.000000000000000000, -0.7613463080411777550 ) ) ;
#122881=CARTESIAN_POINT ( 'NONE',  ( 1.642778471875001811, -3.492708332855375630, 2.845375778867859751 ) ) ;
#122913=CARTESIAN_POINT ( 'NONE',  ( -2.599325408948150784, -3.206724562287903257, 2.073009253707752464 ) ) ;
#122916=ORIENTED_EDGE ( 'NONE', *, *, #3680, .T. ) ;
#122936=ORIENTED_EDGE ( 'NONE', *, *, #56061, .T. ) ;
#122986=CARTESIAN_POINT ( 'NONE',  ( -0.9311234436981480345, -1.428119629485601338, -3.475000000000001421 ) ) ;
#123076=ORIENTED_EDGE ( 'NONE', *, *, #133615, .F. ) ;
#123211=CARTESIAN_POINT ( 'NONE',  ( -3.285556943750000070, -0.8929624362542626370, 0.2544620058384380323 ) ) ;
#123278=CARTESIAN_POINT ( 'NONE',  ( 0.000000000000000000, -3.346874999522042149, -3.793834371823813001 ) ) ;
#123316=VECTOR ( 'NONE', #116072, 1000.000000000000000 ) ;
#123330=DIRECTION ( 'NONE',  ( -0.000000000000000000, -1.000000000000000000, -0.000000000000000000 ) ) ;
#123334=CARTESIAN_POINT ( 'NONE',  ( 3.285556943750000070, -3.171874999522043215, 0.000000000000000000 ) ) ;
#123350=DIRECTION ( 'NONE',  ( 0.000000000000000000, 0.000000000000000000, 1.000000000000000000 ) ) ;
#123365=CARTESIAN_POINT ( 'NONE',  ( 0.000000000000000000, -0.5000000000000005551, 0.000000000000000000 ) ) ;
#123523=CARTESIAN_POINT ( 'NONE',  ( -1.642778471875000035, -3.667708332855373676, -2.845375778867859751 ) ) ;
#123555=DIRECTION ( 'NONE',  ( -0.6483454320283799088, 0.000000000000000000, 0.7613463080411786432 ) ) ;
#123710=ORIENTED_EDGE ( 'NONE', *, *, #9209, .T. ) ;
#123712=ORIENTED_EDGE ( 'NONE', *, *, #132981, .T. ) ;
#123760=LINE ( 'NONE', #188660, #39676 ) ;
#123793=CARTESIAN_POINT ( 'NONE',  ( 3.285556943750000514, -1.801041666188707424, 1.896917185911906500 ) ) ;
#123849=CARTESIAN_POINT ( 'NONE',  ( 1.001543065824772753E-15, -1.509374999522041794, 3.793834371823811669 ) ) ;
#123937=CARTESIAN_POINT ( 'NONE',  ( -1.737500000000000266, -0.4083333333333334370, -3.009438278150923907 ) ) ;
#123956=CARTESIAN_POINT ( 'NONE',  ( -1.782949938078044916, -1.500000000000001332, 2.093702347113242102 ) ) ;
#123987=ORIENTED_EDGE ( 'NONE', *, *, #55534, .T. ) ;
#124023=CARTESIAN_POINT ( 'NONE',  ( 1.737500000000001155, -1.283333333333334325, 3.009438278150922130 ) ) ;
#124087=CARTESIAN_POINT ( 'NONE',  ( -3.420250508247430155, -0.02876672507465954931, -0.2938434605158617985 ) ) ;
#124113=FACE_OUTER_BOUND ( 'NONE', #185911, .T. ) ;
#124332=CARTESIAN_POINT ( 'NONE',  ( 3.285556943750000514, -3.113541666188709645, 1.896917185911906500 ) ) ;
#124365=ORIENTED_EDGE ( 'NONE', *, *, #153278, .T. ) ;
#124394=CARTESIAN_POINT ( 'NONE',  ( 1.001543065824772753E-15, -0.3718749995220430038, 3.793834371823811669 ) ) ;
#124494=CARTESIAN_POINT ( 'NONE',  ( -2.549999999999999378, 1.000000000000000888, 1.849324200890692271 ) ) ;
#124500=EDGE_LOOP ( 'NONE', ( #25045, #168535, #97699, #22887 ) ) ;
#124545=CARTESIAN_POINT ( 'NONE',  ( -1.642778471874998480, -0.4010416661887096224, 2.845375778867863303 ) ) ;
#124580=CARTESIAN_POINT ( 'NONE',  ( -3.285556943749998737, -3.930208332855377407, 1.896917185911908499 ) ) ;
#124593=EDGE_CURVE ( 'NONE', #36461, #80335, #7011, .T. ) ;
#124617=LINE ( 'NONE', #7554, #26639 ) ;
#124726=CONICAL_SURFACE ( 'NONE', #152310, 3.000000000000000000, 0.7853981633974523868 ) ;
#124844=CARTESIAN_POINT ( 'NONE',  ( -3.285556943750000070, -1.246874999522043392, 0.000000000000000000 ) ) ;
#124854=CARTESIAN_POINT ( 'NONE',  ( 1.333315192109769454, 8.250054423670803772, 10.85938449304425113 ) ) ;
#124900=CYLINDRICAL_SURFACE ( 'NONE', #187822, 10.25000000000000000 ) ;
#124905=CARTESIAN_POINT ( 'NONE',  ( -1.642778471874998480, -2.238541666188708312, 2.845375778867863303 ) ) ;
#124998=CARTESIAN_POINT ( 'NONE',  ( -3.475000000000000533, -1.049999999999998934, 0.000000000000000000 ) ) ;
#125034=CARTESIAN_POINT ( 'NONE',  ( -0.3037066968988046400, -3.101636548795144943, 3.416163890146756810 ) ) ;
#125041=EDGE_CURVE ( 'NONE', #167380, #213109, #26360, .T. ) ;
#125069=CIRCLE ( 'NONE', #69594, 11.00000000000000000 ) ;
#125074=AXIS2_PLACEMENT_3D ( 'NONE', #196601, #79647, #96996 ) ;
#125089=CARTESIAN_POINT ( 'NONE',  ( 3.475000000000000533, -0.9041666666666666741, 2.006292185433948827 ) ) ;
#125112=DIRECTION ( 'NONE',  ( 0.000000000000000000, 0.000000000000000000, -1.000000000000000000 ) ) ;
#125142=ADVANCED_FACE ( 'NONE', ( #4968 ), #144399, .F. ) ;
#125160=CARTESIAN_POINT ( 'NONE',  ( 3.475000000000000533, -0.8604166657107521488, 2.006292185433948827 ) ) ;
#125225=ADVANCED_FACE ( 'NONE', ( #131358 ), #164861, .T. ) ;
#125316=FACE_OUTER_BOUND ( 'NONE', #183175, .T. ) ;
#125320=FACE_OUTER_BOUND ( 'NONE', #177808, .T. ) ;
#125328=CARTESIAN_POINT ( 'NONE',  ( -3.285556943750000514, -2.326041666188708668, -1.896917185911906722 ) ) ;
#125371=ORIENTED_EDGE ( 'NONE', *, *, #211811, .T. ) ;
#125387=CARTESIAN_POINT ( 'NONE',  ( -1.642778471874998480, -3.201041666188710000, 2.845375778867863303 ) ) ;
#125455=CARTESIAN_POINT ( 'NONE',  ( 1.642778471875001811, -3.930208332855376074, 2.845375778867859751 ) ) ;
#125554=CARTESIAN_POINT ( 'NONE',  ( 0.000000000000000000, 0.5999999999999998668, 0.000000000000000000 ) ) ;
#125579=CIRCLE ( 'NONE', #73537, 3.150000000000000799 ) ;
#125641=CARTESIAN_POINT ( 'NONE',  ( -3.475000000000000533, -1.079166666666665941, -2.006292185433948827 ) ) ;
#125746=DIRECTION ( 'NONE',  ( -0.000000000000000000, 1.000000000000000000, -0.000000000000000000 ) ) ;
#125797=( BOUNDED_SURFACE ( )  B_SPLINE_SURFACE ( 1, 2, ( 
 ( #149805, #70645, #136755, #164975, #36030, #67440, #201715, #54434, #181219, #16567, #82650, #148734, #133585, #302, #66373, #132521, #34958, #198519, #101029, #167120, #73883, #156214, #56570, #105336, #76012, #40328, #170300, #91219, #25116, #6719, #26184, #204917, #203850, #8869, #208128, #39244, #124844, #7790, #157280, #108580, #55495, #106433, #121649, #139976, #205998, #122729, #142115, #188692, #207066, #57634, #71716, #190810, #104254, #174608, #74948, #123793, #21888, #137829, #141059, #41403, #172455, #120576, #189751, #24042, #107513, #173542, #90146, #171373, #186553, #58696, #87998, #42470, #92299, #72798, #158343, #9937, #187616, #38182, #154070, #22966, #5635, #89081, #155138, #138898, #146101, #48588, #212112, #164455, #82125, #213182, #84268, #64811, #149270, #16042, #10991, #66914, #43536, #116826, #181748, #65849, #175661, #77066, #99460, #198007, #49634, #133055, #849, #199056, #196948, #63749, #125917, #34443, #130958, #83187, #147157, #81071, #180699, #27248, #50702, #150353, #163400, #109659, #129908, #182828, #100517, #131998, #32323, #148218, #115758, #191876, #114704, #33379, #166592, #165517, #98391, #179648, #18181, #59757, #214220 ),
 ( #93355, #159392, #17109, #195892, #47530, #113643, #31268, #97343, #14975, #170854, #168719, #135179, #200134, #187094, #105903, #52833, #87481, #202259, #201194, #102661, #118970, #117904, #2992, #4055, #89629, #184948, #36575, #171927, #20322, #69059, #88555, #204390, #67982, #37656, #151418, #103733, #104809, #120045, #138372, #39796, #72264, #86408, #54978, #154616, #1924, #152475, #153547, #167654, #136237, #22444, #56045, #101586, #21373, #6195, #122201, #134125, #35509, #70125, #38728, #188163, #53910, #186019, #19255, #203326, #51787, #23523, #183897, #85336, #169784, #5116, #71193, #137310, #121131, #193507, #45148, #9421, #93903, #57109, #207610, #92833, #155681, #190292, #174087, #75492, #139442, #111260, #177263, #141603, #25660, #127535, #208668, #43018, #110194, #91769, #59229, #40879, #61378, #157825, #28878, #143740, #60299, #205477, #142658, #124332, #192421, #7263, #125387, #191353, #126457, #109132, #44075, #123278, #73340, #108062, #189240, #176204, #27805, #175145, #10473, #77617, #159942, #26731, #11547, #41949, #209734, #106984, #173009, #8347, #24590, #90697, #74432, #158877, #156760, #76547, #140532, #206544, #58174, #116566, #33131 ) ),
 .UNSPECIFIED., .F., .F., .T. ) 
 B_SPLINE_SURFACE_WITH_KNOTS ( ( 2, 2 ),
 ( 3, 2, 2, 2, 2, 2, 2, 2, 2, 2, 2, 2, 2, 2, 2, 2, 2, 2, 2, 2, 2, 2, 2, 2, 2, 2, 2, 2, 2, 2, 2, 2, 2, 2, 2, 2, 2, 2, 2, 2, 2, 2, 2, 2, 2, 2, 2, 2, 2, 2, 2, 2, 2, 2, 2, 2, 2, 2, 2, 2, 2, 2, 2, 2, 2, 2, 2, 2, 2, 3 ),
 ( 0.000000000000000000, 1.000000000000000000 ),
 ( 0.000000000000000000, 0.01388888888888888812, 0.02777777777777777624, 0.04166666666666666435, 0.05555555555555555247, 0.06944444444444444753, 0.08333333333333332871, 0.09722222222222222376, 0.1111111111111111049, 0.1250000000000000000, 0.1388888888888888951, 0.1527777777777777901, 0.1666666666666666574, 0.1805555555555555525, 0.1944444444444444475, 0.2083333333333333426, 0.2222222222222222099, 0.2361111111111111049, 0.2500000000000000000, 0.2638888888888888951, 0.2777777777777777901, 0.2916666666666666852, 0.3055555555555555802, 0.3194444444444444198, 0.3333333333333333148, 0.3472222222222222099, 0.3611111111111111049, 0.3750000000000000000, 0.3888888888888888951, 0.4027777777777777901, 0.4166666666666666852, 0.4305555555555555802, 0.4444444444444444198, 0.4583333333333333148, 0.4722222222222222099, 0.4861111111111111049, 0.5000000000000000000, 0.5138888888888888395, 0.5277777777777777901, 0.5416666666666666297, 0.5555555555555555802, 0.5694444444444444198, 0.5833333333333333703, 0.5972222222222222099, 0.6111111111111111605, 0.6250000000000000000, 0.6388888888888888395, 0.6527777777777777901, 0.6666666666666666297, 0.6805555555555555802, 0.6944444444444444198, 0.7083333333333333703, 0.7222222222222222099, 0.7361111111111111605, 0.7500000000000000000, 0.7638888888888888395, 0.7777777777777777901, 0.7916666666666666297, 0.8055555555555555802, 0.8194444444444444198, 0.8333333333333333703, 0.8472222222222222099, 0.8611111111111111605, 0.8750000000000000000, 0.8888888888888888395, 0.9027777777777777901, 0.9166666666666666297, 0.9305555555555555802, 0.9444444444444444198, 0.9523586353390159909 ),
 .UNSPECIFIED. ) 
 GEOMETRIC_REPRESENTATION_ITEM ( )  RATIONAL_B_SPLINE_SURFACE ( (
 ( 1.000000000000000000, 0.8660254037844387076, 1.000000000000000000, 0.8660254037844387076, 1.000000000000000000, 0.8660254037844387076, 1.000000000000000000, 0.8660254037844387076, 1.000000000000000000, 0.8660254037844387076, 1.000000000000000000, 0.8660254037844387076, 1.000000000000000000, 0.8660254037844387076, 1.000000000000000000, 0.8660254037844387076, 1.000000000000000000, 0.8660254037844387076, 1.000000000000000000, 0.8660254037844387076, 1.000000000000000000, 0.8660254037844387076, 1.000000000000000000, 0.8660254037844387076, 1.000000000000000000, 0.8660254037844387076, 1.000000000000000000, 0.8660254037844387076, 1.000000000000000000, 0.8660254037844387076, 1.000000000000000000, 0.8660254037844387076, 1.000000000000000000, 0.8660254037844387076, 1.000000000000000000, 0.8660254037844387076, 1.000000000000000000, 0.8660254037844387076, 1.000000000000000000, 0.8660254037844387076, 1.000000000000000000, 0.8660254037844387076, 1.000000000000000000, 0.8660254037844387076, 1.000000000000000000, 0.8660254037844387076, 1.000000000000000000, 0.8660254037844387076, 1.000000000000000000, 0.8660254037844387076, 1.000000000000000000, 0.8660254037844387076, 1.000000000000000000, 0.8660254037844387076, 1.000000000000000000, 0.8660254037844387076, 1.000000000000000000, 0.8660254037844387076, 1.000000000000000000, 0.8660254037844387076, 1.000000000000000000, 0.8660254037844387076, 1.000000000000000000, 0.8660254037844387076, 1.000000000000000000, 0.8660254037844387076, 1.000000000000000000, 0.8660254037844387076, 1.000000000000000000, 0.8660254037844387076, 1.000000000000000000, 0.8660254037844387076, 1.000000000000000000, 0.8660254037844387076, 1.000000000000000000, 0.8660254037844387076, 1.000000000000000000, 0.8660254037844387076, 1.000000000000000000, 0.8660254037844387076, 1.000000000000000000, 0.8660254037844387076, 1.000000000000000000, 0.8660254037844387076, 1.000000000000000000, 0.8660254037844387076, 1.000000000000000000, 0.8660254037844387076, 1.000000000000000000, 0.8660254037844387076, 1.000000000000000000, 0.8660254037844387076, 1.000000000000000000, 0.8660254037844387076, 1.000000000000000000, 0.8660254037844387076, 1.000000000000000000, 0.8660254037844387076, 1.000000000000000000, 0.8660254037844387076, 1.000000000000000000, 0.8660254037844387076, 1.000000000000000000, 0.8660254037844387076, 1.000000000000000000, 0.8660254037844387076, 1.000000000000000000, 0.8660254037844387076, 1.000000000000000000, 0.8660254037844387076, 1.000000000000000000, 0.8660254037844387076, 1.000000000000000000, 0.8660254037844387076, 1.000000000000000000, 0.8660254037844387076, 1.000000000000000000, 0.8660254037844387076, 1.000000000000000000, 0.8660254037844387076, 1.000000000000000000, 0.8660254037844387076, 1.000000000000000000, 0.8660254037844387076, 1.000000000000000000, 0.8660254037844387076, 1.000000000000000000, 0.8660254037844387076, 1.000000000000000000, 0.8660254037844387076, 1.000000000000000000, 0.8660254037844387076, 1.000000000000000000, 0.8660254037844387076, 1.000000000000000000, 0.8660254037844387076, 1.000000000000000000, 0.9236583618779372618, 0.9343189745674063129),
 ( 1.000000000000000000, 0.8660254037844387076, 1.000000000000000000, 0.8660254037844387076, 1.000000000000000000, 0.8660254037844387076, 1.000000000000000000, 0.8660254037844387076, 1.000000000000000000, 0.8660254037844387076, 1.000000000000000000, 0.8660254037844387076, 1.000000000000000000, 0.8660254037844387076, 1.000000000000000000, 0.8660254037844387076, 1.000000000000000000, 0.8660254037844387076, 1.000000000000000000, 0.8660254037844387076, 1.000000000000000000, 0.8660254037844387076, 1.000000000000000000, 0.8660254037844387076, 1.000000000000000000, 0.8660254037844387076, 1.000000000000000000, 0.8660254037844387076, 1.000000000000000000, 0.8660254037844387076, 1.000000000000000000, 0.8660254037844387076, 1.000000000000000000, 0.8660254037844387076, 1.000000000000000000, 0.8660254037844387076, 1.000000000000000000, 0.8660254037844387076, 1.000000000000000000, 0.8660254037844387076, 1.000000000000000000, 0.8660254037844387076, 1.000000000000000000, 0.8660254037844387076, 1.000000000000000000, 0.8660254037844387076, 1.000000000000000000, 0.8660254037844387076, 1.000000000000000000, 0.8660254037844387076, 1.000000000000000000, 0.8660254037844387076, 1.000000000000000000, 0.8660254037844387076, 1.000000000000000000, 0.8660254037844387076, 1.000000000000000000, 0.8660254037844387076, 1.000000000000000000, 0.8660254037844387076, 1.000000000000000000, 0.8660254037844387076, 1.000000000000000000, 0.8660254037844387076, 1.000000000000000000, 0.8660254037844387076, 1.000000000000000000, 0.8660254037844387076, 1.000000000000000000, 0.8660254037844387076, 1.000000000000000000, 0.8660254037844387076, 1.000000000000000000, 0.8660254037844387076, 1.000000000000000000, 0.8660254037844387076, 1.000000000000000000, 0.8660254037844387076, 1.000000000000000000, 0.8660254037844387076, 1.000000000000000000, 0.8660254037844387076, 1.000000000000000000, 0.8660254037844387076, 1.000000000000000000, 0.8660254037844387076, 1.000000000000000000, 0.8660254037844387076, 1.000000000000000000, 0.8660254037844387076, 1.000000000000000000, 0.8660254037844387076, 1.000000000000000000, 0.8660254037844387076, 1.000000000000000000, 0.8660254037844387076, 1.000000000000000000, 0.8660254037844387076, 1.000000000000000000, 0.8660254037844387076, 1.000000000000000000, 0.8660254037844387076, 1.000000000000000000, 0.8660254037844387076, 1.000000000000000000, 0.8660254037844387076, 1.000000000000000000, 0.8660254037844387076, 1.000000000000000000, 0.8660254037844387076, 1.000000000000000000, 0.8660254037844387076, 1.000000000000000000, 0.8660254037844387076, 1.000000000000000000, 0.8660254037844387076, 1.000000000000000000, 0.8660254037844387076, 1.000000000000000000, 0.8660254037844387076, 1.000000000000000000, 0.8660254037844387076, 1.000000000000000000, 0.8660254037844387076, 1.000000000000000000, 0.8660254037844387076, 1.000000000000000000, 0.8660254037844387076, 1.000000000000000000, 0.8660254037844387076, 1.000000000000000000, 0.8660254037844387076, 1.000000000000000000, 0.8660254037844387076, 1.000000000000000000, 0.8660254037844387076, 1.000000000000000000, 0.9236583618779372618, 0.9343189745674063129) ) ) 
 REPRESENTATION_ITEM ( '' )  SURFACE ( )  );
#125828=CARTESIAN_POINT ( 'NONE',  ( -0.9311234436981532525, -2.334380368602567035, 3.474999999999999201 ) ) ;
#125917=CARTESIAN_POINT ( 'NONE',  ( -1.642778471875000035, -3.405208332855375275, -2.845375778867859751 ) ) ;
#125971=CARTESIAN_POINT ( 'NONE',  ( -3.285556943750000514, -1.976041666188710577, -1.896917185911906500 ) ) ;
#126059=CARTESIAN_POINT ( 'NONE',  ( -3.475000000000000533, -0.7291666666666675178, -2.006292185433948827 ) ) ;
#126132=CARTESIAN_POINT ( 'NONE',  ( 0.000000000000000000, -2.996874999522043392, -3.793834371823813445 ) ) ;
#126150=CARTESIAN_POINT ( 'NONE',  ( 1.737499999999999378, -1.866666666666665808, -3.009438278150925683 ) ) ;
#126225=CARTESIAN_POINT ( 'NONE',  ( -3.475000000000000533, -1.356249999044083943, 0.000000000000000000 ) ) ;
#126255=EDGE_CURVE ( 'NONE', #55892, #89074, #106049, .T. ) ;
#126312=CARTESIAN_POINT ( 'NONE',  ( -3.285556943749998737, -0.4302083328553760744, 1.896917185911908499 ) ) ;
#126327=CARTESIAN_POINT ( 'NONE',  ( 1.556029036868112669, 0.4000000000000010214, -1.827231139298829188 ) ) ;
#126355=AXIS2_PLACEMENT_3D ( 'NONE', #150562, #83400, #68198 ) ;
#126395=CARTESIAN_POINT ( 'NONE',  ( 3.285556943750000514, -3.201041666188709112, 1.896917185911906722 ) ) ;
#126440=VERTEX_POINT ( 'NONE', #45545 ) ;
#126451=ORIENTED_EDGE ( 'NONE', *, *, #59704, .F. ) ;
#126457=CARTESIAN_POINT ( 'NONE',  ( -3.285556943750000070, -3.259374999522044014, 0.000000000000000000 ) ) ;
#126480=CARTESIAN_POINT ( 'NONE',  ( 0.000000000000000000, -1.500000000000001332, 0.000000000000000000 ) ) ;
#126523=CARTESIAN_POINT ( 'NONE',  ( -3.285556943750000070, -1.509374999522042238, 0.000000000000000000 ) ) ;
#126545=DIRECTION ( 'NONE',  ( 0.000000000000000000, 1.000000000000000000, 0.000000000000000000 ) ) ;
#126570=CARTESIAN_POINT ( 'NONE',  ( -1.737500000000000266, -1.764583332377417380, -3.009438278150923907 ) ) ;
#126638=CARTESIAN_POINT ( 'NONE',  ( -0.3861634464758929020, -3.134276582748693585, -3.366986391098497400 ) ) ;
#126668=CARTESIAN_POINT ( 'NONE',  ( -1.642778471875000035, -2.267708332855375541, -2.845375778867859751 ) ) ;
#126706=CARTESIAN_POINT ( 'NONE',  ( 1.737500000000001155, -1.983333333333333393, 3.009438278150922130 ) ) ;
#126773=CARTESIAN_POINT ( 'NONE',  ( -3.398092380850382455, -3.087907399781644191, -0.5045427134251018186 ) ) ;
#126789=EDGE_LOOP ( 'NONE', ( #177604, #172927, #56519, #43989 ) ) ;
#126845=AXIS2_PLACEMENT_3D ( 'NONE', #55408, #25029, #104169 ) ;
#126916=CARTESIAN_POINT ( 'NONE',  ( -1.250000000000039302, 8.500000000000000000, -10.85702537530423228 ) ) ;
#126923=B_SPLINE_CURVE_WITH_KNOTS ( 'NONE', 3,
 ( #213205, #144011, #145070, #45414 ),
 .UNSPECIFIED., .F., .F.,
 ( 4, 4 ),
 ( 0.000000000000000000, 0.0002939798689656232381 ),
 .UNSPECIFIED. ) ;
#126962=CIRCLE ( 'NONE', #116557, 0.4999999999999995559 ) ;
#126973=CARTESIAN_POINT ( 'NONE',  ( -1.642778471875000035, -0.5177083328553738761, -2.845375778867859751 ) ) ;
#127041=CARTESIAN_POINT ( 'NONE',  ( 1.001543065824772753E-15, -3.259374999522042682, 3.793834371823811669 ) ) ;
#127070=EDGE_CURVE ( 'NONE', #59550, #153466, #126962, .T. ) ;
#127132=CARTESIAN_POINT ( 'NONE',  ( -3.475000000000000533, -1.079166666666665941, -2.006292185433948827 ) ) ;
#127149=DIRECTION ( 'NONE',  ( 0.000000000000000000, 1.000000000000000000, 0.000000000000000000 ) ) ;
#127152=AXIS2_PLACEMENT_3D ( 'NONE', #66170, #179972, #13188 ) ;
#127209=CARTESIAN_POINT ( 'NONE',  ( -1.642778471875000035, -2.967708332855374831, -2.845375778867859751 ) ) ;
#127227=CARTESIAN_POINT ( 'NONE',  ( 1.737499999999999378, -2.566666666666668650, -3.009438278150925683 ) ) ;
#127251=FACE_OUTER_BOUND ( 'NONE', #46267, .T. ) ;
#127300=FACE_OUTER_BOUND ( 'NONE', #200321, .T. ) ;
#127328=EDGE_CURVE ( 'NONE', #137341, #10807, #80435, .T. ) ;
#127384=CARTESIAN_POINT ( 'NONE',  ( -3.285556943750000514, -0.4885416661887091450, -1.896917185911906500 ) ) ;
#127392=PLANE ( 'NONE',  #157059 ) ;
#127407=CARTESIAN_POINT ( 'NONE',  ( 1.734723475976807094E-15, 2.499999999999998668, 0.000000000000000000 ) ) ;
#127417=EDGE_LOOP ( 'NONE', ( #35013, #171963, #57042, #97055, #71101, #136270, #146807, #131417, #210244, #41870, #166664, #122936, #114056, #7408, #207270, #98733, #191234, #185951 ) ) ;
#127427=VECTOR ( 'NONE', #189976, 1000.000000000000000 ) ;
#127473=CARTESIAN_POINT ( 'NONE',  ( 3.285556943749998737, -2.792708332855373676, -1.896917185911906722 ) ) ;
#127518=ORIENTED_EDGE ( 'NONE', *, *, #153552, .F. ) ;
#127535=CARTESIAN_POINT ( 'NONE',  ( 3.285556943749998737, -2.705208332855374209, -1.896917185911906500 ) ) ;
#127571=AXIS2_PLACEMENT_3D ( 'NONE', #90916, #174305, #109354 ) ;
#127600=CARTESIAN_POINT ( 'NONE',  ( 3.285556943750000070, -1.334374999522040861, 0.000000000000000000 ) ) ;
#127749=CARTESIAN_POINT ( 'NONE',  ( -1.642778471874998480, -2.851041666188706802, 2.845375778867863303 ) ) ;
#127759=AXIS2_PLACEMENT_3D ( 'NONE', #28438, #162721, #175770 ) ;
#127789=CARTESIAN_POINT ( 'NONE',  ( 1.737500000000001155, -1.633333333333333748, 3.009438278150922130 ) ) ;
#127855=CARTESIAN_POINT ( 'NONE',  ( 1.642778471875000035, -0.3135416661887088785, -2.845375778867859751 ) ) ;
#127996=CARTESIAN_POINT ( 'NONE',  ( 1.249999999999964695, 8.500000000000000000, -9.921567416492218072 ) ) ;
#128141=EDGE_CURVE ( 'NONE', #110540, #75662, #10760, .T. ) ;
#128165=CARTESIAN_POINT ( 'NONE',  ( 0.000000000000000000, 6.999999999999999112, 0.000000000000000000 ) ) ;
#128182=DIRECTION ( 'NONE',  ( 0.000000000000000000, 0.000000000000000000, -1.000000000000000000 ) ) ;
#128202=VERTEX_POINT ( 'NONE', #163441 ) ;
#128211=CARTESIAN_POINT ( 'NONE',  ( 1.737500000000001155, -1.983333333333333393, 3.009438278150922130 ) ) ;
#128301=CARTESIAN_POINT ( 'NONE',  ( 0.000000000000000000, -1.137499999999999067, -4.012584370867899430 ) ) ;
#128361=( BOUNDED_SURFACE ( )  B_SPLINE_SURFACE ( 1, 2, ( 
 ( #15241, #95484, #196154, #81328, #111768, #62940, #162592, #113908, #77052, #145310, #93343, #129108, #97600, #64014, #126973, #79195, #65056, #160448, #177775, #14166, #131212, #210246, #159379, #163659, #13117, #47794, #194002, #176700, #195082, #45651, #46720, #112833, #130162, #44587, #30460, #197200, #178849, #29390, #94409, #48839, #110700, #180953, #114953, #28313, #12055, #10978, #144253, #133310, #32576, #164709, #200383, #52031, #36826, #34696, #199315, #166847, #41, #16297, #35765, #152721, #82382, #202511, #50961, #20570, #4303, #116019, #151672, #150608, #119218, #148473, #67175, #3243, #54161, #184141, #185201, #118157, #17364, #66105, #83448, #117085, #183084, #136489, #69309, #100765, #132247, #101840, #167908, #102907, #2168, #201442, #134379, #168966, #135421, #19506, #68245, #120300, #198255, #18443, #85582, #98652, #49895, #53083, #84520, #86653, #70374, #182005, #33636, #99709, #165781, #149528, #1114, #157009, #6447, #58427, #170028, #140780, #108312, #204644, #55228, #56295, #40051, #158076, #123523, #7518, #154865, #188414, #103985, #205725, #174332, #141853, #139702, #124580, #74677, #9664, #90943, #206795, #87722, #187349, #8595 ),
 ( #21614, #72525, #190541, #207858, #189487, #42197, #57360, #171102, #153795, #22693, #138621, #122455, #75740, #25908, #106160, #71447, #41130, #107242, #92018, #89881, #59484, #73600, #186273, #37909, #173263, #155933, #5365, #137559, #172186, #24844, #203577, #121374, #38978, #23776, #105064, #88806, #60548, #125641, #45390, #161260, #109382, #179646, #96279, #160189, #212110, #175389, #79995, #47528, #143987, #208914, #209978, #193744, #97340, #62672, #12847, #94150, #127789, #43264, #145043, #113641, #81069, #78921, #63747, #13913, #163398, #30189, #146099, #26975, #126706, #162329, #14972, #129906, #195890, #93080, #111506, #31266, #192667, #61619, #128831, #147155, #28057, #191602, #213180, #177512, #159122, #11790, #44321, #211046, #77864, #29124, #194813, #10723, #76792, #46449, #178581, #95211, #112570, #110443, #142914, #176445, #152473, #168716, #148216, #98389, #35507, #117902, #165515, #64809, #196946, #18179, #84266, #69057, #66912, #17107, #199054, #32321, #48586, #67980, #184946, #114702, #20320, #83185, #52831, #36573, #214218, #50700, #116824, #149268, #101584, #151416, #49631, #150351, #847, #1921, #82123, #130956, #133052, #182826, #65847 ) ),
 .UNSPECIFIED., .F., .F., .T. ) 
 B_SPLINE_SURFACE_WITH_KNOTS ( ( 2, 2 ),
 ( 3, 2, 2, 2, 2, 2, 2, 2, 2, 2, 2, 2, 2, 2, 2, 2, 2, 2, 2, 2, 2, 2, 2, 2, 2, 2, 2, 2, 2, 2, 2, 2, 2, 2, 2, 2, 2, 2, 2, 2, 2, 2, 2, 2, 2, 2, 2, 2, 2, 2, 2, 2, 2, 2, 2, 2, 2, 2, 2, 2, 2, 2, 2, 2, 2, 2, 2, 2, 2, 3 ),
 ( 0.000000000000000000, 1.000000000000000000 ),
 ( 0.000000000000000000, 0.01388888888888888812, 0.02777777777777777624, 0.04166666666666666435, 0.05555555555555555247, 0.06944444444444444753, 0.08333333333333332871, 0.09722222222222222376, 0.1111111111111111049, 0.1250000000000000000, 0.1388888888888888951, 0.1527777777777777901, 0.1666666666666666574, 0.1805555555555555525, 0.1944444444444444475, 0.2083333333333333426, 0.2222222222222222099, 0.2361111111111111049, 0.2500000000000000000, 0.2638888888888888951, 0.2777777777777777901, 0.2916666666666666852, 0.3055555555555555802, 0.3194444444444444198, 0.3333333333333333148, 0.3472222222222222099, 0.3611111111111111049, 0.3750000000000000000, 0.3888888888888888951, 0.4027777777777777901, 0.4166666666666666852, 0.4305555555555555802, 0.4444444444444444198, 0.4583333333333333148, 0.4722222222222222099, 0.4861111111111111049, 0.5000000000000000000, 0.5138888888888888395, 0.5277777777777777901, 0.5416666666666666297, 0.5555555555555555802, 0.5694444444444444198, 0.5833333333333333703, 0.5972222222222222099, 0.6111111111111111605, 0.6250000000000000000, 0.6388888888888888395, 0.6527777777777777901, 0.6666666666666666297, 0.6805555555555555802, 0.6944444444444444198, 0.7083333333333333703, 0.7222222222222222099, 0.7361111111111111605, 0.7500000000000000000, 0.7638888888888888395, 0.7777777777777777901, 0.7916666666666666297, 0.8055555555555555802, 0.8194444444444444198, 0.8333333333333333703, 0.8472222222222222099, 0.8611111111111111605, 0.8750000000000000000, 0.8888888888888888395, 0.9027777777777777901, 0.9166666666666666297, 0.9305555555555555802, 0.9444444444444444198, 0.9523586252412667985 ),
 .UNSPECIFIED. ) 
 GEOMETRIC_REPRESENTATION_ITEM ( )  RATIONAL_B_SPLINE_SURFACE ( (
 ( 1.000000000000000000, 0.8660254037844387076, 1.000000000000000000, 0.8660254037844387076, 1.000000000000000000, 0.8660254037844387076, 1.000000000000000000, 0.8660254037844387076, 1.000000000000000000, 0.8660254037844387076, 1.000000000000000000, 0.8660254037844387076, 1.000000000000000000, 0.8660254037844387076, 1.000000000000000000, 0.8660254037844387076, 1.000000000000000000, 0.8660254037844387076, 1.000000000000000000, 0.8660254037844387076, 1.000000000000000000, 0.8660254037844387076, 1.000000000000000000, 0.8660254037844387076, 1.000000000000000000, 0.8660254037844387076, 1.000000000000000000, 0.8660254037844387076, 1.000000000000000000, 0.8660254037844387076, 1.000000000000000000, 0.8660254037844387076, 1.000000000000000000, 0.8660254037844387076, 1.000000000000000000, 0.8660254037844387076, 1.000000000000000000, 0.8660254037844387076, 1.000000000000000000, 0.8660254037844387076, 1.000000000000000000, 0.8660254037844387076, 1.000000000000000000, 0.8660254037844387076, 1.000000000000000000, 0.8660254037844387076, 1.000000000000000000, 0.8660254037844387076, 1.000000000000000000, 0.8660254037844387076, 1.000000000000000000, 0.8660254037844387076, 1.000000000000000000, 0.8660254037844387076, 1.000000000000000000, 0.8660254037844387076, 1.000000000000000000, 0.8660254037844387076, 1.000000000000000000, 0.8660254037844387076, 1.000000000000000000, 0.8660254037844387076, 1.000000000000000000, 0.8660254037844387076, 1.000000000000000000, 0.8660254037844387076, 1.000000000000000000, 0.8660254037844387076, 1.000000000000000000, 0.8660254037844387076, 1.000000000000000000, 0.8660254037844387076, 1.000000000000000000, 0.8660254037844387076, 1.000000000000000000, 0.8660254037844387076, 1.000000000000000000, 0.8660254037844387076, 1.000000000000000000, 0.8660254037844387076, 1.000000000000000000, 0.8660254037844387076, 1.000000000000000000, 0.8660254037844387076, 1.000000000000000000, 0.8660254037844387076, 1.000000000000000000, 0.8660254037844387076, 1.000000000000000000, 0.8660254037844387076, 1.000000000000000000, 0.8660254037844387076, 1.000000000000000000, 0.8660254037844387076, 1.000000000000000000, 0.8660254037844387076, 1.000000000000000000, 0.8660254037844387076, 1.000000000000000000, 0.8660254037844387076, 1.000000000000000000, 0.8660254037844387076, 1.000000000000000000, 0.8660254037844387076, 1.000000000000000000, 0.8660254037844387076, 1.000000000000000000, 0.8660254037844387076, 1.000000000000000000, 0.8660254037844387076, 1.000000000000000000, 0.8660254037844387076, 1.000000000000000000, 0.8660254037844387076, 1.000000000000000000, 0.8660254037844387076, 1.000000000000000000, 0.8660254037844387076, 1.000000000000000000, 0.8660254037844387076, 1.000000000000000000, 0.8660254037844387076, 1.000000000000000000, 0.8660254037844387076, 1.000000000000000000, 0.8660254037844387076, 1.000000000000000000, 0.8660254037844387076, 1.000000000000000000, 0.8660254037844387076, 1.000000000000000000, 0.8660254037844387076, 1.000000000000000000, 0.8660254037844387076, 1.000000000000000000, 0.8660254037844387076, 1.000000000000000000, 0.9236584592825519691, 0.9343189473637074638),
 ( 1.000000000000000000, 0.8660254037844387076, 1.000000000000000000, 0.8660254037844387076, 1.000000000000000000, 0.8660254037844387076, 1.000000000000000000, 0.8660254037844387076, 1.000000000000000000, 0.8660254037844387076, 1.000000000000000000, 0.8660254037844387076, 1.000000000000000000, 0.8660254037844387076, 1.000000000000000000, 0.8660254037844387076, 1.000000000000000000, 0.8660254037844387076, 1.000000000000000000, 0.8660254037844387076, 1.000000000000000000, 0.8660254037844387076, 1.000000000000000000, 0.8660254037844387076, 1.000000000000000000, 0.8660254037844387076, 1.000000000000000000, 0.8660254037844387076, 1.000000000000000000, 0.8660254037844387076, 1.000000000000000000, 0.8660254037844387076, 1.000000000000000000, 0.8660254037844387076, 1.000000000000000000, 0.8660254037844387076, 1.000000000000000000, 0.8660254037844387076, 1.000000000000000000, 0.8660254037844387076, 1.000000000000000000, 0.8660254037844387076, 1.000000000000000000, 0.8660254037844387076, 1.000000000000000000, 0.8660254037844387076, 1.000000000000000000, 0.8660254037844387076, 1.000000000000000000, 0.8660254037844387076, 1.000000000000000000, 0.8660254037844387076, 1.000000000000000000, 0.8660254037844387076, 1.000000000000000000, 0.8660254037844387076, 1.000000000000000000, 0.8660254037844387076, 1.000000000000000000, 0.8660254037844387076, 1.000000000000000000, 0.8660254037844387076, 1.000000000000000000, 0.8660254037844387076, 1.000000000000000000, 0.8660254037844387076, 1.000000000000000000, 0.8660254037844387076, 1.000000000000000000, 0.8660254037844387076, 1.000000000000000000, 0.8660254037844387076, 1.000000000000000000, 0.8660254037844387076, 1.000000000000000000, 0.8660254037844387076, 1.000000000000000000, 0.8660254037844387076, 1.000000000000000000, 0.8660254037844387076, 1.000000000000000000, 0.8660254037844387076, 1.000000000000000000, 0.8660254037844387076, 1.000000000000000000, 0.8660254037844387076, 1.000000000000000000, 0.8660254037844387076, 1.000000000000000000, 0.8660254037844387076, 1.000000000000000000, 0.8660254037844387076, 1.000000000000000000, 0.8660254037844387076, 1.000000000000000000, 0.8660254037844387076, 1.000000000000000000, 0.8660254037844387076, 1.000000000000000000, 0.8660254037844387076, 1.000000000000000000, 0.8660254037844387076, 1.000000000000000000, 0.8660254037844387076, 1.000000000000000000, 0.8660254037844387076, 1.000000000000000000, 0.8660254037844387076, 1.000000000000000000, 0.8660254037844387076, 1.000000000000000000, 0.8660254037844387076, 1.000000000000000000, 0.8660254037844387076, 1.000000000000000000, 0.8660254037844387076, 1.000000000000000000, 0.8660254037844387076, 1.000000000000000000, 0.8660254037844387076, 1.000000000000000000, 0.8660254037844387076, 1.000000000000000000, 0.8660254037844387076, 1.000000000000000000, 0.8660254037844387076, 1.000000000000000000, 0.8660254037844387076, 1.000000000000000000, 0.8660254037844387076, 1.000000000000000000, 0.8660254037844387076, 1.000000000000000000, 0.8660254037844387076, 1.000000000000000000, 0.8660254037844387076, 1.000000000000000000, 0.9236584592825519691, 0.9343189473637074638) ) ) 
 REPRESENTATION_ITEM ( '' )  SURFACE ( )  );
#128371=CARTESIAN_POINT ( 'NONE',  ( 3.475000000000000533, -1.152083332377417557, -2.006292185433951047 ) ) ;
#128427=CARTESIAN_POINT ( 'NONE',  ( -3.474999999999997868, -2.770833333333333037, 2.006292185433951047 ) ) ;
#128454=EDGE_CURVE ( 'NONE', #88263, #114098, #187809, .T. ) ;
#128535=CARTESIAN_POINT ( 'NONE',  ( 1.642778471875001811, -2.880208332855377584, 2.845375778867859751 ) ) ;
#128661=CARTESIAN_POINT ( 'NONE',  ( 1.642778471875001811, -1.042708332855375009, 2.845375778867859751 ) ) ;
#128793=CARTESIAN_POINT ( 'NONE',  ( 1.001543065824772753E-15, -1.421874999522042327, 3.793834371823811669 ) ) ;
#128831=CARTESIAN_POINT ( 'NONE',  ( 3.475000000000000533, -2.274999999999999467, 0.000000000000000000 ) ) ;
#128836=( LENGTH_UNIT ( ) NAMED_UNIT ( * ) SI_UNIT ( .MILLI., .METRE. ) );
#128864=ORIENTED_EDGE ( 'NONE', *, *, #57277, .F. ) ;
#128895=DIRECTION ( 'NONE',  ( -0.000000000000000000, 1.000000000000000000, -0.000000000000000000 ) ) ;
#128900=CARTESIAN_POINT ( 'NONE',  ( -3.343839487215291673, -3.074644732671757641, 0.8435610638829383889 ) ) ;
#128959=CARTESIAN_POINT ( 'NONE',  ( -3.137887434649874407, -0.8887487162373172156, -0.9976822016299863316 ) ) ;
#129037=EDGE_LOOP ( 'NONE', ( #108599, #31969 ) ) ;
#129078=CARTESIAN_POINT ( 'NONE',  ( 1.499999999999963141, 6.999999999999999112, -9.886859966642596476 ) ) ;
#129108=CARTESIAN_POINT ( 'NONE',  ( -3.285556943749998737, -0.4302083328553760744, 1.896917185911908499 ) ) ;
#129181=CARTESIAN_POINT ( 'NONE',  ( 0.000000000000000000, -3.434374999522041616, -3.793834371823813001 ) ) ;
#129197=CARTESIAN_POINT ( 'NONE',  ( 3.475000000000000533, -2.945833333333332416, -2.006292185433951047 ) ) ;
#129234=CARTESIAN_POINT ( 'NONE',  ( -1.737499999999997824, -1.341666666666668117, 3.009438278150925683 ) ) ;
#129278=CARTESIAN_POINT ( 'NONE',  ( -1.737499999999997824, -1.341666666666668117, 3.009438278150925683 ) ) ;
#129338=ORIENTED_EDGE ( 'NONE', *, *, #127070, .F. ) ;
#129363=CARTESIAN_POINT ( 'NONE',  ( 3.475000000000000533, -3.325000000000001510, 0.000000000000000000 ) ) ;
#129364=DIRECTION ( 'NONE',  ( 0.000000000000000000, 1.000000000000000000, 0.000000000000000000 ) ) ;
#129406=DIRECTION ( 'NONE',  ( 0.000000000000000000, -0.000000000000000000, 1.000000000000000000 ) ) ;
#129435=CARTESIAN_POINT ( 'NONE',  ( 1.737499999999999378, -2.522916665710750461, -3.009438278150925683 ) ) ;
#129520=CARTESIAN_POINT ( 'NONE',  ( 1.642778471875000035, -0.5760416661887077794, -2.845375778867859751 ) ) ;
#129564=EDGE_CURVE ( 'NONE', #142643, #144530, #118614, .T. ) ;
#129586=DIRECTION ( 'NONE',  ( 0.000000000000000000, 0.000000000000000000, -1.000000000000000000 ) ) ;
#129593=EDGE_CURVE ( 'NONE', #3985, #118628, #13172, .T. ) ;
#129600=AXIS2_PLACEMENT_3D ( 'NONE', #86896, #204883, #19747 ) ;
#129660=CARTESIAN_POINT ( 'NONE',  ( 0.000000000000000000, 1.000000000000000888, 0.000000000000000000 ) ) ;
#129725=CARTESIAN_POINT ( 'NONE',  ( 1.642778471875000035, -0.9260416661887073131, -2.845375778867859751 ) ) ;
#129773=CYLINDRICAL_SURFACE ( 'NONE', #200610, 3.475000000000000089 ) ;
#129867=CARTESIAN_POINT ( 'NONE',  ( -3.285556943750000514, -2.238541666188709200, -1.896917185911906500 ) ) ;
#129899=AXIS2_PLACEMENT_3D ( 'NONE', #111454, #64757, #77811 ) ;
#129906=CARTESIAN_POINT ( 'NONE',  ( -3.474999999999998312, -2.070833333333331971, 2.006292185433951047 ) ) ;
#129908=CARTESIAN_POINT ( 'NONE',  ( -1.642778471875000035, -3.755208332855374476, -2.845375778867859751 ) ) ;
#129974=CARTESIAN_POINT ( 'NONE',  ( 3.285556943750000070, -0.3718749995220427262, 0.000000000000000000 ) ) ;
#130093=ORIENTED_EDGE ( 'NONE', *, *, #141806, .T. ) ;
#130158=ORIENTED_EDGE ( 'NONE', *, *, #53039, .F. ) ;
#130162=CARTESIAN_POINT ( 'NONE',  ( 1.642778471875001811, -1.042708332855375009, 2.845375778867859751 ) ) ;
#130169=FACE_OUTER_BOUND ( 'NONE', #175588, .T. ) ;
#130232=CARTESIAN_POINT ( 'NONE',  ( 1.001543065824772753E-15, -3.609374999522044547, 3.793834371823811669 ) ) ;
#130259=VERTEX_POINT ( 'NONE', #200392 ) ;
#130274=TOROIDAL_SURFACE ( 'NONE', #78235, 3.599999999999999201, 0.4999999999999998890 ) ;
#130300=CARTESIAN_POINT ( 'NONE',  ( 2.579764790942817854, -3.169229722560920504, -2.142845477429654810 ) ) ;
#130380=ORIENTED_EDGE ( 'NONE', *, *, #189291, .F. ) ;
#130398=CARTESIAN_POINT ( 'NONE',  ( 0.9311234436981455920, -3.003119629485602182, 3.475000000000003197 ) ) ;
#130418=CARTESIAN_POINT ( 'NONE',  ( -3.475000000000000533, -2.800000000000000266, 0.000000000000000000 ) ) ;
#130484=AXIS2_PLACEMENT_3D ( 'NONE', #19013, #118723, #169546 ) ;
#130492=CARTESIAN_POINT ( 'NONE',  ( -3.474999999999998312, -3.077083332377416713, 2.006292185433951047 ) ) ;
#130533=ORIENTED_EDGE ( 'NONE', *, *, #135864, .T. ) ;
#130574=CARTESIAN_POINT ( 'NONE',  ( 3.285556943750000070, -2.034374999522043481, 0.000000000000000000 ) ) ;
#130600=ORIENTED_EDGE ( 'NONE', *, *, #26315, .T. ) ;
#130691=AXIS2_PLACEMENT_3D ( 'NONE', #26797, #158948, #110263 ) ;
#130772=CARTESIAN_POINT ( 'NONE',  ( -3.285556943750000514, -2.238541666188709200, -1.896917185911906500 ) ) ;
#130778=VERTEX_POINT ( 'NONE', #116039 ) ;
#130914=CARTESIAN_POINT ( 'NONE',  ( 0.000000000000000000, -2.296874999522042327, -3.793834371823813001 ) ) ;
#130956=CARTESIAN_POINT ( 'NONE',  ( 0.000000000000000000, -3.937499999999998224, -4.012584370867899430 ) ) ;
#130958=CARTESIAN_POINT ( 'NONE',  ( 1.642778471875000035, -3.463541666188708845, -2.845375778867859751 ) ) ;
#131036=VECTOR ( 'NONE', #85181, 1000.000000000000000 ) ;
#131138=TOROIDAL_SURFACE ( 'NONE', #6421, 2.400000000000000355, 0.1000000000000000056 ) ;
#131139=CARTESIAN_POINT ( 'NONE',  ( 0.000000000000000000, -1.399999999999998579, 0.000000000000000000 ) ) ;
#131212=CARTESIAN_POINT ( 'NONE',  ( 1.642778471875001811, -0.6927083328553753638, 2.845375778867859751 ) ) ;
#131283=CARTESIAN_POINT ( 'NONE',  ( 1.642778471875000035, -3.463541666188708845, -2.845375778867859751 ) ) ;
#131343=CARTESIAN_POINT ( 'NONE',  ( 3.293788687723198105, -3.198457330048023017, 0.4502801952423823306 ) ) ;
#131358=FACE_OUTER_BOUND ( 'NONE', #36385, .T. ) ;
#131359=CARTESIAN_POINT ( 'NONE',  ( -3.423725384795993421, -0.02120445489797120192, -0.4190739096163836885 ) ) ;
#131369=CARTESIAN_POINT ( 'NONE',  ( 0.000000000000000000, -2.887499999999999289, -4.012584370867899430 ) ) ;
#131417=ORIENTED_EDGE ( 'NONE', *, *, #200594, .T. ) ;
#131445=( BOUNDED_CURVE ( )  B_SPLINE_CURVE ( 3, ( #51986, #199271, #171047, #149482 ),
 .UNSPECIFIED., .F., .T. ) 
 B_SPLINE_CURVE_WITH_KNOTS ( ( 4, 4 ),
 ( 1.420228054018210395, 1.445468495626831107 ),
 .UNSPECIFIED. ) 
 CURVE ( )  GEOMETRIC_REPRESENTATION_ITEM ( )  RATIONAL_B_SPLINE_CURVE ( ( 1.000000000000000000, 0.9999469107135832147, 0.9999469107135832147, 1.000000000000000000 ) ) 
 REPRESENTATION_ITEM ( '' )  );
#131488=DIRECTION ( 'NONE',  ( 0.000000000000000000, 0.000000000000000000, 1.000000000000000000 ) ) ;
#131522=CARTESIAN_POINT ( 'NONE',  ( 1.737500000000001155, -2.289583332377418401, 3.009438278150922130 ) ) ;
#131580=FACE_OUTER_BOUND ( 'NONE', #170645, .T. ) ;
#131612=CARTESIAN_POINT ( 'NONE',  ( -1.642778471875000035, -1.217708332855376607, -2.845375778867859751 ) ) ;
#131738=CIRCLE ( 'NONE', #204322, 0.1000000000000000333 ) ;
#131811=CARTESIAN_POINT ( 'NONE',  ( 3.285556943750000070, -3.784374999522041705, 0.000000000000000000 ) ) ;
#131853=ADVANCED_FACE ( 'NONE', ( #61686 ), #51334, .T. ) ;
#131899=ADVANCED_FACE ( 'NONE', ( #35312 ), #3853, .F. ) ;
#131924=ORIENTED_EDGE ( 'NONE', *, *, #113521, .T. ) ;
#131952=CARTESIAN_POINT ( 'NONE',  ( -1.642778471875000035, -3.317708332855374476, -2.845375778867859751 ) ) ;
#131998=CARTESIAN_POINT ( 'NONE',  ( 3.285556943749998737, -3.842708332855377051, -1.896917185911906500 ) ) ;
#132002=DIRECTION ( 'NONE',  ( 0.000000000000000000, 0.000000000000000000, 1.000000000000000000 ) ) ;
#132062=CARTESIAN_POINT ( 'NONE',  ( 0.000000000000000000, -0.9843749995220403282, -3.793834371823813001 ) ) ;
#132168=DIRECTION ( 'NONE',  ( 3.706092522800016599E-15, 0.000000000000000000, 1.000000000000000000 ) ) ;
#132179=DIRECTION ( 'NONE',  ( 0.000000000000000000, 1.000000000000000000, 0.000000000000000000 ) ) ;
#132234=EDGE_CURVE ( 'NONE', #139750, #76889, #73135, .T. ) ;
#132247=CARTESIAN_POINT ( 'NONE',  ( -3.285556943750000070, -2.559374999522041172, 0.000000000000000000 ) ) ;
#132304=LINE ( 'NONE', #164769, #123316 ) ;
#132313=APPLICATION_CONTEXT ( 'automotive_design' ) ;
#132336=VERTEX_POINT ( 'NONE', #170653 ) ;
#132340=FACE_OUTER_BOUND ( 'NONE', #106192, .T. ) ;
#132390=CARTESIAN_POINT ( 'NONE',  ( 2.287227787140717172, -3.222749323649096720, 2.379012648498802118 ) ) ;
#132418=CARTESIAN_POINT ( 'NONE',  ( 1.001543065824772753E-15, -2.712499999999999911, 4.012584370867899430 ) ) ;
#132508=CARTESIAN_POINT ( 'NONE',  ( 3.475000000000000533, -3.004166666666665542, 2.006292185433948827 ) ) ;
#132521=CARTESIAN_POINT ( 'NONE',  ( 0.000000000000000000, -0.6343749995220417937, -3.793834371823813001 ) ) ;
#132528=AXIS2_PLACEMENT_3D ( 'NONE', #193166, #178002, #48020 ) ;
#132574=CARTESIAN_POINT ( 'NONE',  ( -1.737499999999997824, -2.697916665710752060, 3.009438278150925683 ) ) ;
#132597=CARTESIAN_POINT ( 'NONE',  ( 0.9311234436981545848, -1.503130369558482560, -3.474999999999999201 ) ) ;
#132628=CYLINDRICAL_SURFACE ( 'NONE', #190117, 3.475000000000000089 ) ;
#132660=CARTESIAN_POINT ( 'NONE',  ( -3.285556943749998737, -2.180208332855376518, 1.896917185911908499 ) ) ;
#132862=CARTESIAN_POINT ( 'NONE',  ( 1.001543065824772753E-15, -3.171874999522042327, 3.793834371823811669 ) ) ;
#132929=ORIENTED_EDGE ( 'NONE', *, *, #185077, .T. ) ;
#132938=PLANE ( 'NONE',  #1639 ) ;
#132939=DIRECTION ( 'NONE',  ( -3.491481338843133750E-15, -0.000000000000000000, -1.000000000000000000 ) ) ;
#132981=EDGE_CURVE ( 'NONE', #139750, #157226, #49583, .T. ) ;
#133013=CARTESIAN_POINT ( 'NONE',  ( 3.475000000000000533, -0.1750000000000015432, 0.000000000000000000 ) ) ;
#133052=CARTESIAN_POINT ( 'NONE',  ( 1.737499999999999378, -3.966666666666666785, -3.009438278150925683 ) ) ;
#133055=CARTESIAN_POINT ( 'NONE',  ( 1.001543065824772753E-15, -3.259374999522042682, 3.793834371823811669 ) ) ;
#133121=CARTESIAN_POINT ( 'NONE',  ( 1.001543065824772753E-15, -2.559374999522041172, 3.793834371823811669 ) ) ;
#133174=CARTESIAN_POINT ( 'NONE',  ( -3.065858701071340509, -0.8887487162373149951, -1.201087490044906669 ) ) ;
#133201=CYLINDRICAL_SURFACE ( 'NONE', #151823, 2.500000000000000888 ) ;
#133282=CARTESIAN_POINT ( 'NONE',  ( -3.349705649621375958, -0.9332739474907891797, 0.06918225470302911961 ) ) ;
#133310=CARTESIAN_POINT ( 'NONE',  ( -3.285556943749998737, -1.480208332855375453, 1.896917185911908499 ) ) ;
#133316=CARTESIAN_POINT ( 'NONE',  ( -3.283337425626721373, -0.1112512837626866702, -0.1207467602163218856 ) ) ;
#133451=CARTESIAN_POINT ( 'NONE',  ( 1.752543019934815760, -3.157786969197629467, -2.872674334950378938 ) ) ;
#133457=CYLINDRICAL_SURFACE ( 'NONE', #213949, 3.475000000000000089 ) ;
#133469=CARTESIAN_POINT ( 'NONE',  ( -3.475000000000000533, 0.000000000000000000, 0.000000000000000000 ) ) ;
#133480=CARTESIAN_POINT ( 'NONE',  ( 3.475000000000000533, -3.704166666666666163, 2.006292185433948827 ) ) ;
#133509=DIRECTION ( 'NONE',  ( 0.000000000000000000, 1.000000000000000000, 0.000000000000000000 ) ) ;
#133585=CARTESIAN_POINT ( 'NONE',  ( -3.285556943750000070, -0.5468749995220407722, 0.000000000000000000 ) ) ;
#133608=CARTESIAN_POINT ( 'NONE',  ( 3.285556943750000070, -2.034374999522043481, 0.000000000000000000 ) ) ;
#133615=EDGE_CURVE ( 'NONE', #179285, #51499, #146089, .T. ) ;
#133643=CARTESIAN_POINT ( 'NONE',  ( 1.467871227757891193E-11, -3.138498625356828775, -3.379301813585260383 ) ) ;
#133646=CARTESIAN_POINT ( 'NONE',  ( -3.474999999999998312, -2.377083332377420088, 2.006292185433951047 ) ) ;
#133667=CARTESIAN_POINT ( 'NONE',  ( 0.000000000000000000, -1.500000000000001332, 0.000000000000000000 ) ) ;
#133731=CARTESIAN_POINT ( 'NONE',  ( 3.285556943749998737, -1.655208332855374609, -1.896917185911906500 ) ) ;
#133843=CARTESIAN_POINT ( 'NONE',  ( 0.000000000000000000, 8.500000000000000000, 0.000000000000000000 ) ) ;
#133936=CARTESIAN_POINT ( 'NONE',  ( -3.285556943750000070, -3.959374999522043304, 0.000000000000000000 ) ) ;
#133991=AXIS2_PLACEMENT_3D ( 'NONE', #149560, #167940, #18473 ) ;
#134082=CARTESIAN_POINT ( 'NONE',  ( 1.001543065824772753E-15, -0.6125000000000012657, 4.012584370867899430 ) ) ;
#134125=CARTESIAN_POINT ( 'NONE',  ( 3.285556943750000514, -1.713541666188707735, 1.896917185911906500 ) ) ;
#134152=VECTOR ( 'NONE', #2402, 1000.000000000000000 ) ;
#134184=CARTESIAN_POINT ( 'NONE',  ( 1.642778471875000035, -1.713541666188707291, -2.845375778867859751 ) ) ;
#134200=CARTESIAN_POINT ( 'NONE',  ( -1.458777222063855294, 0.9000000000000014655, 1.713029193092652669 ) ) ;
#134379=CARTESIAN_POINT ( 'NONE',  ( 3.285556943750000070, -2.734374999522042771, 0.000000000000000000 ) ) ;
#134421=CARTESIAN_POINT ( 'NONE',  ( -1.737500000000000266, -2.114583332377416802, -3.009438278150923907 ) ) ;
#134465=VECTOR ( 'NONE', #99430, 1000.000000000000000 ) ;
#134509=CARTESIAN_POINT ( 'NONE',  ( 1.416652131158605110, 8.000043606524068096, -10.86080395187258318 ) ) ;
#134515=CARTESIAN_POINT ( 'NONE',  ( 0.1842363695348751551, -3.140514841257148859, -3.377285597684139162 ) ) ;
#134520=DIRECTION ( 'NONE',  ( 0.000000000000000000, 0.000000000000000000, -1.000000000000000000 ) ) ;
#134530=CARTESIAN_POINT ( 'NONE',  ( -3.456098937306357310, -0.009090518290199266216, -0.2650254050244002513 ) ) ;
#134541=CARTESIAN_POINT ( 'NONE',  ( -3.475000000000000533, -2.450000000000000622, 0.000000000000000000 ) ) ;
#134555=AXIS2_PLACEMENT_3D ( 'NONE', #133667, #153076, #4653 ) ;
#134570=ORIENTED_EDGE ( 'NONE', *, *, #3140, .T. ) ;
#134605=FACE_OUTER_BOUND ( 'NONE', #91171, .T. ) ;
#134608=DIRECTION ( 'NONE',  ( 1.000000000000000000, 0.000000000000000000, -3.491481338843133355E-15 ) ) ;
#134667=CARTESIAN_POINT ( 'NONE',  ( -3.285556943750000070, -1.159374999522042815, 0.000000000000000000 ) ) ;
#134700=CARTESIAN_POINT ( 'NONE',  ( 3.475000000000000533, -3.952083332377417602, -2.006292185433951047 ) ) ;
#134752=DIRECTION ( 'NONE',  ( 0.000000000000000000, 1.000000000000000000, 0.000000000000000000 ) ) ;
#134786=CARTESIAN_POINT ( 'NONE',  ( 3.285556943750000070, -2.384374999522043126, 0.000000000000000000 ) ) ;
#134911=ORIENTED_EDGE ( 'NONE', *, *, #46704, .T. ) ;
#134968=CIRCLE ( 'NONE', #79591, 11.00000000000000000 ) ;
#134984=CARTESIAN_POINT ( 'NONE',  ( -1.642778471874998480, -3.201041666188710000, 2.845375778867863303 ) ) ;
#134989=VERTEX_POINT ( 'NONE', #41362 ) ;
#135066=DIRECTION ( 'NONE',  ( 3.491481338843133355E-15, 0.000000000000000000, 1.000000000000000000 ) ) ;
#135098=VERTEX_POINT ( 'NONE', #145279 ) ;
#135134=CARTESIAN_POINT ( 'NONE',  ( -3.475000000000000533, -0.3791666666666649865, -2.006292185433948827 ) ) ;
#135179=CARTESIAN_POINT ( 'NONE',  ( -3.285556943749998737, -0.4302083328553760744, 1.896917185911908499 ) ) ;
#135209=VERTEX_POINT ( 'NONE', #129078 ) ;
#135222=DIRECTION ( 'NONE',  ( 0.000000000000000000, 1.000000000000000000, 0.000000000000000000 ) ) ;
#135242=CARTESIAN_POINT ( 'NONE',  ( -3.285556943750000514, -1.276041666188709511, -1.896917185911906500 ) ) ;
#135245=CARTESIAN_POINT ( 'NONE',  ( 0.9311234436981545848, -1.809380368602567346, -3.474999999999999201 ) ) ;
#135289=DIRECTION ( 'NONE',  ( 0.000000000000000000, 1.000000000000000000, 0.000000000000000000 ) ) ;
#135392=CARTESIAN_POINT ( 'NONE',  ( -3.372896589461368055, -0.9467711724014528096, 0.1326515144533354784 ) ) ;
#135421=CARTESIAN_POINT ( 'NONE',  ( 1.642778471875001811, -2.792708332855376785, 2.845375778867859751 ) ) ;
#135549=CARTESIAN_POINT ( 'NONE',  ( 1.255262969126037241E-15, 5.000000000000000888, -10.25000000000000000 ) ) ;
#135651=CARTESIAN_POINT ( 'NONE',  ( 0.000000000000000000, 6.999999999999999112, 0.000000000000000000 ) ) ;
#135713=CARTESIAN_POINT ( 'NONE',  ( 3.285556943750000514, -2.413541666188708579, 1.896917185911906722 ) ) ;
#135748=CARTESIAN_POINT ( 'NONE',  ( -3.285556943749998737, -0.8677083328553740760, 1.896917185911908499 ) ) ;
#135834=CARTESIAN_POINT ( 'NONE',  ( -1.642778471875000035, -2.967708332855374831, -2.845375778867859751 ) ) ;
#135864=EDGE_CURVE ( 'NONE', #1142, #205126, #136700, .T. ) ;
#136038=DIRECTION ( 'NONE',  ( 1.000000000000000000, 0.000000000000000000, -3.706092522800016599E-15 ) ) ;
#136062=CARTESIAN_POINT ( 'NONE',  ( 3.475000000000000533, -1.502083332377415870, -2.006292185433951047 ) ) ;
#136167=CARTESIAN_POINT ( 'NONE',  ( -0.9311234436981532525, -2.028130369558482471, 3.474999999999999201 ) ) ;
#136196=CARTESIAN_POINT ( 'NONE',  ( 1.642778471875001811, -3.142708332855375986, 2.845375778867859751 ) ) ;
#136237=CARTESIAN_POINT ( 'NONE',  ( -3.285556943750000070, -1.509374999522042238, 0.000000000000000000 ) ) ;
#136270=ORIENTED_EDGE ( 'NONE', *, *, #82484, .T. ) ;
#136275=CARTESIAN_POINT ( 'NONE',  ( 0.000000000000000000, 8.500000000000000000, 0.000000000000000000 ) ) ;
#136299=CARTESIAN_POINT ( 'NONE',  ( 3.285556943750000070, -2.471874999522040373, 0.000000000000000000 ) ) ;
#136317=CARTESIAN_POINT ( 'NONE',  ( 1.416814887940471390, 7.999555336178685749, 9.899480522462164700 ) ) ;
#136431=DIRECTION ( 'NONE',  ( 0.000000000000000000, 1.000000000000000000, 0.000000000000000000 ) ) ;
#136464=VERTEX_POINT ( 'NONE', #164415 ) ;
#136483=AXIS2_PLACEMENT_3D ( 'NONE', #53296, #183289, #55430 ) ;
#136489=CARTESIAN_POINT ( 'NONE',  ( 1.001543065824772753E-15, -2.471874999522041705, 3.793834371823811669 ) ) ;
#136523=CARTESIAN_POINT ( 'NONE',  ( 1.499999999999959588, 7.750000000000000000, -10.86128356754324820 ) ) ;
#136567=ORIENTED_EDGE ( 'NONE', *, *, #53039, .T. ) ;
#136582=CARTESIAN_POINT ( 'NONE',  ( 0.000000000000000000, 0.5000000000000004441, 0.000000000000000000 ) ) ;
#136596=ORIENTED_EDGE ( 'NONE', *, *, #9209, .F. ) ;
#136610=CARTESIAN_POINT ( 'NONE',  ( 1.255262969126037241E-15, 12.31951671548121219, -10.25000000000000000 ) ) ;
#136693=DIRECTION ( 'NONE',  ( -0.6483454320283800199, 0.000000000000000000, 0.7613463080411786432 ) ) ;
#136700=CIRCLE ( 'NONE', #167760, 10.25000000000000000 ) ;
#136755=CARTESIAN_POINT ( 'NONE',  ( -1.642778471875000035, -0.2552083328553750308, -2.845375778867859751 ) ) ;
#136813=CARTESIAN_POINT ( 'NONE',  ( 1.642778471875000035, -1.363541666188707646, -2.845375778867859751 ) ) ;
#136825=VECTOR ( 'NONE', #211539, 1000.000000000000000 ) ;
#136904=CARTESIAN_POINT ( 'NONE',  ( 3.285556943750000070, -3.784374999522041705, 0.000000000000000000 ) ) ;
#137060=CARTESIAN_POINT ( 'NONE',  ( -3.285556943750000070, -0.1093749995220438809, 0.000000000000000000 ) ) ;
#137127=DIRECTION ( 'NONE',  ( 0.000000000000000000, 0.000000000000000000, 1.000000000000000000 ) ) ;
#137227=ORIENTED_EDGE ( 'NONE', *, *, #13474, .T. ) ;
#137243=CARTESIAN_POINT ( 'NONE',  ( -3.285556943750000514, -0.9260416661887073131, -1.896917185911906722 ) ) ;
#137261=ORIENTED_EDGE ( 'NONE', *, *, #194552, .T. ) ;
#137310=CARTESIAN_POINT ( 'NONE',  ( -3.285556943749998737, -2.180208332855376518, 1.896917185911908499 ) ) ;
#137341=VERTEX_POINT ( 'NONE', #28838 ) ;
#137370=CARTESIAN_POINT ( 'NONE',  ( 1.642778471875001811, -2.880208332855377584, 2.845375778867859751 ) ) ;
#137451=ORIENTED_EDGE ( 'NONE', *, *, #78072, .F. ) ;
#137455=CARTESIAN_POINT ( 'NONE',  ( 2.046417720077495783, -0.9634407361576915463, 2.739321268633221340 ) ) ;
#137559=CARTESIAN_POINT ( 'NONE',  ( 0.000000000000000000, -0.7875000000000005329, -4.012584370867899430 ) ) ;
#137712=CIRCLE ( 'NONE', #179135, 2.350000000000000533 ) ;
#137767=CARTESIAN_POINT ( 'NONE',  ( 0.000000000000000000, 8.500000000000000000, 0.000000000000000000 ) ) ;
#137792=( BOUNDED_CURVE ( )  B_SPLINE_CURVE ( 2, ( #95426, #79138, #149469 ),
 .UNSPECIFIED., .F., .T. ) 
 B_SPLINE_CURVE_WITH_KNOTS ( ( 3, 3 ),
 ( 0.6458333333333333703, 0.6514247127752519351 ),
 .UNSPECIFIED. ) 
 CURVE ( )  GEOMETRIC_REPRESENTATION_ITEM ( )  RATIONAL_B_SPLINE_CURVE ( ( 0.9330127018922192983, 0.9330127018922197424, 0.9764392566477293478 ) ) 
 REPRESENTATION_ITEM ( '' )  );
#137828=DIRECTION ( 'NONE',  ( 1.000000000000000000, 0.000000000000000000, -3.491481338843133355E-15 ) ) ;
#137829=CARTESIAN_POINT ( 'NONE',  ( 1.001543065824772753E-15, -1.859374999522040550, 3.793834371823811669 ) ) ;
#137854=CARTESIAN_POINT ( 'NONE',  ( 1.001543065824772753E-15, -1.771874999522040861, 3.793834371823810780 ) ) ;
#137889=CARTESIAN_POINT ( 'NONE',  ( 1.001543065824772753E-15, -0.4593749995220425819, 3.793834371823811669 ) ) ;
#137970=CARTESIAN_POINT ( 'NONE',  ( -1.642778471874998480, -2.851041666188706802, 2.845375778867863303 ) ) ;
#138135=FACE_OUTER_BOUND ( 'NONE', #77088, .T. ) ;
#138146=STYLED_ITEM ( 'NONE', ( #12852 ), #37156 ) ;
#138257=ORIENTED_EDGE ( 'NONE', *, *, #22298, .T. ) ;
#138372=CARTESIAN_POINT ( 'NONE',  ( -1.642778471875000035, -1.217708332855376607, -2.845375778867859751 ) ) ;
#138435=CARTESIAN_POINT ( 'NONE',  ( 1.642778471875000035, -3.463541666188708845, -2.845375778867859751 ) ) ;
#138486=CARTESIAN_POINT ( 'NONE',  ( 0.000000000000000000, 6.999999999999999112, -11.00000000000000000 ) ) ;
#138517=CARTESIAN_POINT ( 'NONE',  ( 3.278550485571194439, -0.9336338327896769318, -0.8199742731213923719 ) ) ;
#138548=CARTESIAN_POINT ( 'NONE',  ( 1.347111479062088405E-15, 2.000000000000001776, 11.00000000000000000 ) ) ;
#138621=CARTESIAN_POINT ( 'NONE',  ( -1.737499999999997824, -0.2916666666666657415, 3.009438278150925683 ) ) ;
#138834=DIRECTION ( 'NONE',  ( 1.000000000000000000, 0.000000000000000000, -3.491481338843133355E-15 ) ) ;
#138848=DIRECTION ( 'NONE',  ( 0.000000000000000000, -1.000000000000000000, 0.000000000000000000 ) ) ;
#138858=CIRCLE ( 'NONE', #166504, 2.400000000000000799 ) ;
#138898=CARTESIAN_POINT ( 'NONE',  ( -3.285556943749998737, -2.617708332855374298, 1.896917185911908499 ) ) ;
#138901=CARTESIAN_POINT ( 'NONE',  ( 2.550000000000000266, 1.000000000000000888, 1.849324200890695824 ) ) ;
#138957=CARTESIAN_POINT ( 'NONE',  ( -3.285556943749998737, -2.617708332855374298, 1.896917185911908499 ) ) ;
#139044=CARTESIAN_POINT ( 'NONE',  ( -3.285556943750000070, -3.959374999522043304, 0.000000000000000000 ) ) ;
#139063=DIRECTION ( 'NONE',  ( 0.000000000000000000, -1.000000000000000000, -0.000000000000000000 ) ) ;
#139074=EDGE_CURVE ( 'NONE', #202980, #183045, #78080, .T. ) ;
#139081=ORIENTED_EDGE ( 'NONE', *, *, #183120, .F. ) ;
#139101=AXIS2_PLACEMENT_3D ( 'NONE', #188327, #24756, #160100 ) ;
#139266=DIRECTION ( 'NONE',  ( 0.000000000000000000, 1.000000000000000000, 0.000000000000000000 ) ) ;
#139330=EDGE_CURVE ( 'NONE', #27240, #128202, #68518, .T. ) ;
#139337=DIRECTION ( 'NONE',  ( 0.6483454320283800199, 0.000000000000000000, -0.7613463080411787542 ) ) ;
#139375=CARTESIAN_POINT ( 'NONE',  ( 3.285556943749998737, -2.092708332855377051, -1.896917185911906722 ) ) ;
#139381=EDGE_CURVE ( 'NONE', #79131, #139750, #82653, .T. ) ;
#139433=AXIS2_PLACEMENT_3D ( 'NONE', #193197, #129364, #145567 ) ;
#139442=CARTESIAN_POINT ( 'NONE',  ( -3.285556943750000070, -2.559374999522041172, 0.000000000000000000 ) ) ;
#139463=AXIS2_PLACEMENT_3D ( 'NONE', #4623, #6770, #58747 ) ;
#139508=CARTESIAN_POINT ( 'NONE',  ( -3.285556943750000514, -4.076041666188709556, -1.896917185911906500 ) ) ;
#139528=VECTOR ( 'NONE', #77350, 1000.000000000000000 ) ;
#139551=CARTESIAN_POINT ( 'NONE',  ( 5.510910596163088569E-16, 2.499999999999998668, 4.500000000000000000 ) ) ;
#139639=CARTESIAN_POINT ( 'NONE',  ( 1.347111479062088405E-15, 2.999999999999999112, 11.00000000000000000 ) ) ;
#139702=CARTESIAN_POINT ( 'NONE',  ( -1.642778471874998480, -3.901041666188709289, 2.845375778867863303 ) ) ;
#139713=ORIENTED_EDGE ( 'NONE', *, *, #204566, .T. ) ;
#139730=CARTESIAN_POINT ( 'NONE',  ( 1.224646799147353059E-15, 1.000000000000000888, 9.999999999999998224 ) ) ;
#139750=VERTEX_POINT ( 'NONE', #138901 ) ;
#139887=ORIENTED_EDGE ( 'NONE', *, *, #98482, .F. ) ;
#139916=EDGE_CURVE ( 'NONE', #153986, #54700, #85026, .T. ) ;
#139922=EDGE_LOOP ( 'NONE', ( #123712, #190109, #147087, #83832 ) ) ;
#139939=CARTESIAN_POINT ( 'NONE',  ( 2.550000000000000266, 2.499999999999998668, -1.849324200890695824 ) ) ;
#139951=AXIS2_PLACEMENT_3D ( 'NONE', #16102, #200189, #198068 ) ;
#139976=CARTESIAN_POINT ( 'NONE',  ( 3.285556943750000514, -1.451041666188708890, 1.896917185911906500 ) ) ;
#139997=ORIENTED_EDGE ( 'NONE', *, *, #3680, .F. ) ;
#140032=CARTESIAN_POINT ( 'NONE',  ( -3.285556943749998737, -2.267708332855375986, 1.896917185911908499 ) ) ;
#140122=CARTESIAN_POINT ( 'NONE',  ( -3.475000000000000533, -0.3499999999999996447, 0.000000000000000000 ) ) ;
#140141=ADVANCED_FACE ( 'NONE', ( #124113 ), #59015, .F. ) ;
#140200=DIRECTION ( 'NONE',  ( -0.000000000000000000, -1.000000000000000000, -0.000000000000000000 ) ) ;
#140215=CARTESIAN_POINT ( 'NONE',  ( 3.475000000000000533, -1.195833333333332194, -2.006292185433951047 ) ) ;
#140263=CYLINDRICAL_SURFACE ( 'NONE', #64563, 3.475000000000000089 ) ;
#140293=CARTESIAN_POINT ( 'NONE',  ( -1.737499999999997824, -1.647916665710749573, 3.009438278150925683 ) ) ;
#140415=ORIENTED_EDGE ( 'NONE', *, *, #200871, .F. ) ;
#140426=CARTESIAN_POINT ( 'NONE',  ( 0.000000000000000000, 1.000000000000000888, 0.000000000000000000 ) ) ;
#140427=ADVANCED_FACE ( 'NONE', ( #108532 ), #23995, .T. ) ;
#140468=CARTESIAN_POINT ( 'NONE',  ( 0.000000000000000000, -1.334374999522042859, -3.793834371823813445 ) ) ;
#140532=CARTESIAN_POINT ( 'NONE',  ( -1.642778471875000035, -4.017708332855376874, -2.845375778867859751 ) ) ;
#140597=CARTESIAN_POINT ( 'NONE',  ( -3.285556943750000070, -3.696874999522044458, 0.000000000000000000 ) ) ;
#140646=DIRECTION ( 'NONE',  ( -0.000000000000000000, -1.000000000000000000, -0.000000000000000000 ) ) ;
#140677=CARTESIAN_POINT ( 'NONE',  ( 0.8814639207992844838, -0.9023425969398091162, -3.213948531368630679 ) ) ;
#140702=ORIENTED_EDGE ( 'NONE', *, *, #69404, .F. ) ;
#140719=CARTESIAN_POINT ( 'NONE',  ( 0.000000000000000000, -1.500000000000001332, 0.000000000000000000 ) ) ;
#140746=CARTESIAN_POINT ( 'NONE',  ( 1.642778471875001811, -1.042708332855375009, 2.845375778867859751 ) ) ;
#140780=CARTESIAN_POINT ( 'NONE',  ( 3.285556943750000514, -3.463541666188707957, 1.896917185911906500 ) ) ;
#141059=CARTESIAN_POINT ( 'NONE',  ( -1.642778471874998480, -1.888541666188708890, 2.845375778867863303 ) ) ;
#141108=CARTESIAN_POINT ( 'NONE',  ( 0.000000000000000000, 2.999999999999999112, 0.000000000000000000 ) ) ;
#141116=CARTESIAN_POINT ( 'NONE',  ( -1.642778471875000035, -2.705208332855375986, -2.845375778867859751 ) ) ;
#141145=CIRCLE ( 'NONE', #110087, 0.09999999999999986677 ) ;
#141183=DIRECTION ( 'NONE',  ( 0.000000000000000000, -1.000000000000000000, 0.000000000000000000 ) ) ;
#141207=CARTESIAN_POINT ( 'NONE',  ( 1.737500000000001155, -0.5833333333333314830, 3.009438278150922130 ) ) ;
#141214=CARTESIAN_POINT ( 'NONE',  ( 1.224646799147353059E-15, 6.999999999999999112, 9.999999999999998224 ) ) ;
#141281=CARTESIAN_POINT ( 'NONE',  ( 1.001543065824772753E-15, -3.171874999522042771, 3.793834371823810780 ) ) ;
#141299=CARTESIAN_POINT ( 'NONE',  ( 3.475000000000000533, -2.304166666666668473, 2.006292185433948827 ) ) ;
#141317=EDGE_CURVE ( 'NONE', #46791, #5559, #88753, .T. ) ;
#141371=CARTESIAN_POINT ( 'NONE',  ( -1.737500000000000266, -0.3645833323774189116, -3.009438278150923907 ) ) ;
#141408=CARTESIAN_POINT ( 'NONE',  ( 2.687227643083427534E-13, -3.232243495192088201, 3.285556943749999625 ) ) ;
#141434=DIRECTION ( 'NONE',  ( 0.000000000000000000, 0.000000000000000000, 1.000000000000000000 ) ) ;
#141487=ORIENTED_EDGE ( 'NONE', *, *, #69404, .T. ) ;
#141537=AXIS2_PLACEMENT_3D ( 'NONE', #40268, #189700, #59702 ) ;
#141541=CARTESIAN_POINT ( 'NONE',  ( 3.285556943750000514, -2.851041666188706358, 1.896917185911906722 ) ) ;
#141603=CARTESIAN_POINT ( 'NONE',  ( 0.000000000000000000, -2.646874999522040639, -3.793834371823813001 ) ) ;
#141608=ADVANCED_FACE ( 'NONE', ( #97297 ), #130274, .F. ) ;
#141666=CARTESIAN_POINT ( 'NONE',  ( 2.960184520039609524, -4.197067588314596698, -1.425549731837409961 ) ) ;
#141673=VERTEX_POINT ( 'NONE', #65803 ) ;
#141748=CARTESIAN_POINT ( 'NONE',  ( 3.338979018791977449, -0.9437212195340001220, 0.5034934222078586430 ) ) ;
#141806=EDGE_CURVE ( 'NONE', #5998, #7325, #162888, .T. ) ;
#141817=APPLICATION_CONTEXT ( 'automotive_design' ) ;
#141842=LINE ( 'NONE', #160178, #101213 ) ;
#141848=ORIENTED_EDGE ( 'NONE', *, *, #192668, .F. ) ;
#141853=CARTESIAN_POINT ( 'NONE',  ( 1.001543065824772753E-15, -3.871874999522043836, 3.793834371823811669 ) ) ;
#141894=CARTESIAN_POINT ( 'NONE',  ( -1.782949938078044694, -3.499999999999999556, 2.093702347113241657 ) ) ;
#142067=ORIENTED_EDGE ( 'NONE', *, *, #111491, .T. ) ;
#142084=DIRECTION ( 'NONE',  ( -0.000000000000000000, 1.000000000000000000, -0.000000000000000000 ) ) ;
#142095=EDGE_CURVE ( 'NONE', #164595, #213437, #87750, .T. ) ;
#142115=CARTESIAN_POINT ( 'NONE',  ( -1.642778471874998480, -1.538541666188709245, 2.845375778867863303 ) ) ;
#142168=CARTESIAN_POINT ( 'NONE',  ( 0.000000000000000000, -1.684374999522041172, -3.793834371823813001 ) ) ;
#142262=CARTESIAN_POINT ( 'NONE',  ( 3.475000000000000533, -1.545833333333334503, -2.006292185433951047 ) ) ;
#142295=ADVANCED_FACE ( 'NONE', ( #59448 ), #152535, .T. ) ;
#142337=CARTESIAN_POINT ( 'NONE',  ( 1.642778471875001811, -3.142708332855375986, 2.845375778867859751 ) ) ;
#142356=CARTESIAN_POINT ( 'NONE',  ( -3.475000000000000533, -1.750000000000001554, 0.000000000000000000 ) ) ;
#142426=CARTESIAN_POINT ( 'NONE',  ( 3.475000000000000533, -1.210416665710750683, 2.006292185433948827 ) ) ;
#142435=DIRECTION ( 'NONE',  ( -3.491481338843133355E-15, 0.000000000000000000, -1.000000000000000000 ) ) ;
#142482=CARTESIAN_POINT ( 'NONE',  ( -1.737500000000000266, -2.858333333333334281, -3.009438278150923907 ) ) ;
#142643=VERTEX_POINT ( 'NONE', #170851 ) ;
#142658=CARTESIAN_POINT ( 'NONE',  ( 3.285556943750000070, -3.084374999522042415, 0.000000000000000000 ) ) ;
#142724=CARTESIAN_POINT ( 'NONE',  ( 1.642778471875001811, -0.6927083328553753638, 2.845375778867859751 ) ) ;
#142748=CARTESIAN_POINT ( 'NONE',  ( 0.000000000000000000, -1.600000000000000755, 0.000000000000000000 ) ) ;
#142758=EDGE_CURVE ( 'NONE', #160077, #16835, #23008, .T. ) ;
#142856=ADVANCED_FACE ( 'NONE', ( #159940, #12603 ), #31021, .T. ) ;
#142875=CARTESIAN_POINT ( 'NONE',  ( -1.642778471874998480, -1.101041666188708801, 2.845375778867863303 ) ) ;
#142914=CARTESIAN_POINT ( 'NONE',  ( -1.737500000000000266, -2.858333333333334281, -3.009438278150923907 ) ) ;
#142986=CARTESIAN_POINT ( 'NONE',  ( 0.000000000000000000, 0.9000000000000014655, 0.000000000000000000 ) ) ;
#142998=VERTEX_POINT ( 'NONE', #210808 ) ;
#143162=DIRECTION ( 'NONE',  ( 0.000000000000000000, -1.000000000000000000, 0.000000000000000000 ) ) ;
#143174=DIRECTION ( 'NONE',  ( -0.7613463080411786432, 0.000000000000000000, -0.6483454320283800199 ) ) ;
#143248=CARTESIAN_POINT ( 'NONE',  ( -3.285556943750000070, -1.596874999522043037, 0.000000000000000000 ) ) ;
#143336=CARTESIAN_POINT ( 'NONE',  ( 1.737499999999999378, -2.216666666666665453, -3.009438278150925683 ) ) ;
#143408=CARTESIAN_POINT ( 'NONE',  ( -1.642778471874998480, -3.201041666188710000, 2.845375778867863303 ) ) ;
#143427=CARTESIAN_POINT ( 'NONE',  ( 1.001543065824772753E-15, -0.9624999999999998002, 4.012584370867899430 ) ) ;
#143498=ORIENTED_EDGE ( 'NONE', *, *, #164027, .F. ) ;
#143501=CARTESIAN_POINT ( 'NONE',  ( 1.737499999999999378, -1.122916665710751882, -3.009438278150925683 ) ) ;
#143591=CARTESIAN_POINT ( 'NONE',  ( 0.000000000000000000, -0.8968749995220406390, -3.793834371823813001 ) ) ;
#143740=CARTESIAN_POINT ( 'NONE',  ( 0.000000000000000000, -2.996874999522043392, -3.793834371823813001 ) ) ;
#143801=CARTESIAN_POINT ( 'NONE',  ( 3.285556943749998737, -0.9552083328553737651, -1.896917185911906500 ) ) ;
#143947=CARTESIAN_POINT ( 'NONE',  ( -3.285556943749998737, -2.530208332855374831, 1.896917185911908499 ) ) ;
#143987=CARTESIAN_POINT ( 'NONE',  ( -3.475000000000000533, -1.399999999999998579, 0.000000000000000000 ) ) ;
#144011=CARTESIAN_POINT ( 'NONE',  ( -3.418820436464110379, -0.03388596222681408004, -0.09792497310439811364 ) ) ;
#144051=CARTESIAN_POINT ( 'NONE',  ( 3.285556943750000514, -1.101041666188710355, 1.896917185911906500 ) ) ;
#144145=CARTESIAN_POINT ( 'NONE',  ( -1.416814887940403000, 7.999555336178692855, 9.899480522462175358 ) ) ;
#144180=DIRECTION ( 'NONE',  ( -0.8660254037844397068, 0.4999999999999978906, 0.000000000000000000 ) ) ;
#144253=CARTESIAN_POINT ( 'NONE',  ( -1.642778471874998480, -1.451041666188708446, 2.845375778867863303 ) ) ;
#144321=CARTESIAN_POINT ( 'NONE',  ( 0.000000000000000000, -4.134374999522041350, -3.793834371823813001 ) ) ;
#144399=PLANE ( 'NONE',  #15973 ) ;
#144412=CARTESIAN_POINT ( 'NONE',  ( 0.000000000000000000, -0.7875000000000005329, -4.012584370867899430 ) ) ;
#144428=DIRECTION ( 'NONE',  ( 1.000000000000000000, 0.000000000000000000, -0.000000000000000000 ) ) ;
#144429=CARTESIAN_POINT ( 'NONE',  ( 5.510910596163088569E-16, 1.000000000000000888, 4.500000000000000000 ) ) ;
#144471=CARTESIAN_POINT ( 'NONE',  ( -1.685698123273788429, -1.500000000000000000, 1.979500400907064916 ) ) ;
#144472=CARTESIAN_POINT ( 'NONE',  ( -2.128168088883454642E-12, -3.089410100848593466, 3.428390338093493028 ) ) ;
#144480=CARTESIAN_POINT ( 'NONE',  ( 3.285556943749998737, -2.705208332855374209, -1.896917185911906722 ) ) ;
#144499=CARTESIAN_POINT ( 'NONE',  ( 3.475000000000000533, -1.545833333333334503, -2.006292185433951047 ) ) ;
#144519=PRESENTATION_STYLE_ASSIGNMENT (( #94682 ) ) ;
#144530=VERTEX_POINT ( 'NONE', #74708 ) ;
#144535=CARTESIAN_POINT ( 'NONE',  ( 0.000000000000000000, 2.000000000000001776, 0.000000000000000000 ) ) ;
#144554=CARTESIAN_POINT ( 'NONE',  ( 1.347111479062088405E-15, 6.999999999999999112, 11.00000000000000000 ) ) ;
#144570=CARTESIAN_POINT ( 'NONE',  ( 0.000000000000000000, -1.793749999044085275, -4.012584370867899430 ) ) ;
#144710=ORIENTED_EDGE ( 'NONE', *, *, #26563, .T. ) ;
#144734=CARTESIAN_POINT ( 'NONE',  ( 0.000000000000000000, -1.500000000000001332, 0.000000000000000000 ) ) ;
#144738=EDGE_CURVE ( 'NONE', #193157, #174327, #2818, .T. ) ;
#144740=CARTESIAN_POINT ( 'NONE',  ( 1.642778471875001811, -2.530208332855374387, 2.845375778867859751 ) ) ;
#144864=CARTESIAN_POINT ( 'NONE',  ( 1.642778471875000035, -1.276041666188710400, -2.845375778867859751 ) ) ;
#144886=PLANE ( 'NONE',  #36010 ) ;
#145005=CARTESIAN_POINT ( 'NONE',  ( -3.285556943749998737, -1.830208332855373987, 1.896917185911908499 ) ) ;
#145043=CARTESIAN_POINT ( 'NONE',  ( -1.737499999999997824, -1.691666666666667762, 3.009438278150925683 ) ) ;
#145070=CARTESIAN_POINT ( 'NONE',  ( -3.421885780383957520, -0.03116325934363972996, -0.1958776937478875768 ) ) ;
#145109=CARTESIAN_POINT ( 'NONE',  ( -3.285556943749998737, -0.5177083328553757635, 1.896917185911908499 ) ) ;
#145110=CARTESIAN_POINT ( 'NONE',  ( -2.986852260795243463, -3.064349949800098560, 1.744271399710988879 ) ) ;
#145114=LINE ( 'NONE', #147226, #23287 ) ;
#145134=ORIENTED_EDGE ( 'NONE', *, *, #126255, .F. ) ;
#145193=ORIENTED_EDGE ( 'NONE', *, *, #26563, .F. ) ;
#145235=LINE ( 'NONE', #25035, #116920 ) ;
#145254=CARTESIAN_POINT ( 'NONE',  ( -2.324088772396477673E-16, -1.093749999044084653, -3.475000000000000089 ) ) ;
#145279=CARTESIAN_POINT ( 'NONE',  ( -2.550000000000000266, 1.000000000000000888, -1.849324200890690717 ) ) ;
#145305=VERTEX_POINT ( 'NONE', #53085 ) ;
#145310=CARTESIAN_POINT ( 'NONE',  ( 1.001543065824772753E-15, -0.3718749995220430038, 3.793834371823811669 ) ) ;
#145323=CARTESIAN_POINT ( 'NONE',  ( -0.1532706334859310904, -0.8918953437966909981, -3.289477106180646704 ) ) ;
#145376=CARTESIAN_POINT ( 'NONE',  ( 0.2631197012187462270, -3.232243495192088645, 3.285556943749978753 ) ) ;
#145386=CARTESIAN_POINT ( 'NONE',  ( 3.285556943750000070, -3.871874999522042504, 0.000000000000000000 ) ) ;
#145401=CARTESIAN_POINT ( 'NONE',  ( -2.324088772396477673E-16, -2.887500000000000178, -3.475000000000000089 ) ) ;
#145435=CARTESIAN_POINT ( 'NONE',  ( -0.9311234436981480345, -1.471869630441517751, -3.475000000000001421 ) ) ;
#145468=DIRECTION ( 'NONE',  ( 0.000000000000000000, 0.000000000000000000, -1.000000000000000000 ) ) ;
#145481=CARTESIAN_POINT ( 'NONE',  ( 1.737499999999999378, -1.166666666666666519, -3.009438278150925683 ) ) ;
#145510=ORIENTED_EDGE ( 'NONE', *, *, #209784, .F. ) ;
#145566=CARTESIAN_POINT ( 'NONE',  ( -3.475000000000000533, -3.529166666666667229, -2.006292185433948827 ) ) ;
#145567=DIRECTION ( 'NONE',  ( 1.000000000000000000, 0.000000000000000000, -3.491481338843133355E-15 ) ) ;
#145613=DIRECTION ( 'NONE',  ( 1.000000000000000000, 0.000000000000000000, 0.000000000000000000 ) ) ;
#145623=LINE ( 'NONE', #144554, #84693 ) ;
#145642=CARTESIAN_POINT ( 'NONE',  ( 3.475000000000000533, -2.260416665710749839, 2.006292185433948827 ) ) ;
#145726=CARTESIAN_POINT ( 'NONE',  ( 3.285556943750000070, -0.2843749995220419269, 0.000000000000000000 ) ) ;
#145748=DIRECTION ( 'NONE',  ( -0.6483454320283800199, 0.000000000000000000, 0.7613463080411787542 ) ) ;
#145801=CARTESIAN_POINT ( 'NONE',  ( -3.285556943750000514, -3.026041666188709733, -1.896917185911906722 ) ) ;
#145820=ORIENTED_EDGE ( 'NONE', *, *, #121881, .F. ) ;
#145885=CARTESIAN_POINT ( 'NONE',  ( 4.408728476930470165E-16, -0.5000000000000004441, -3.599999999999999201 ) ) ;
#145922=CARTESIAN_POINT ( 'NONE',  ( 1.642778471875001811, -2.092708332855373943, 2.845375778867859751 ) ) ;
#145929=VERTEX_POINT ( 'NONE', #8596 ) ;
#146052=ORIENTED_EDGE ( 'NONE', *, *, #209026, .F. ) ;
#146058=CARTESIAN_POINT ( 'NONE',  ( 0.000000000000000000, -1.946874999522044014, -3.793834371823813001 ) ) ;
#146067=VECTOR ( 'NONE', #38891, 1000.000000000000000 ) ;
#146089=CIRCLE ( 'NONE', #156914, 2.500000000000000888 ) ;
#146099=CARTESIAN_POINT ( 'NONE',  ( 3.475000000000000533, -1.924999999999999600, 0.000000000000000000 ) ) ;
#146101=CARTESIAN_POINT ( 'NONE',  ( -3.285556943750000070, -2.646874999522041971, 0.000000000000000000 ) ) ;
#146250=DIRECTION ( 'NONE',  ( 0.000000000000000000, 0.000000000000000000, -1.000000000000000000 ) ) ;
#146317=CARTESIAN_POINT ( 'NONE',  ( 0.000000000000000000, 1.000000000000000888, -4.500000000000000000 ) ) ;
#146370=CARTESIAN_POINT ( 'NONE',  ( -0.3058401130151643388, -0.8903248038550014565, -3.276851707331648544 ) ) ;
#146432=CARTESIAN_POINT ( 'NONE',  ( -1.642778471874998480, -3.638541666188710444, 2.845375778867863303 ) ) ;
#146480=DIRECTION ( 'NONE',  ( -0.6483454320283799088, 0.000000000000000000, 0.7613463080411786432 ) ) ;
#146499=CARTESIAN_POINT ( 'NONE',  ( 0.9110743962804412899, -3.148497594347263284, -3.249005144921567556 ) ) ;
#146518=DIRECTION ( 'NONE',  ( 0.3162277660168373861, -0.9486832980505139901, 0.000000000000000000 ) ) ;
#146529=CARTESIAN_POINT ( 'NONE',  ( -1.737499999999997824, -3.441666666666665986, 3.009438278150925683 ) ) ;
#146583=VERTEX_POINT ( 'NONE', #100303 ) ;
#146637=CIRCLE ( 'NONE', #91290, 2.250000000000000444 ) ;
#146654=EDGE_CURVE ( 'NONE', #22347, #7256, #132304, .T. ) ;
#146689=CARTESIAN_POINT ( 'NONE',  ( 1.737499999999999378, -3.222916665710749751, -3.009438278150925683 ) ) ;
#146717=CIRCLE ( 'NONE', #22166, 2.750000000000000444 ) ;
#146777=CARTESIAN_POINT ( 'NONE',  ( -1.642778471874998480, -1.801041666188708090, 2.845375778867863303 ) ) ;
#146807=ORIENTED_EDGE ( 'NONE', *, *, #168859, .T. ) ;
#146830=ORIENTED_EDGE ( 'NONE', *, *, #151508, .F. ) ;
#146978=CARTESIAN_POINT ( 'NONE',  ( 1.642778471875001811, -1.392708332855374653, 2.845375778867859751 ) ) ;
#147015=CARTESIAN_POINT ( 'NONE',  ( 0.000000000000000000, 12.31951671548121219, 0.000000000000000000 ) ) ;
#147087=ORIENTED_EDGE ( 'NONE', *, *, #15780, .T. ) ;
#147116=CARTESIAN_POINT ( 'NONE',  ( 3.285556943750000070, -3.084374999522042415, 0.000000000000000000 ) ) ;
#147155=CARTESIAN_POINT ( 'NONE',  ( 3.475000000000000533, -2.304166666666668473, 2.006292185433948827 ) ) ;
#147157=CARTESIAN_POINT ( 'NONE',  ( 3.285556943750000070, -3.521874999522042859, 0.000000000000000000 ) ) ;
#147182=AXIS2_PLACEMENT_3D ( 'NONE', #131139, #45578, #178773 ) ;
#147222=CARTESIAN_POINT ( 'NONE',  ( -2.529473476623105288, -3.056106844972871439, 2.371225858872531234 ) ) ;
#147226=CARTESIAN_POINT ( 'NONE',  ( 1.499999999999963141, 8.500000000000000000, -9.886859966642596476 ) ) ;
#147339=VECTOR ( 'NONE', #29571, 1000.000000000000000 ) ;
#147351=DIRECTION ( 'NONE',  ( 1.000000000000000000, 0.000000000000000000, -3.706092522800016599E-15 ) ) ;
#147471=CARTESIAN_POINT ( 'NONE',  ( 0.5263138230170816279, -3.232243495192089089, 3.254015791315836736 ) ) ;
#147482=CARTESIAN_POINT ( 'NONE',  ( -1.642778471875000035, -3.755208332855374476, -2.845375778867859751 ) ) ;
#147562=CARTESIAN_POINT ( 'NONE',  ( -3.473320263822863740, -0.001938837310419191983, -0.06665759106987857729 ) ) ;
#147574=CARTESIAN_POINT ( 'NONE',  ( -1.737500000000000266, -2.508333333333334636, -3.009438278150923907 ) ) ;
#147610=CARTESIAN_POINT ( 'NONE',  ( 1.500000000000039524, 7.064371086078061523, 10.89416074946469770 ) ) ;
#147684=SURFACE_STYLE_FILL_AREA ( #192133 ) ;
#147737=CARTESIAN_POINT ( 'NONE',  ( 3.475000000000000533, -2.610416665710752593, 2.006292185433948827 ) ) ;
#147763=AXIS2_PLACEMENT_3D ( 'NONE', #71060, #41822, #6066 ) ;
#147824=CARTESIAN_POINT ( 'NONE',  ( 1.642778471875000035, -0.9260416661887073131, -2.845375778867859751 ) ) ;
#147918=ADVANCED_FACE ( 'NONE', ( #105966 ), #5177, .F. ) ;
#147958=EDGE_LOOP ( 'NONE', ( #39871, #107125, #96736 ) ) ;
#148028=CARTESIAN_POINT ( 'NONE',  ( 0.000000000000000000, -3.346874999522042149, -3.793834371823813001 ) ) ;
#148176=CARTESIAN_POINT ( 'NONE',  ( 1.001543065824772753E-15, -2.821874999522044458, 3.793834371823811669 ) ) ;
#148216=CARTESIAN_POINT ( 'NONE',  ( 3.475000000000000533, -2.974999999999998312, 0.000000000000000000 ) ) ;
#148218=CARTESIAN_POINT ( 'NONE',  ( 3.285556943750000514, -3.901041666188710177, 1.896917185911906500 ) ) ;
#148334=CARTESIAN_POINT ( 'NONE',  ( -3.280072367755099361, -0.8887487162373143290, 0.2896574332902090432 ) ) ;
#148426=CARTESIAN_POINT ( 'NONE',  ( 0.9311234436981455920, -2.696869630441517618, 3.475000000000003197 ) ) ;
#148448=CIRCLE ( 'NONE', #165755, 0.09999999999999999167 ) ;
#148469=ORIENTED_EDGE ( 'NONE', *, *, #151730, .F. ) ;
#148473=CARTESIAN_POINT ( 'NONE',  ( 1.001543065824772753E-15, -2.121874999522043836, 3.793834371823811669 ) ) ;
#148539=ORIENTED_EDGE ( 'NONE', *, *, #156570, .T. ) ;
#148589=CARTESIAN_POINT ( 'NONE',  ( -3.474999999999997868, -1.370833333333331350, 2.006292185433951047 ) ) ;
#148634=CARTESIAN_POINT ( 'NONE',  ( 1.001543065824772753E-15, -3.762499999999999289, 4.012584370867899430 ) ) ;
#148671=CARTESIAN_POINT ( 'NONE',  ( 0.000000000000000000, -1.600000000000000755, 0.000000000000000000 ) ) ;
#148694=CARTESIAN_POINT ( 'NONE',  ( -2.550000000000000266, -7.105553651663779391, -1.849324200890692271 ) ) ;
#148703=CARTESIAN_POINT ( 'NONE',  ( 0.9311234436981579154, -2.859380368602566502, -3.474999999999996536 ) ) ;
#148734=CARTESIAN_POINT ( 'NONE',  ( -3.285556943749998737, -0.5177083328553757635, 1.896917185911908499 ) ) ;
#148789=CARTESIAN_POINT ( 'NONE',  ( -3.475000000000000533, -2.785416665710751527, -2.006292185433948827 ) ) ;
#148876=CARTESIAN_POINT ( 'NONE',  ( 0.000000000000000000, -1.946874999522044014, -3.793834371823813001 ) ) ;
#149068=EDGE_LOOP ( 'NONE', ( #82755, #53168, #130093, #152991 ) ) ;
#149075=CARTESIAN_POINT ( 'NONE',  ( -3.285556943750000514, -3.288541666188709023, -1.896917185911906500 ) ) ;
#149150=TOROIDAL_SURFACE ( 'NONE', #204486, 3.399419719642636561, 0.1000000000000000056 ) ;
#149219=ORIENTED_EDGE ( 'NONE', *, *, #42175, .F. ) ;
#149225=CARTESIAN_POINT ( 'NONE',  ( -3.475000000000000533, -0.02916666666666653876, -2.006292185433948827 ) ) ;
#149268=CARTESIAN_POINT ( 'NONE',  ( 3.475000000000000533, -3.704166666666666163, 2.006292185433948827 ) ) ;
#149270=CARTESIAN_POINT ( 'NONE',  ( 1.642778471875001811, -2.880208332855377584, 2.845375778867859751 ) ) ;
#149336=CARTESIAN_POINT ( 'NONE',  ( 3.285556943749998737, -1.392708332855375764, -1.896917185911906500 ) ) ;
#149469=CARTESIAN_POINT ( 'NONE',  ( -1.432719062495390716, -3.042800438942089514, 3.165902886691621010 ) ) ;
#149482=CARTESIAN_POINT ( 'NONE',  ( -1.250000000000035749, 8.500000000000000000, -9.921567416492205638 ) ) ;
#149528=CARTESIAN_POINT ( 'NONE',  ( -3.285556943750000514, -3.288541666188709023, -1.896917185911906500 ) ) ;
#149560=CARTESIAN_POINT ( 'NONE',  ( 0.000000000000000000, -1.500000000000001332, 0.000000000000000000 ) ) ;
#149617=ORIENTED_EDGE ( 'NONE', *, *, #196844, .F. ) ;
#149621=CYLINDRICAL_SURFACE ( 'NONE', #160648, 11.00000000000000000 ) ;
#149669=CARTESIAN_POINT ( 'NONE',  ( 2.655622817947407732, -3.216694470489968705, 1.969572979196722473 ) ) ;
#149686=CARTESIAN_POINT ( 'NONE',  ( -1.499999999999946709, 7.750000000000000000, 15.75000000000000711 ) ) ;
#149696=CARTESIAN_POINT ( 'NONE',  ( 3.475000000000000533, -3.354166666666667851, 2.006292185433948827 ) ) ;
#149725=EDGE_LOOP ( 'NONE', ( #139997, #163207, #39722, #146052 ) ) ;
#149738=EDGE_CURVE ( 'NONE', #79131, #49812, #28659, .T. ) ;
#149791=CARTESIAN_POINT ( 'NONE',  ( -3.475000000000000533, -3.499999999999999556, 0.000000000000000000 ) ) ;
#149805=CARTESIAN_POINT ( 'NONE',  ( -3.285556943750000070, -0.1968749995220411830, 0.000000000000000000 ) ) ;
#149831=CARTESIAN_POINT ( 'NONE',  ( -3.285556943749998737, -1.830208332855373987, 1.896917185911908721 ) ) ;
#149867=CARTESIAN_POINT ( 'NONE',  ( -3.475000000000000533, -2.085416665710750905, -2.006292185433948827 ) ) ;
#149891=CARTESIAN_POINT ( 'NONE',  ( 0.9311234436981489226, -1.646869630441518240, 3.475000000000000533 ) ) ;
#149905=DIRECTION ( 'NONE',  ( -1.000000000000000000, 0.000000000000000000, 0.000000000000000000 ) ) ;
#149939=MECHANICAL_DESIGN_GEOMETRIC_PRESENTATION_REPRESENTATION('',(#187945),#200917);
#149953=CARTESIAN_POINT ( 'NONE',  ( 1.642778471875000035, -2.676041666188708756, -2.845375778867859751 ) ) ;
#150005=ORIENTED_EDGE ( 'NONE', *, *, #141317, .T. ) ;
#150047=ORIENTED_EDGE ( 'NONE', *, *, #57277, .T. ) ;
#150090=PLANE ( 'NONE',  #71494 ) ;
#150161=CARTESIAN_POINT ( 'NONE',  ( 1.642778471875001811, -3.492708332855375630, 2.845375778867859751 ) ) ;
#150167=CARTESIAN_POINT ( 'NONE',  ( 0.000000000000000000, 0.5000000000000004441, 0.000000000000000000 ) ) ;
#150213=CARTESIAN_POINT ( 'NONE',  ( 0.000000000000000000, 2.000000000000001776, 10.25000000000000000 ) ) ;
#150242=DIRECTION ( 'NONE',  ( 0.000000000000000000, 1.000000000000000000, 0.000000000000000000 ) ) ;
#150309=CARTESIAN_POINT ( 'NONE',  ( 0.000000000000000000, -0.5000000000000004441, 0.000000000000000000 ) ) ;
#150311=CARTESIAN_POINT ( 'NONE',  ( 3.475000000000000533, -0.5250000000000011324, 0.000000000000000000 ) ) ;
#150351=CARTESIAN_POINT ( 'NONE',  ( -3.474999999999998312, -3.820833333333332416, 2.006292185433951047 ) ) ;
#150353=CARTESIAN_POINT ( 'NONE',  ( -3.285556943749998737, -3.667708332855377673, 1.896917185911908499 ) ) ;
#150416=CARTESIAN_POINT ( 'NONE',  ( 1.001543065824772753E-15, -1.509374999522041794, 3.793834371823811669 ) ) ;
#150420=CARTESIAN_POINT ( 'NONE',  ( 0.9311234436981489226, -1.953119629485602804, 3.475000000000000533 ) ) ;
#150562=CARTESIAN_POINT ( 'NONE',  ( 0.000000000000000000, 6.999999999999999112, 0.000000000000000000 ) ) ;
#150568=ORIENTED_EDGE ( 'NONE', *, *, #155760, .F. ) ;
#150579=CARTESIAN_POINT ( 'NONE',  ( -3.263163593824906172, -0.8930720647284263736, 0.4328774883419782005 ) ) ;
#150608=CARTESIAN_POINT ( 'NONE',  ( 3.285556943750000514, -2.063541666188710266, 1.896917185911906500 ) ) ;
#150612=CARTESIAN_POINT ( 'NONE',  ( 4.255647627037052709E-16, 0.5000000000000004441, 3.475000000000000089 ) ) ;
#150659=EDGE_CURVE ( 'NONE', #5754, #153475, #99259, .T. ) ;
#150741=DIRECTION ( 'NONE',  ( -0.7613463080411786432, 0.000000000000000000, -0.6483454320283800199 ) ) ;
#150765=AXIS2_PLACEMENT_3D ( 'NONE', #195027, #206999, #43469 ) ;
#150775=CARTESIAN_POINT ( 'NONE',  ( 1.001543065824772753E-15, -2.362500000000001155, 4.012584370867899430 ) ) ;
#150841=LINE ( 'NONE', #52259, #134152 ) ;
#150881=CARTESIAN_POINT ( 'NONE',  ( 2.550000000000000266, 1.000000000000000888, -1.849324200890695824 ) ) ;
#150902=CARTESIAN_POINT ( 'NONE',  ( 1.001543065824772753E-15, -2.121874999522043392, 3.793834371823810780 ) ) ;
#150924=AXIS2_PLACEMENT_3D ( 'NONE', #129660, #112323, #63506 ) ;
#150938=CARTESIAN_POINT ( 'NONE',  ( -1.642778471874998480, -1.188541666188709600, 2.845375778867863303 ) ) ;
#150975=ORIENTED_EDGE ( 'NONE', *, *, #59704, .T. ) ;
#151024=CARTESIAN_POINT ( 'NONE',  ( 3.285556943749998737, -2.355208332855375453, -1.896917185911906500 ) ) ;
#151034=DIRECTION ( 'NONE',  ( 0.000000000000000000, 0.000000000000000000, 1.000000000000000000 ) ) ;
#151100=CARTESIAN_POINT ( 'NONE',  ( -0.4365480345679259022, -0.9795170267801369679, 3.437609648208244106 ) ) ;
#151225=CARTESIAN_POINT ( 'NONE',  ( -3.285556943750000070, -3.259374999522044014, 0.000000000000000000 ) ) ;
#151376=CARTESIAN_POINT ( 'NONE',  ( 0.000000000000000000, -3.346874999522042149, -3.793834371823813001 ) ) ;
#151416=CARTESIAN_POINT ( 'NONE',  ( 1.001543065824772753E-15, -3.762499999999999289, 4.012584370867899430 ) ) ;
#151418=CARTESIAN_POINT ( 'NONE',  ( -1.642778471874998480, -1.101041666188708801, 2.845375778867863303 ) ) ;
#151482=CARTESIAN_POINT ( 'NONE',  ( 3.285556943749998737, -2.092708332855377051, -1.896917185911906500 ) ) ;
#151508=EDGE_CURVE ( 'NONE', #152360, #104308, #152295, .T. ) ;
#151588=CARTESIAN_POINT ( 'NONE',  ( 4.255647627037052709E-16, 0.5000000000000004441, 3.475000000000000089 ) ) ;
#151647=CARTESIAN_POINT ( 'NONE',  ( 1.393942678861017859, 1.000000000000001332, -1.636894562288534472 ) ) ;
#151672=CARTESIAN_POINT ( 'NONE',  ( 3.285556943750000070, -2.034374999522043481, 0.000000000000000000 ) ) ;
#151730=EDGE_CURVE ( 'NONE', #135098, #79131, #172072, .T. ) ;
#151772=EDGE_CURVE ( 'NONE', #157888, #130259, #11448, .T. ) ;
#151823=AXIS2_PLACEMENT_3D ( 'NONE', #199204, #50851, #182974 ) ;
#151826=CARTESIAN_POINT ( 'NONE',  ( -3.432209171205097498, -0.01729076450818782182, -0.4009769568943012397 ) ) ;
#151934=FACE_OUTER_BOUND ( 'NONE', #28913, .T. ) ;
#151961=CARTESIAN_POINT ( 'NONE',  ( 1.642778471875001811, -2.442708332855377140, 2.845375778867859751 ) ) ;
#151965=TOROIDAL_SURFACE ( 'NONE', #103565, 2.149999999999999911, 0.1000000000000000056 ) ;
#151993=CARTESIAN_POINT ( 'NONE',  ( 0.000000000000000000, -4.243749999044082344, -4.012584370867899430 ) ) ;
#152082=CARTESIAN_POINT ( 'NONE',  ( -3.285556943749998737, -3.930208332855377407, 1.896917185911908499 ) ) ;
#152280=CARTESIAN_POINT ( 'NONE',  ( 3.285556943750000070, -3.434374999522042060, 0.000000000000000000 ) ) ;
#152290=ORIENTED_EDGE ( 'NONE', *, *, #82484, .F. ) ;
#152295=B_SPLINE_CURVE_WITH_KNOTS ( 'NONE', 3,
 ( #36986, #172337, #101996, #68403, #35920, #169124, #201598 ),
 .UNSPECIFIED., .F., .F.,
 ( 4, 3, 4 ),
 ( 0.001837494195021916864, 0.002395020826491697005, 0.002588355962777582134 ),
 .UNSPECIFIED. ) ;
#152303=CARTESIAN_POINT ( 'NONE',  ( 7.204675194429079505E-15, -1.443749999044083854, -3.475000000000000089 ) ) ;
#152310=AXIS2_PLACEMENT_3D ( 'NONE', #161769, #10154, #160688 ) ;
#152360=VERTEX_POINT ( 'NONE', #2363 ) ;
#152409=CARTESIAN_POINT ( 'NONE',  ( 0.000000000000000000, -2.034374999522043481, -3.793834371823813445 ) ) ;
#152433=CARTESIAN_POINT ( 'NONE',  ( -1.642778471875000035, -3.667708332855373676, -2.845375778867859751 ) ) ;
#152473=CARTESIAN_POINT ( 'NONE',  ( 1.737499999999999378, -2.916666666666668295, -3.009438278150925683 ) ) ;
#152475=CARTESIAN_POINT ( 'NONE',  ( 1.001543065824772753E-15, -1.421874999522042327, 3.793834371823811669 ) ) ;
#152512=LINE ( 'NONE', #165557, #101460 ) ;
#152515=ADVANCED_FACE ( 'NONE', ( #170225, #201632 ), #54356, .T. ) ;
#152533=CARTESIAN_POINT ( 'NONE',  ( -3.285556943750000514, -2.326041666188709112, -1.896917185911906500 ) ) ;
#152535=( BOUNDED_SURFACE ( )  B_SPLINE_SURFACE ( 1, 2, ( 
 ( #22660, #191565, #56260, #171063, #155895, #90907, #88771, #76754, #58389, #107201, #124545, #173225, #24805, #156971, #172148, #43229, #7483, #73565, #108275, #38942, #122418, #189451, #8560, #188376, #93044, #158039, #105025, #26936, #40014, #106125, #23740, #74640, #140746, #159086, #142875, #190502, #42160, #174296, #91981, #160154, #62633, #61581, #44284, #28015, #192632, #128793, #94113, #111469, #11752, #30150, #196906, #79955, #48546, #15998, #13877, #98348, #179604, #78882, #213142, #145005, #114664, #113601, #180658, #146058, #45350, #162289, #212071, #211011, #63710, #161222, #110405, #77826, #46411, #129867, #126668, #130914, #194774, #163358, #177475, #112527, #176409, #95173, #81029, #143947, #178540, #82083, #60507, #29089, #97299, #164414, #96239, #12809, #209943, #148176, #127749, #193706, #32283, #195851, #64772, #47491, #31225, #14933, #147116, #33336, #136196, #201151, #200090, #182781, #202214, #53868, #131952, #151376, #101544, #49592, #99418, #120001, #185978, #83147, #118928, #65805, #165473, #21330, #152433, #90376, #183854, #2945, #37611, #1877, #4012, #100471, #214178, #197963, #167613, #17068, #103692, #52789, #51739, #34399, #169741 ),
 ( #115716, #149225, #181706, #800, #66868, #184908, #133013, #199013, #50658, #70082, #116784, #35466, #69017, #135134, #166546, #18134, #86362, #84223, #150311, #67937, #19211, #134082, #117862, #36532, #85290, #102619, #168674, #20278, #192113, #207308, #12298, #125089, #191047, #143427, #29647, #57861, #158574, #43777, #206234, #128301, #193196, #140215, #110950, #8029, #124023, #74119, #107754, #76247, #176957, #78378, #41640, #175903, #160704, #144499, #173780, #10173, #157516, #189989, #25355, #91455, #142356, #9111, #58931, #75187, #126150, #210506, #27494, #62141, #112027, #109890, #194263, #61068, #174845, #94661, #26422, #45909, #209423, #178029, #93594, #141299, #159638, #11235, #92534, #77314, #42712, #108820, #208366, #59997, #127227, #44844, #156445, #28573, #198507, #212632, #31782, #161784, #130418, #116275, #211565, #114163, #51220, #95732, #64273, #132508, #199576, #180156, #196405, #195341, #183341, #117344, #63199, #13375, #79449, #49095, #129363, #17617, #82637, #81581, #48050, #83703, #149791, #145566, #32833, #197454, #46973, #113089, #1365, #67427, #179095, #291, #30717, #96800, #162849, #33889, #14427, #65304, #98910, #164962, #80517 ) ),
 .UNSPECIFIED., .F., .F., .T. ) 
 B_SPLINE_SURFACE_WITH_KNOTS ( ( 2, 2 ),
 ( 3, 2, 2, 2, 2, 2, 2, 2, 2, 2, 2, 2, 2, 2, 2, 2, 2, 2, 2, 2, 2, 2, 2, 2, 2, 2, 2, 2, 2, 2, 2, 2, 2, 2, 2, 2, 2, 2, 2, 2, 2, 2, 2, 2, 2, 2, 2, 2, 2, 2, 2, 2, 2, 2, 2, 2, 2, 2, 2, 2, 2, 2, 2, 2, 2, 2, 2, 2, 2, 3 ),
 ( 0.000000000000000000, 1.000000000000000000 ),
 ( 0.000000000000000000, 0.01388888888888888812, 0.02777777777777777624, 0.04166666666666666435, 0.05555555555555555247, 0.06944444444444444753, 0.08333333333333332871, 0.09722222222222222376, 0.1111111111111111049, 0.1250000000000000000, 0.1388888888888888951, 0.1527777777777777901, 0.1666666666666666574, 0.1805555555555555525, 0.1944444444444444475, 0.2083333333333333426, 0.2222222222222222099, 0.2361111111111111049, 0.2500000000000000000, 0.2638888888888888951, 0.2777777777777777901, 0.2916666666666666852, 0.3055555555555555802, 0.3194444444444444198, 0.3333333333333333148, 0.3472222222222222099, 0.3611111111111111049, 0.3750000000000000000, 0.3888888888888888951, 0.4027777777777777901, 0.4166666666666666852, 0.4305555555555555802, 0.4444444444444444198, 0.4583333333333333148, 0.4722222222222222099, 0.4861111111111111049, 0.5000000000000000000, 0.5138888888888888395, 0.5277777777777777901, 0.5416666666666666297, 0.5555555555555555802, 0.5694444444444444198, 0.5833333333333333703, 0.5972222222222222099, 0.6111111111111111605, 0.6250000000000000000, 0.6388888888888888395, 0.6527777777777777901, 0.6666666666666666297, 0.6805555555555555802, 0.6944444444444444198, 0.7083333333333333703, 0.7222222222222222099, 0.7361111111111111605, 0.7500000000000000000, 0.7638888888888888395, 0.7777777777777777901, 0.7916666666666666297, 0.8055555555555555802, 0.8194444444444444198, 0.8333333333333333703, 0.8472222222222222099, 0.8611111111111111605, 0.8750000000000000000, 0.8888888888888888395, 0.9027777777777777901, 0.9166666666666666297, 0.9305555555555555802, 0.9444444444444444198, 0.9523586252412667985 ),
 .UNSPECIFIED. ) 
 GEOMETRIC_REPRESENTATION_ITEM ( )  RATIONAL_B_SPLINE_SURFACE ( (
 ( 1.000000000000000000, 0.8660254037844387076, 1.000000000000000000, 0.8660254037844387076, 1.000000000000000000, 0.8660254037844387076, 1.000000000000000000, 0.8660254037844387076, 1.000000000000000000, 0.8660254037844387076, 1.000000000000000000, 0.8660254037844387076, 1.000000000000000000, 0.8660254037844387076, 1.000000000000000000, 0.8660254037844387076, 1.000000000000000000, 0.8660254037844387076, 1.000000000000000000, 0.8660254037844387076, 1.000000000000000000, 0.8660254037844387076, 1.000000000000000000, 0.8660254037844387076, 1.000000000000000000, 0.8660254037844387076, 1.000000000000000000, 0.8660254037844387076, 1.000000000000000000, 0.8660254037844387076, 1.000000000000000000, 0.8660254037844387076, 1.000000000000000000, 0.8660254037844387076, 1.000000000000000000, 0.8660254037844387076, 1.000000000000000000, 0.8660254037844387076, 1.000000000000000000, 0.8660254037844387076, 1.000000000000000000, 0.8660254037844387076, 1.000000000000000000, 0.8660254037844387076, 1.000000000000000000, 0.8660254037844387076, 1.000000000000000000, 0.8660254037844387076, 1.000000000000000000, 0.8660254037844387076, 1.000000000000000000, 0.8660254037844387076, 1.000000000000000000, 0.8660254037844387076, 1.000000000000000000, 0.8660254037844387076, 1.000000000000000000, 0.8660254037844387076, 1.000000000000000000, 0.8660254037844387076, 1.000000000000000000, 0.8660254037844387076, 1.000000000000000000, 0.8660254037844387076, 1.000000000000000000, 0.8660254037844387076, 1.000000000000000000, 0.8660254037844387076, 1.000000000000000000, 0.8660254037844387076, 1.000000000000000000, 0.8660254037844387076, 1.000000000000000000, 0.8660254037844387076, 1.000000000000000000, 0.8660254037844387076, 1.000000000000000000, 0.8660254037844387076, 1.000000000000000000, 0.8660254037844387076, 1.000000000000000000, 0.8660254037844387076, 1.000000000000000000, 0.8660254037844387076, 1.000000000000000000, 0.8660254037844387076, 1.000000000000000000, 0.8660254037844387076, 1.000000000000000000, 0.8660254037844387076, 1.000000000000000000, 0.8660254037844387076, 1.000000000000000000, 0.8660254037844387076, 1.000000000000000000, 0.8660254037844387076, 1.000000000000000000, 0.8660254037844387076, 1.000000000000000000, 0.8660254037844387076, 1.000000000000000000, 0.8660254037844387076, 1.000000000000000000, 0.8660254037844387076, 1.000000000000000000, 0.8660254037844387076, 1.000000000000000000, 0.8660254037844387076, 1.000000000000000000, 0.8660254037844387076, 1.000000000000000000, 0.8660254037844387076, 1.000000000000000000, 0.8660254037844387076, 1.000000000000000000, 0.8660254037844387076, 1.000000000000000000, 0.8660254037844387076, 1.000000000000000000, 0.8660254037844387076, 1.000000000000000000, 0.8660254037844387076, 1.000000000000000000, 0.8660254037844387076, 1.000000000000000000, 0.8660254037844387076, 1.000000000000000000, 0.8660254037844387076, 1.000000000000000000, 0.8660254037844387076, 1.000000000000000000, 0.8660254037844387076, 1.000000000000000000, 0.8660254037844387076, 1.000000000000000000, 0.8660254037844387076, 1.000000000000000000, 0.9236584592825519691, 0.9343189473637074638),
 ( 1.000000000000000000, 0.8660254037844387076, 1.000000000000000000, 0.8660254037844387076, 1.000000000000000000, 0.8660254037844387076, 1.000000000000000000, 0.8660254037844387076, 1.000000000000000000, 0.8660254037844387076, 1.000000000000000000, 0.8660254037844387076, 1.000000000000000000, 0.8660254037844387076, 1.000000000000000000, 0.8660254037844387076, 1.000000000000000000, 0.8660254037844387076, 1.000000000000000000, 0.8660254037844387076, 1.000000000000000000, 0.8660254037844387076, 1.000000000000000000, 0.8660254037844387076, 1.000000000000000000, 0.8660254037844387076, 1.000000000000000000, 0.8660254037844387076, 1.000000000000000000, 0.8660254037844387076, 1.000000000000000000, 0.8660254037844387076, 1.000000000000000000, 0.8660254037844387076, 1.000000000000000000, 0.8660254037844387076, 1.000000000000000000, 0.8660254037844387076, 1.000000000000000000, 0.8660254037844387076, 1.000000000000000000, 0.8660254037844387076, 1.000000000000000000, 0.8660254037844387076, 1.000000000000000000, 0.8660254037844387076, 1.000000000000000000, 0.8660254037844387076, 1.000000000000000000, 0.8660254037844387076, 1.000000000000000000, 0.8660254037844387076, 1.000000000000000000, 0.8660254037844387076, 1.000000000000000000, 0.8660254037844387076, 1.000000000000000000, 0.8660254037844387076, 1.000000000000000000, 0.8660254037844387076, 1.000000000000000000, 0.8660254037844387076, 1.000000000000000000, 0.8660254037844387076, 1.000000000000000000, 0.8660254037844387076, 1.000000000000000000, 0.8660254037844387076, 1.000000000000000000, 0.8660254037844387076, 1.000000000000000000, 0.8660254037844387076, 1.000000000000000000, 0.8660254037844387076, 1.000000000000000000, 0.8660254037844387076, 1.000000000000000000, 0.8660254037844387076, 1.000000000000000000, 0.8660254037844387076, 1.000000000000000000, 0.8660254037844387076, 1.000000000000000000, 0.8660254037844387076, 1.000000000000000000, 0.8660254037844387076, 1.000000000000000000, 0.8660254037844387076, 1.000000000000000000, 0.8660254037844387076, 1.000000000000000000, 0.8660254037844387076, 1.000000000000000000, 0.8660254037844387076, 1.000000000000000000, 0.8660254037844387076, 1.000000000000000000, 0.8660254037844387076, 1.000000000000000000, 0.8660254037844387076, 1.000000000000000000, 0.8660254037844387076, 1.000000000000000000, 0.8660254037844387076, 1.000000000000000000, 0.8660254037844387076, 1.000000000000000000, 0.8660254037844387076, 1.000000000000000000, 0.8660254037844387076, 1.000000000000000000, 0.8660254037844387076, 1.000000000000000000, 0.8660254037844387076, 1.000000000000000000, 0.8660254037844387076, 1.000000000000000000, 0.8660254037844387076, 1.000000000000000000, 0.8660254037844387076, 1.000000000000000000, 0.8660254037844387076, 1.000000000000000000, 0.8660254037844387076, 1.000000000000000000, 0.8660254037844387076, 1.000000000000000000, 0.8660254037844387076, 1.000000000000000000, 0.8660254037844387076, 1.000000000000000000, 0.8660254037844387076, 1.000000000000000000, 0.8660254037844387076, 1.000000000000000000, 0.8660254037844387076, 1.000000000000000000, 0.9236584592825519691, 0.9343189473637074638) ) ) 
 REPRESENTATION_ITEM ( '' )  SURFACE ( )  );
#152670=CARTESIAN_POINT ( 'NONE',  ( 0.9311234436981489226, -1.996869630441517662, 3.475000000000000533 ) ) ;
#152679=ORIENTED_EDGE ( 'NONE', *, *, #127070, .T. ) ;
#152721=CARTESIAN_POINT ( 'NONE',  ( -3.285556943749998737, -1.830208332855373987, 1.896917185911908499 ) ) ;
#152724=CARTESIAN_POINT ( 'NONE',  ( 1.224646799147353059E-15, 8.500000000000000000, 9.999999999999996447 ) ) ;
#152756=CARTESIAN_POINT ( 'NONE',  ( 1.394453263437886604E-15, -2.362500000000000266, 3.474999999999999645 ) ) ;
#152810=VECTOR ( 'NONE', #5855, 1000.000000000000000 ) ;
#152991=ORIENTED_EDGE ( 'NONE', *, *, #56061, .F. ) ;
#153020=CARTESIAN_POINT ( 'NONE',  ( 1.001543065824772753E-15, -1.071874999522044014, 3.793834371823810780 ) ) ;
#153048=CYLINDRICAL_SURFACE ( 'NONE', #139463, 3.475000000000000089 ) ;
#153052=CARTESIAN_POINT ( 'NONE',  ( 3.285556943750000514, -0.7510416661887079348, 1.896917185911906500 ) ) ;
#153076=DIRECTION ( 'NONE',  ( -0.000000000000000000, -1.000000000000000000, -0.000000000000000000 ) ) ;
#153141=CARTESIAN_POINT ( 'NONE',  ( 3.285556943750000070, -3.434374999522042060, 0.000000000000000000 ) ) ;
#153164=VERTEX_POINT ( 'NONE', #79120 ) ;
#153207=CARTESIAN_POINT ( 'NONE',  ( 1.255262969126037241E-15, 12.31951671548121219, -10.25000000000000000 ) ) ;
#153278=EDGE_CURVE ( 'NONE', #198335, #108029, #145235, .T. ) ;
#153456=ORIENTED_EDGE ( 'NONE', *, *, #26315, .F. ) ;
#153466=VERTEX_POINT ( 'NONE', #80187 ) ;
#153475=VERTEX_POINT ( 'NONE', #166774 ) ;
#153490=CARTESIAN_POINT ( 'NONE',  ( -3.599999999999999201, -0.5000000000000004441, 0.000000000000000000 ) ) ;
#153536=DIRECTION ( 'NONE',  ( 0.000000000000000000, 0.000000000000000000, -1.000000000000000000 ) ) ;
#153540=ORIENTED_EDGE ( 'NONE', *, *, #128141, .F. ) ;
#153547=CARTESIAN_POINT ( 'NONE',  ( -1.642778471874998480, -1.451041666188708446, 2.845375778867863303 ) ) ;
#153552=EDGE_CURVE ( 'NONE', #56590, #60185, #58106, .T. ) ;
#153610=CARTESIAN_POINT ( 'NONE',  ( 1.642778471875000035, -2.763541666188709556, -2.845375778867859751 ) ) ;
#153700=VECTOR ( 'NONE', #113295, 1000.000000000000000 ) ;
#153795=CARTESIAN_POINT ( 'NONE',  ( 1.737500000000001155, -0.2333333333333319215, 3.009438278150922130 ) ) ;
#153805=AXIS2_PLACEMENT_3D ( 'NONE', #17341, #65034, #68222 ) ;
#153833=CARTESIAN_POINT ( 'NONE',  ( 1.464175926609780964E-14, -2.537500000000001865, -3.475000000000000533 ) ) ;
#153857=AXIS2_PLACEMENT_3D ( 'NONE', #140426, #156650, #139337 ) ;
#153952=CARTESIAN_POINT ( 'NONE',  ( -3.419980048151579854, -0.02405074183678669250, -0.4062349772740375120 ) ) ;
#153986=VERTEX_POINT ( 'NONE', #138548 ) ;
#154053=ORIENTED_EDGE ( 'NONE', *, *, #10280, .F. ) ;
#154070=CARTESIAN_POINT ( 'NONE',  ( 3.285556943750000070, -2.471874999522040373, 0.000000000000000000 ) ) ;
#154092=CARTESIAN_POINT ( 'NONE',  ( -1.642778471875000035, -1.217708332855376607, -2.845375778867859751 ) ) ;
#154120=DIRECTION ( 'NONE',  ( 0.000000000000000000, 0.000000000000000000, 1.000000000000000000 ) ) ;
#154126=CARTESIAN_POINT ( 'NONE',  ( -3.285556943750000070, -0.1968749995220411830, 0.000000000000000000 ) ) ;
#154198=ADVANCED_FACE ( 'NONE', ( #125316 ), #157748, .T. ) ;
#154212=CARTESIAN_POINT ( 'NONE',  ( 3.285556943749998737, -3.755208332855373587, -1.896917185911906500 ) ) ;
#154251=CARTESIAN_POINT ( 'NONE',  ( -2.769334607113469904, -3.219464545100549469, 1.817267084746972516 ) ) ;
#154281=CARTESIAN_POINT ( 'NONE',  ( 1.782949938078045138, -1.500000000000001332, -2.093702347113241657 ) ) ;
#154464=LINE ( 'NONE', #201039, #131036 ) ;
#154548=CARTESIAN_POINT ( 'NONE',  ( -1.642778471875000035, -1.655208332855377051, -2.845375778867859751 ) ) ;
#154616=CARTESIAN_POINT ( 'NONE',  ( 3.285556943750000514, -1.363541666188709423, 1.896917185911906500 ) ) ;
#154673=CARTESIAN_POINT ( 'NONE',  ( -1.642778471875000035, -3.055208332855375630, -2.845375778867859751 ) ) ;
#154760=CARTESIAN_POINT ( 'NONE',  ( 3.018384101681789389, -0.9522666703177655734, 1.551720975324444973 ) ) ;
#154842=DIRECTION ( 'NONE',  ( 0.000000000000000000, -0.000000000000000000, -1.000000000000000000 ) ) ;
#154865=CARTESIAN_POINT ( 'NONE',  ( 1.642778471875000035, -3.726041666188707691, -2.845375778867859751 ) ) ;
#154947=ORIENTED_EDGE ( 'NONE', *, *, #58935, .T. ) ;
#155054=ORIENTED_EDGE ( 'NONE', *, *, #124593, .F. ) ;
#155075=CARTESIAN_POINT ( 'NONE',  ( -1.249999999999963807, 8.500000000000000000, 10.85702537530424827 ) ) ;
#155088=CARTESIAN_POINT ( 'NONE',  ( 0.000000000000000000, 0.5000000000000004441, 0.000000000000000000 ) ) ;
#155119=CARTESIAN_POINT ( 'NONE',  ( 0.9311234436981579154, -2.203130369558480961, -3.474999999999996536 ) ) ;
#155131=VERTEX_POINT ( 'NONE', #56773 ) ;
#155138=CARTESIAN_POINT ( 'NONE',  ( -1.642778471874998480, -2.588541666188707957, 2.845375778867863303 ) ) ;
#155185=CARTESIAN_POINT ( 'NONE',  ( -1.250000000000035749, 8.500000000000000000, -9.921567416492205638 ) ) ;
#155194=CARTESIAN_POINT ( 'NONE',  ( 1.642778471875000035, -1.013541666188708223, -2.845375778867859751 ) ) ;
#155249=CYLINDRICAL_SURFACE ( 'NONE', #159047, 4.500000000000000000 ) ;
#155281=CARTESIAN_POINT ( 'NONE',  ( 3.285556943750000070, -3.084374999522042415, 0.000000000000000000 ) ) ;
#155385=DIRECTION ( 'NONE',  ( -0.6483454320283789096, 0.000000000000000000, 0.7613463080411795314 ) ) ;
#155410=CARTESIAN_POINT ( 'NONE',  ( -1.499999999999964029, 8.500000000000000000, 9.886859966642596476 ) ) ;
#155491=CARTESIAN_POINT ( 'NONE',  ( 0.000000000000000000, 0.06547992991065912372, 0.000000000000000000 ) ) ;
#155537=ORIENTED_EDGE ( 'NONE', *, *, #48694, .T. ) ;
#155561=VERTEX_POINT ( 'NONE', #80419 ) ;
#155602=DIRECTION ( 'NONE',  ( -0.000000000000000000, -1.000000000000000000, -0.000000000000000000 ) ) ;
#155614=CARTESIAN_POINT ( 'NONE',  ( 3.285556943749998737, -1.392708332855375764, -1.896917185911906722 ) ) ;
#155681=CARTESIAN_POINT ( 'NONE',  ( 1.642778471875001811, -2.442708332855377140, 2.845375778867859751 ) ) ;
#155738=ADVANCED_FACE ( 'NONE', ( #32730 ), #196307, .F. ) ;
#155743=CARTESIAN_POINT ( 'NONE',  ( 3.285556943750000514, -3.551041666188707424, 1.896917185911906500 ) ) ;
#155760=EDGE_CURVE ( 'NONE', #24541, #85130, #16456, .T. ) ;
#155801=B_SPLINE_CURVE_WITH_KNOTS ( 'NONE', 3,
 ( #196353, #147610, #33838, #199523, #35969, #102047, #17563 ),
 .UNSPECIFIED., .F., .F.,
 ( 4, 3, 4 ),
 ( 0.002201685690204605809, 0.002395020826490573771, 0.002952547457960620625 ),
 .UNSPECIFIED. ) ;
#155889=ORIENTED_EDGE ( 'NONE', *, *, #156113, .T. ) ;
#155895=CARTESIAN_POINT ( 'NONE',  ( 1.642778471875000035, -0.2260416661887081069, -2.845375778867859751 ) ) ;
#155902=ORIENTED_EDGE ( 'NONE', *, *, #103930, .F. ) ;
#155910=CARTESIAN_POINT ( 'NONE',  ( 0.000000000000000000, -3.499999999999999556, 0.000000000000000000 ) ) ;
#155916=ADVANCED_FACE ( 'NONE', ( #60196 ), #72158, .F. ) ;
#155933=CARTESIAN_POINT ( 'NONE',  ( -3.475000000000000533, -0.7291666666666675178, -2.006292185433948827 ) ) ;
#155967=CARTESIAN_POINT ( 'NONE',  ( -0.9311234436981496998, -2.378130369558483004, 3.475000000000000977 ) ) ;
#156035=CARTESIAN_POINT ( 'NONE',  ( 0.000000000000000000, 12.31951671548121219, 10.25000000000000000 ) ) ;
#156113=EDGE_CURVE ( 'NONE', #55184, #206199, #105329, .T. ) ;
#156162=ORIENTED_EDGE ( 'NONE', *, *, #103675, .T. ) ;
#156181=DIRECTION ( 'NONE',  ( -0.000000000000000000, -1.000000000000000000, -0.000000000000000000 ) ) ;
#156214=CARTESIAN_POINT ( 'NONE',  ( 1.001543065824772753E-15, -0.8093749995220410609, 3.793834371823811669 ) ) ;
#156269=CARTESIAN_POINT ( 'NONE',  ( -3.285556943750000070, -1.946874999522042682, 0.000000000000000000 ) ) ;
#156309=ORIENTED_EDGE ( 'NONE', *, *, #172591, .F. ) ;
#156356=CARTESIAN_POINT ( 'NONE',  ( 1.001543065824772753E-15, -0.2624999999999988454, 4.012584370867899430 ) ) ;
#156445=CARTESIAN_POINT ( 'NONE',  ( 3.475000000000000533, -2.624999999999998668, 0.000000000000000000 ) ) ;
#156493=DIRECTION ( 'NONE',  ( 0.000000000000000000, 0.000000000000000000, -1.000000000000000000 ) ) ;
#156520=CARTESIAN_POINT ( 'NONE',  ( -3.475000000000000533, -1.035416665710751527, -2.006292185433948827 ) ) ;
#156537=AXIS2_PLACEMENT_3D ( 'NONE', #55855, #39604, #86223 ) ;
#156570=EDGE_CURVE ( 'NONE', #76889, #49812, #15698, .T. ) ;
#156619=CARTESIAN_POINT ( 'NONE',  ( 0.000000000000000000, -1.600000000000000755, 0.000000000000000000 ) ) ;
#156650=DIRECTION ( 'NONE',  ( 0.000000000000000000, -1.000000000000000000, -0.000000000000000000 ) ) ;
#156692=CARTESIAN_POINT ( 'NONE',  ( 3.285556943750000514, -1.801041666188707202, 1.896917185911906722 ) ) ;
#156760=CARTESIAN_POINT ( 'NONE',  ( -3.285556943750000070, -3.959374999522043304, 0.000000000000000000 ) ) ;
#156787=( BOUNDED_CURVE ( )  B_SPLINE_CURVE ( 2, ( #15360, #79319, #129234, #148589, #193054, #81453, #82502, #145435, #65174 ),
 .UNSPECIFIED., .F., .T. ) 
 B_SPLINE_CURVE_WITH_KNOTS ( ( 3, 2, 2, 2, 3 ),
 ( 0.3125000000000000000, 0.3194444444444444198, 0.3333333333333333148, 0.3472222222222222099, 0.3541666666666666852 ),
 .UNSPECIFIED. ) 
 CURVE ( )  GEOMETRIC_REPRESENTATION_ITEM ( )  RATIONAL_B_SPLINE_CURVE ( ( 0.9330127018922194093, 0.9330127018922194093, 1.000000000000000000, 0.8660254037844387076, 1.000000000000000000, 0.8660254037844387076, 1.000000000000000000, 0.9330127018922190762, 0.9330127018922194093 ) ) 
 REPRESENTATION_ITEM ( '' )  );
#156819=CARTESIAN_POINT ( 'NONE',  ( 3.285556943749998737, -0.2552083328553768071, -1.896917185911906500 ) ) ;
#156852=DIRECTION ( 'NONE',  ( -0.000000000000000000, 1.000000000000000000, -0.000000000000000000 ) ) ;
#156894=ORIENTED_EDGE ( 'NONE', *, *, #20202, .F. ) ;
#156903=CARTESIAN_POINT ( 'NONE',  ( 2.923734802589327941, -0.9258770086069849636, -1.625642389100794949 ) ) ;
#156914=AXIS2_PLACEMENT_3D ( 'NONE', #201637, #133509, #53285 ) ;
#156922=CYLINDRICAL_SURFACE ( 'NONE', #139101, 3.475000000000000089 ) ;
#156968=CARTESIAN_POINT ( 'NONE',  ( 0.000000000000000000, 5.999999999999998224, 0.000000000000000000 ) ) ;
#156971=CARTESIAN_POINT ( 'NONE',  ( -3.285556943750000514, -0.4885416661887091450, -1.896917185911906500 ) ) ;
#157009=CARTESIAN_POINT ( 'NONE',  ( 0.000000000000000000, -3.346874999522042149, -3.793834371823813001 ) ) ;
#157059=AXIS2_PLACEMENT_3D ( 'NONE', #157686, #90557, #110054 ) ;
#157174=CARTESIAN_POINT ( 'NONE',  ( -1.500000000000039524, 7.193113254731344774, -10.88798745763943110 ) ) ;
#157208=CYLINDRICAL_SURFACE ( 'NONE', #150765, 11.00000000000000000 ) ;
#157226=VERTEX_POINT ( 'NONE', #36807 ) ;
#157258=CARTESIAN_POINT ( 'NONE',  ( -1.556029036868112447, 0.4000000000000010214, 1.827231139298829632 ) ) ;
#157265=CARTESIAN_POINT ( 'NONE',  ( 1.718115394875207702, -1.500000000000000888, -2.017567716309123682 ) ) ;
#157280=CARTESIAN_POINT ( 'NONE',  ( -1.642778471875000035, -1.305208332855377407, -2.845375778867859751 ) ) ;
#157338=CARTESIAN_POINT ( 'NONE',  ( 3.285556943749998737, -2.442708332855375364, -1.896917185911906500 ) ) ;
#157352=CARTESIAN_POINT ( 'NONE',  ( 3.475000000000000533, -3.004166666666665542, 2.006292185433948827 ) ) ;
#157360=CARTESIAN_POINT ( 'NONE',  ( 2.687227643083427534E-13, -3.232243495192088201, 3.285556943749999625 ) ) ;
#157403=FACE_OUTER_BOUND ( 'NONE', #86219, .T. ) ;
#157429=CARTESIAN_POINT ( 'NONE',  ( -3.475000000000000533, -1.779166666666666785, -2.006292185433948827 ) ) ;
#157464=CARTESIAN_POINT ( 'NONE',  ( -2.128168088883454642E-12, -3.089410100848593466, 3.428390338093493028 ) ) ;
#157507=VECTOR ( 'NONE', #62885, 1000.000000000000000 ) ;
#157516=CARTESIAN_POINT ( 'NONE',  ( 1.737500000000001155, -1.633333333333333748, 3.009438278150922130 ) ) ;
#157592=CARTESIAN_POINT ( 'NONE',  ( -3.475000000000000533, -0.3354166657107504612, -2.006292185433948827 ) ) ;
#157686=CARTESIAN_POINT ( 'NONE',  ( 0.000000000000000000, 0.5000000000000004441, 0.000000000000000000 ) ) ;
#157748=CYLINDRICAL_SURFACE ( 'NONE', #27011, 11.00000000000000000 ) ;
#157825=CARTESIAN_POINT ( 'NONE',  ( -3.285556943750000514, -2.938541666188710266, -1.896917185911906500 ) ) ;
#157884=AXIS2_PLACEMENT_3D ( 'NONE', #114453, #195644, #177261 ) ;
#157888=VERTEX_POINT ( 'NONE', #60524 ) ;
#157891=CARTESIAN_POINT ( 'NONE',  ( 2.520460663003311730, -4.179124451297094645, -2.338645729556988240 ) ) ;
#157902=FACE_OUTER_BOUND ( 'NONE', #15337, .T. ) ;
#157974=CARTESIAN_POINT ( 'NONE',  ( 2.539911556248050761, -0.9198678134644189264, -2.162407946988131435 ) ) ;
#158039=CARTESIAN_POINT ( 'NONE',  ( -3.285556943750000514, -0.8385416661887076240, -1.896917185911906500 ) ) ;
#158040=CARTESIAN_POINT ( 'NONE',  ( 0.000000000000000000, 2.000000000000001776, 0.000000000000000000 ) ) ;
#158043=ADVANCED_FACE ( 'NONE', ( #45367 ), #97318, .T. ) ;
#158055=PLANE ( 'NONE',  #29331 ) ;
#158060=CARTESIAN_POINT ( 'NONE',  ( 0.000000000000000000, -0.5000000000000004441, 3.599999999999999201 ) ) ;
#158076=CARTESIAN_POINT ( 'NONE',  ( -3.285556943750000514, -3.638541666188706891, -1.896917185911906500 ) ) ;
#158261=CARTESIAN_POINT ( 'NONE',  ( -1.737500000000000266, -2.464583332377416447, -3.009438278150923907 ) ) ;
#158343=CARTESIAN_POINT ( 'NONE',  ( -1.642778471875000035, -2.355208332855376341, -2.845375778867859751 ) ) ;
#158393=CARTESIAN_POINT ( 'NONE',  ( 3.285556943750000514, -2.851041666188706802, 1.896917185911906500 ) ) ;
#158419=CIRCLE ( 'NONE', #203372, 11.00000000000000000 ) ;
#158484=CARTESIAN_POINT ( 'NONE',  ( -1.737499999999997824, -0.6416666666666653862, 3.009438278150925683 ) ) ;
#158574=CARTESIAN_POINT ( 'NONE',  ( -3.475000000000000533, -1.049999999999998934, 0.000000000000000000 ) ) ;
#158594=CARTESIAN_POINT ( 'NONE',  ( -1.737499999999997824, -1.297916665710750150, 3.009438278150925683 ) ) ;
#158647=CARTESIAN_POINT ( 'NONE',  ( -1.737500000000000266, -1.064583332377418090, -3.009438278150923907 ) ) ;
#158681=DIRECTION ( 'NONE',  ( -3.491481338843133750E-15, 0.000000000000000000, -1.000000000000000000 ) ) ;
#158734=CARTESIAN_POINT ( 'NONE',  ( -3.285556943750000514, -0.8385416661887076240, -1.896917185911906500 ) ) ;
#158816=CARTESIAN_POINT ( 'NONE',  ( 1.586093632162032474, -3.231214742333746059, 2.878102786335113183 ) ) ;
#158877=CARTESIAN_POINT ( 'NONE',  ( -3.285556943749998737, -3.930208332855377407, 1.896917185911908499 ) ) ;
#158941=CARTESIAN_POINT ( 'NONE',  ( 1.642778471875000035, -0.5760416661887077794, -2.845375778867859751 ) ) ;
#158948=DIRECTION ( 'NONE',  ( -0.000000000000000000, 1.000000000000000000, -0.000000000000000000 ) ) ;
#158988=CARTESIAN_POINT ( 'NONE',  ( -3.474999999999997868, -1.677083332377419245, 2.006292185433951047 ) ) ;
#159047=AXIS2_PLACEMENT_3D ( 'NONE', #40444, #6830, #120688 ) ;
#159086=CARTESIAN_POINT ( 'NONE',  ( 1.001543065824772753E-15, -1.071874999522043792, 3.793834371823811669 ) ) ;
#159087=DIRECTION ( 'NONE',  ( 0.000000000000000000, 0.000000000000000000, 1.000000000000000000 ) ) ;
#159099=DIRECTION ( 'NONE',  ( 1.000000000000000000, 0.000000000000000000, -3.491481338843133355E-15 ) ) ;
#159122=CARTESIAN_POINT ( 'NONE',  ( -3.475000000000000533, -2.450000000000000622, 0.000000000000000000 ) ) ;
#159261=ORIENTED_EDGE ( 'NONE', *, *, #80012, .T. ) ;
#159379=CARTESIAN_POINT ( 'NONE',  ( -1.642778471874998480, -0.7510416661887092671, 2.845375778867863303 ) ) ;
#159386=ORIENTED_EDGE ( 'NONE', *, *, #156570, .F. ) ;
#159392=CARTESIAN_POINT ( 'NONE',  ( -3.285556943750000514, -0.1385416661887106660, -1.896917185911906500 ) ) ;
#159449=CARTESIAN_POINT ( 'NONE',  ( -1.642778471875000035, -3.055208332855375630, -2.845375778867859751 ) ) ;
#159531=VECTOR ( 'NONE', #34812, 1000.000000000000000 ) ;
#159534=EDGE_LOOP ( 'NONE', ( #4262, #203247, #29545, #90259 ) ) ;
#159543=CARTESIAN_POINT ( 'NONE',  ( -3.475000000000000533, -0.6999999999999992895, 0.000000000000000000 ) ) ;
#159593=EDGE_LOOP ( 'NONE', ( #153456, #199278, #109014, #13210 ) ) ;
#159596=ORIENTED_EDGE ( 'NONE', *, *, #22298, .F. ) ;
#159615=AXIS2_PLACEMENT_3D ( 'NONE', #24780, #74613, #129586 ) ;
#159638=CARTESIAN_POINT ( 'NONE',  ( 1.737500000000001155, -2.333333333333333037, 3.009438278150922130 ) ) ;
#159708=CARTESIAN_POINT ( 'NONE',  ( 0.000000000000000000, -1.093749999044084431, -4.012584370867899430 ) ) ;
#159764=CARTESIAN_POINT ( 'NONE',  ( -2.324088772396477673E-16, -2.887500000000000178, -3.475000000000000089 ) ) ;
#159826=EDGE_CURVE ( 'NONE', #65209, #157888, #13765, .T. ) ;
#159836=DIRECTION ( 'NONE',  ( 0.000000000000000000, -1.000000000000000000, 0.000000000000000000 ) ) ;
#159877=CARTESIAN_POINT ( 'NONE',  ( 0.000000000000000000, -3.084374999522043304, -3.793834371823813445 ) ) ;
#159940=FACE_BOUND ( 'NONE', #42903, .T. ) ;
#159942=CARTESIAN_POINT ( 'NONE',  ( -3.285556943750000070, -3.609374999522043659, 0.000000000000000000 ) ) ;
#159977=( BOUNDED_CURVE ( )  B_SPLINE_CURVE ( 2, ( #37588, #123211, #169718, #137243, #168650, #20254, #5051, #90632, #40812, #184884, #23452, #71127, #187028, #103670, #21307, #87415, #38662, #140468, #104740, #155614, #106920, #170787, #22378, #72197, #172944, #39726, #88489, #102593, #154548, #204320, #105832, #3989, #55978, #156692, #36509, #24522, #7199, #206481, #58111, #73272, #86338, #152409, #122131, #139375, #205406, #57045, #176143, #162025, #111196, #42955, #95971, #125328, #27743, #78615, #210750, #177200, #41887, #25595, #144740, #109065, #62373, #175081, #79689, #26667, #76484, #93838, #28815, #127473, #209669, #141541, #128535, #59168, #10412, #61312, #110132, #145801, #29887, #159877, #94899, #193444, #45087, #126395, #112263, #158816, #191289 ),
 .UNSPECIFIED., .F., .T. ) 
 B_SPLINE_CURVE_WITH_KNOTS ( ( 3, 2, 2, 2, 2, 2, 2, 2, 2, 2, 2, 2, 2, 2, 2, 2, 2, 2, 2, 2, 2, 2, 2, 2, 2, 2, 2, 2, 2, 2, 2, 2, 2, 2, 2, 2, 2, 2, 2, 2, 2, 2, 3 ),
 ( 0.1645590526585348767, 0.1666666666666666574, 0.1805555555555555525, 0.1944444444444444475, 0.2083333333333333426, 0.2222222222222222099, 0.2361111111111111049, 0.2500000000000000000, 0.2638888888888888951, 0.2777777777777777901, 0.2916666666666666852, 0.3055555555555555802, 0.3194444444444444198, 0.3333333333333333148, 0.3472222222222222099, 0.3611111111111111049, 0.3750000000000000000, 0.3888888888888888951, 0.4027777777777777901, 0.4166666666666666852, 0.4305555555555555802, 0.4444444444444444198, 0.4583333333333333148, 0.4722222222222222099, 0.4861111111111111049, 0.5000000000000000000, 0.5138888888888888395, 0.5277777777777777901, 0.5416666666666666297, 0.5555555555555555802, 0.5694444444444444198, 0.5833333333333333703, 0.5972222222222222099, 0.6111111111111111605, 0.6250000000000000000, 0.6388888888888888395, 0.6527777777777777901, 0.6666666666666666297, 0.6805555555555555802, 0.6944444444444444198, 0.7083333333333333703, 0.7222222222222222099, 0.7227726656456107124 ),
 .UNSPECIFIED. ) 
 CURVE ( )  GEOMETRIC_REPRESENTATION_ITEM ( )  RATIONAL_B_SPLINE_CURVE ( ( 0.9655093951251874085, 0.9796695950283244025, 1.000000000000000000, 0.8660254037844387076, 1.000000000000000000, 0.8660254037844387076, 1.000000000000000000, 0.8660254037844387076, 1.000000000000000000, 0.8660254037844387076, 1.000000000000000000, 0.8660254037844387076, 1.000000000000000000, 0.8660254037844387076, 1.000000000000000000, 0.8660254037844387076, 1.000000000000000000, 0.8660254037844387076, 1.000000000000000000, 0.8660254037844387076, 1.000000000000000000, 0.8660254037844387076, 1.000000000000000000, 0.8660254037844387076, 1.000000000000000000, 0.8660254037844387076, 1.000000000000000000, 0.8660254037844387076, 1.000000000000000000, 0.8660254037844387076, 1.000000000000000000, 0.8660254037844387076, 1.000000000000000000, 0.8660254037844387076, 1.000000000000000000, 0.8660254037844387076, 1.000000000000000000, 0.8660254037844387076, 1.000000000000000000, 0.8660254037844387076, 1.000000000000000000, 0.8660254037844387076, 1.000000000000000000, 0.8660254037844387076, 1.000000000000000000, 0.8660254037844387076, 1.000000000000000000, 0.8660254037844387076, 1.000000000000000000, 0.8660254037844387076, 1.000000000000000000, 0.8660254037844387076, 1.000000000000000000, 0.8660254037844387076, 1.000000000000000000, 0.8660254037844387076, 1.000000000000000000, 0.8660254037844387076, 1.000000000000000000, 0.8660254037844387076, 1.000000000000000000, 0.8660254037844387076, 1.000000000000000000, 0.8660254037844387076, 1.000000000000000000, 0.8660254037844387076, 1.000000000000000000, 0.8660254037844387076, 1.000000000000000000, 0.8660254037844387076, 1.000000000000000000, 0.8660254037844387076, 1.000000000000000000, 0.8660254037844387076, 1.000000000000000000, 0.8660254037844387076, 1.000000000000000000, 0.8660254037844387076, 1.000000000000000000, 0.8660254037844387076, 1.000000000000000000, 0.8660254037844387076, 1.000000000000000000, 0.9946903286520650811, 0.9898015223131609863 ) ) 
 REPRESENTATION_ITEM ( '' )  );
#160005=CARTESIAN_POINT ( 'NONE',  ( 0.000000000000000000, -1.596874999522041705, -3.793834371823813001 ) ) ;
#160077=VERTEX_POINT ( 'NONE', #146317 ) ;
#160100=DIRECTION ( 'NONE',  ( 0.000000000000000000, 0.000000000000000000, -1.000000000000000000 ) ) ;
#160154=CARTESIAN_POINT ( 'NONE',  ( 0.000000000000000000, -1.246874999522042948, -3.793834371823813001 ) ) ;
#160178=CARTESIAN_POINT ( 'NONE',  ( 0.000000000000000000, 6.999999999999999112, -11.00000000000000000 ) ) ;
#160189=CARTESIAN_POINT ( 'NONE',  ( 3.475000000000000533, -1.254166666666665098, 2.006292185433948827 ) ) ;
#160207=UNCERTAINTY_MEASURE_WITH_UNIT (LENGTH_MEASURE( 1.000000000000000082E-05 ), #179115, 'distance_accuracy_value', 'NONE');
#160248=CARTESIAN_POINT ( 'NONE',  ( 0.000000000000000000, 0.5000000000000004441, -3.475000000000000089 ) ) ;
#160252=CARTESIAN_POINT ( 'NONE',  ( 3.285556943750000070, -1.071874999522042016, 0.000000000000000000 ) ) ;
#160253=CARTESIAN_POINT ( 'NONE',  ( -3.257807097882708725, -3.093939727723714839, -1.071007828276776319 ) ) ;
#160448=CARTESIAN_POINT ( 'NONE',  ( 3.285556943749998737, -0.6052083328553753416, -1.896917185911906500 ) ) ;
#160518=CARTESIAN_POINT ( 'NONE',  ( 3.285556943750000070, -2.471874999522040373, 0.000000000000000000 ) ) ;
#160528=VERTEX_POINT ( 'NONE', #213128 ) ;
#160613=CARTESIAN_POINT ( 'NONE',  ( 3.475000000000000533, -1.195833333333332194, -2.006292185433951047 ) ) ;
#160648=AXIS2_PLACEMENT_3D ( 'NONE', #201534, #98743, #67265 ) ;
#160678=PRODUCT_DEFINITION ( 'UNKNOWN', '', #118085, #72461 ) ;
#160686=CARTESIAN_POINT ( 'NONE',  ( 0.000000000000000000, -2.646874999522041083, -3.793834371823813445 ) ) ;
#160688=DIRECTION ( 'NONE',  ( 0.000000000000000000, 0.000000000000000000, 1.000000000000000000 ) ) ;
#160704=CARTESIAN_POINT ( 'NONE',  ( 1.737499999999999378, -1.516666666666666163, -3.009438278150925683 ) ) ;
#160779=CARTESIAN_POINT ( 'NONE',  ( 1.737500000000001155, -1.239583332377419689, 3.009438278150922130 ) ) ;
#160868=CARTESIAN_POINT ( 'NONE',  ( -1.642778471875000035, -0.8677083328553769626, -2.845375778867859751 ) ) ;
#160969=EDGE_LOOP ( 'NONE', ( #26236, #77156, #85669, #201069 ) ) ;
#161067=CARTESIAN_POINT ( 'NONE',  ( 1.500000000000035971, 6.999999999999999112, 9.886859966642587594 ) ) ;
#161075=CARTESIAN_POINT ( 'NONE',  ( -3.285556943749998737, -1.130208332855377140, 1.896917185911908499 ) ) ;
#161082=ORIENTED_EDGE ( 'NONE', *, *, #65049, .F. ) ;
#161087=CARTESIAN_POINT ( 'NONE',  ( 1.255262969126037241E-15, 2.999999999999999112, -10.25000000000000000 ) ) ;
#161222=CARTESIAN_POINT ( 'NONE',  ( 1.001543065824772753E-15, -2.121874999522043836, 3.793834371823811669 ) ) ;
#161237=ADVANCED_FACE ( 'NONE', ( #13611 ), #12539, .F. ) ;
#161260=CARTESIAN_POINT ( 'NONE',  ( 0.000000000000000000, -1.137499999999999067, -4.012584370867899430 ) ) ;
#161266=DIRECTION ( 'NONE',  ( 1.000000000000000000, 0.000000000000000000, 0.000000000000000000 ) ) ;
#161325=LINE ( 'NONE', #160248, #1653 ) ;
#161329=CARTESIAN_POINT ( 'NONE',  ( -3.285556943749998737, -0.8677083328553740760, 1.896917185911908499 ) ) ;
#161330=CARTESIAN_POINT ( 'NONE',  ( -2.886704779471910953, -3.062285525734984137, 1.909201817158099335 ) ) ;
#161399=ORIENTED_EDGE ( 'NONE', *, *, #122422, .T. ) ;
#161564=PLANE ( 'NONE',  #22158 ) ;
#161603=CARTESIAN_POINT ( 'NONE',  ( -3.285556943749998737, -4.017708332855375986, 1.896917185911908499 ) ) ;
#161651=CYLINDRICAL_SURFACE ( 'NONE', #93841, 9.999999999999998224 ) ;
#161683=CARTESIAN_POINT ( 'NONE',  ( 1.500000000000035971, 8.500000000000000000, 9.886859966642587594 ) ) ;
#161687=CIRCLE ( 'NONE', #2526, 0.4999999999999995559 ) ;
#161697=CARTESIAN_POINT ( 'NONE',  ( -3.475000000000000533, -2.100000000000000977, 0.000000000000000000 ) ) ;
#161705=EDGE_CURVE ( 'NONE', #31992, #93052, #202837, .T. ) ;
#161714=DIRECTION ( 'NONE',  ( 0.000000000000000000, -0.000000000000000000, 1.000000000000000000 ) ) ;
#161769=CARTESIAN_POINT ( 'NONE',  ( 0.000000000000000000, -3.517800438942085606, 0.000000000000000000 ) ) ;
#161784=CARTESIAN_POINT ( 'NONE',  ( -3.474999999999998312, -2.770833333333333037, 2.006292185433951047 ) ) ;
#161809=AXIS2_PLACEMENT_3D ( 'NONE', #135651, #103143, #134608 ) ;
#161858=CARTESIAN_POINT ( 'NONE',  ( -1.737499999999997824, -1.997916665710752770, 3.009438278150925683 ) ) ;
#161905=ORIENTED_EDGE ( 'NONE', *, *, #14538, .T. ) ;
#161916=CARTESIAN_POINT ( 'NONE',  ( -1.737499999999997824, -2.741666666666666696, 3.009438278150925683 ) ) ;
#161945=CARTESIAN_POINT ( 'NONE',  ( 1.642778471875000035, -0.2260416661887081069, -2.845375778867859751 ) ) ;
#162010=ORIENTED_EDGE ( 'NONE', *, *, #141317, .F. ) ;
#162025=CARTESIAN_POINT ( 'NONE',  ( 1.001543065824772753E-15, -2.209374999522042859, 3.793834371823810780 ) ) ;
#162144=ADVANCED_FACE ( 'NONE', ( #95715 ), #124726, .T. ) ;
#162150=CARTESIAN_POINT ( 'NONE',  ( -3.285556943750000514, -1.888541666188711110, -1.896917185911906500 ) ) ;
#162221=ORIENTED_EDGE ( 'NONE', *, *, #2058, .F. ) ;
#162289=CARTESIAN_POINT ( 'NONE',  ( 3.285556943749998737, -2.005208332855377140, -1.896917185911906500 ) ) ;
#162329=CARTESIAN_POINT ( 'NONE',  ( 1.001543065824772753E-15, -2.012499999999999289, 4.012584370867899430 ) ) ;
#162400=CARTESIAN_POINT ( 'NONE',  ( -3.285556943750000070, -0.1968749995220411830, 0.000000000000000000 ) ) ;
#162401=CARTESIAN_POINT ( 'NONE',  ( -1.325546123766559337, -3.124052913013680488, -3.130165297716357209 ) ) ;
#162486=AXIS2_PLACEMENT_3D ( 'NONE', #103890, #120205, #73504 ) ;
#162516=ORIENTED_EDGE ( 'NONE', *, *, #75988, .F. ) ;
#162592=CARTESIAN_POINT ( 'NONE',  ( 3.285556943750000070, -0.2843749995220419269, 0.000000000000000000 ) ) ;
#162654=CARTESIAN_POINT ( 'NONE',  ( 2.687227643083427534E-13, -3.232243495192088201, 3.285556943749999625 ) ) ;
#162667=CARTESIAN_POINT ( 'NONE',  ( -1.642778471874998480, -3.988541666188710089, 2.845375778867863303 ) ) ;
#162717=CARTESIAN_POINT ( 'NONE',  ( 0.000000000000000000, -1.600000000000000755, 0.000000000000000000 ) ) ;
#162721=DIRECTION ( 'NONE',  ( 0.000000000000000000, 1.000000000000000000, 0.000000000000000000 ) ) ;
#162832=CARTESIAN_POINT ( 'NONE',  ( 3.475000000000000533, -2.902083332377417779, -2.006292185433951047 ) ) ;
#162849=CARTESIAN_POINT ( 'NONE',  ( -3.475000000000000533, -3.849999999999999201, 0.000000000000000000 ) ) ;
#162888=LINE ( 'NONE', #86683, #199269 ) ;
#162921=CARTESIAN_POINT ( 'NONE',  ( 3.475000000000000533, -3.310416665710749218, 2.006292185433948827 ) ) ;
#163007=CARTESIAN_POINT ( 'NONE',  ( 3.285556943750000514, -0.6635416661887083567, 1.896917185911906500 ) ) ;
#163080=( BOUNDED_CURVE ( )  B_SPLINE_CURVE ( 2, ( #112376, #113446, #50503, #46258, #166380, #13726, #164258, #63557, #66706 ),
 .UNSPECIFIED., .F., .T. ) 
 B_SPLINE_CURVE_WITH_KNOTS ( ( 3, 2, 2, 2, 3 ),
 ( 0.5625000000000000000, 0.5694444444444444198, 0.5833333333333333703, 0.5972222222222222099, 0.6041666666666667407 ),
 .UNSPECIFIED. ) 
 CURVE ( )  GEOMETRIC_REPRESENTATION_ITEM ( )  RATIONAL_B_SPLINE_CURVE ( ( 0.9330127018922194093, 0.9330127018922194093, 1.000000000000000000, 0.8660254037844387076, 1.000000000000000000, 0.8660254037844387076, 1.000000000000000000, 0.9330127018922187432, 0.9330127018922192983 ) ) 
 REPRESENTATION_ITEM ( '' )  );
#163207=ORIENTED_EDGE ( 'NONE', *, *, #97858, .T. ) ;
#163215=CARTESIAN_POINT ( 'NONE',  ( 0.000000000000000000, -2.296874999522042327, -3.793834371823813001 ) ) ;
#163358=CARTESIAN_POINT ( 'NONE',  ( 3.285556943749998737, -2.355208332855375453, -1.896917185911906500 ) ) ;
#163398=CARTESIAN_POINT ( 'NONE',  ( 1.737499999999999378, -1.866666666666665808, -3.009438278150925683 ) ) ;
#163400=CARTESIAN_POINT ( 'NONE',  ( -3.285556943750000070, -3.696874999522044458, 0.000000000000000000 ) ) ;
#163441=CARTESIAN_POINT ( 'NONE',  ( -2.549999999999999378, 2.499999999999998668, 1.849324200890692271 ) ) ;
#163463=CARTESIAN_POINT ( 'NONE',  ( -3.285556943750000070, -0.8968749995220438587, 0.000000000000000000 ) ) ;
#163624=ORIENTED_EDGE ( 'NONE', *, *, #209595, .T. ) ;
#163659=CARTESIAN_POINT ( 'NONE',  ( -3.285556943749998737, -0.7802083328553744979, 1.896917185911908499 ) ) ;
#163733=CIRCLE ( 'NONE', #84089, 10.25000000000000000 ) ;
#163750=FACE_OUTER_BOUND ( 'NONE', #207255, .T. ) ;
#163795=AXIS2_PLACEMENT_3D ( 'NONE', #144535, #198544, #131488 ) ;
#163815=CARTESIAN_POINT ( 'NONE',  ( -3.423013188325464640, -0.02164107303108744884, -0.4185776113819570377 ) ) ;
#163827=CARTESIAN_POINT ( 'NONE',  ( -3.474999999999998312, -2.770833333333333037, 2.006292185433951047 ) ) ;
#163844=CARTESIAN_POINT ( 'NONE',  ( 0.000000000000000000, 0.5999999999999998668, 0.000000000000000000 ) ) ;
#163953=CARTESIAN_POINT ( 'NONE',  ( -3.475000000000000533, -1.006249999044084298, 0.000000000000000000 ) ) ;
#163962=CARTESIAN_POINT ( 'NONE',  ( -3.599999999999999201, -0.5000000000000004441, 0.000000000000000000 ) ) ;
#163988=CARTESIAN_POINT ( 'NONE',  ( 1.737499999999999378, -3.572916665710752948, -3.009438278150925683 ) ) ;
#164027=EDGE_CURVE ( 'NONE', #206199, #55184, #118046, .T. ) ;
#164075=CARTESIAN_POINT ( 'NONE',  ( 3.285556943750000070, -1.334374999522040861, 0.000000000000000000 ) ) ;
#164258=CARTESIAN_POINT ( 'NONE',  ( -1.737500000000000266, -2.814583332377419644, -3.009438278150923907 ) ) ;
#164266=ORIENTED_EDGE ( 'NONE', *, *, #15780, .F. ) ;
#164269=CARTESIAN_POINT ( 'NONE',  ( 1.001543065824772753E-15, -1.771874999522040861, 3.793834371823811669 ) ) ;
#164308=CARTESIAN_POINT ( 'NONE',  ( 0.000000000000000000, 1.000000000000000888, 0.000000000000000000 ) ) ;
#164317=DIRECTION ( 'NONE',  ( 0.000000000000000000, 0.000000000000000000, -1.000000000000000000 ) ) ;
#164320=( BOUNDED_CURVE ( )  B_SPLINE_CURVE ( 2, ( #179078, #148703, #164944, #162832, #14410, #16536, #80500, #130398, #48031 ),
 .UNSPECIFIED., .F., .T. ) 
 B_SPLINE_CURVE_WITH_KNOTS ( ( 3, 2, 2, 2, 3 ),
 ( 0.6041666666666667407, 0.6111111111111111605, 0.6250000000000000000, 0.6388888888888888395, 0.6458333333333333703 ),
 .UNSPECIFIED. ) 
 CURVE ( )  GEOMETRIC_REPRESENTATION_ITEM ( )  RATIONAL_B_SPLINE_CURVE ( ( 0.9330127018922192983, 0.9330127018922198534, 1.000000000000000000, 0.8660254037844387076, 1.000000000000000000, 0.8660254037844387076, 1.000000000000000000, 0.9330127018922187432, 0.9330127018922192983 ) ) 
 REPRESENTATION_ITEM ( '' )  );
#164412=DIRECTION ( 'NONE',  ( 0.000000000000000000, 0.000000000000000000, 1.000000000000000000 ) ) ;
#164414=CARTESIAN_POINT ( 'NONE',  ( 3.285556943749998737, -2.705208332855374209, -1.896917185911906500 ) ) ;
#164415=CARTESIAN_POINT ( 'NONE',  ( 4.204028478337375829E-16, -0.02876672507444788529, -3.432849766368870181 ) ) ;
#164455=CARTESIAN_POINT ( 'NONE',  ( 0.000000000000000000, -2.734374999522040550, -3.793834371823813001 ) ) ;
#164460=( LENGTH_UNIT ( ) NAMED_UNIT ( * ) SI_UNIT ( .MILLI., .METRE. ) );
#164503=DIRECTION ( 'NONE',  ( 0.000000000000000000, 0.000000000000000000, 1.000000000000000000 ) ) ;
#164595=VERTEX_POINT ( 'NONE', #176894 ) ;
#164602=ORIENTED_EDGE ( 'NONE', *, *, #184990, .T. ) ;
#164637=CARTESIAN_POINT ( 'NONE',  ( 0.000000000000000000, 0.5000000000000004441, 0.000000000000000000 ) ) ;
#164686=CARTESIAN_POINT ( 'NONE',  ( -3.320873661936399657, -0.9167811538275831840, 0.1393910267247679413 ) ) ;
#164709=CARTESIAN_POINT ( 'NONE',  ( -3.285556943750000514, -1.538541666188708357, -1.896917185911906500 ) ) ;
#164711=CARTESIAN_POINT ( 'NONE',  ( 1.464175926609780964E-14, -2.187499999999999112, -3.475000000000000533 ) ) ;
#164769=CARTESIAN_POINT ( 'NONE',  ( 1.500000000000035971, 8.500000000000000000, 9.886859966642587594 ) ) ;
#164782=CARTESIAN_POINT ( 'NONE',  ( -3.285556943750000514, -3.376041666188708490, -1.896917185911906500 ) ) ;
#164838=PLANE ( 'NONE',  #42809 ) ;
#164861=CYLINDRICAL_SURFACE ( 'NONE', #81728, 3.475000000000000089 ) ;
#164862=DIRECTION ( 'NONE',  ( -0.000000000000000000, -1.000000000000000000, -0.000000000000000000 ) ) ;
#164863=CARTESIAN_POINT ( 'NONE',  ( 1.500000000000053291, 7.750000000000000000, 15.74999999999999289 ) ) ;
#164872=CARTESIAN_POINT ( 'NONE',  ( 1.737499999999999378, -3.616666666666667140, -3.009438278150925683 ) ) ;
#164944=CARTESIAN_POINT ( 'NONE',  ( 1.737499999999999378, -2.872916665710750106, -3.009438278150925683 ) ) ;
#164962=CARTESIAN_POINT ( 'NONE',  ( 2.665787487727776295, -3.982249430249628297, -2.473491247225932721 ) ) ;
#164975=CARTESIAN_POINT ( 'NONE',  ( 0.000000000000000000, -0.2843749995220433702, -3.793834371823813001 ) ) ;
#165035=CARTESIAN_POINT ( 'NONE',  ( -3.474999999999998312, -2.727083332377418845, 2.006292185433951047 ) ) ;
#165079=EDGE_LOOP ( 'NONE', ( #101798, #156309 ) ) ;
#165124=CARTESIAN_POINT ( 'NONE',  ( 3.285556943749998737, -2.005208332855377140, -1.896917185911906500 ) ) ;
#165326=CARTESIAN_POINT ( 'NONE',  ( 3.285556943750000514, -3.463541666188707957, 1.896917185911906500 ) ) ;
#165473=CARTESIAN_POINT ( 'NONE',  ( -3.285556943750000070, -3.609374999522043659, 0.000000000000000000 ) ) ;
#165515=CARTESIAN_POINT ( 'NONE',  ( -1.737499999999997824, -3.091666666666666341, 3.009438278150925683 ) ) ;
#165517=CARTESIAN_POINT ( 'NONE',  ( -3.285556943750000514, -4.076041666188709556, -1.896917185911906500 ) ) ;
#165553=DIRECTION ( 'NONE',  ( 1.000000000000000000, 0.000000000000000000, -3.491481338843133355E-15 ) ) ;
#165557=CARTESIAN_POINT ( 'NONE',  ( -3.285556943750000070, -0.1531249995220425320, 0.000000000000000000 ) ) ;
#165583=CARTESIAN_POINT ( 'NONE',  ( -3.285556943749998737, -2.617708332855374298, 1.896917185911908499 ) ) ;
#165749=CARTESIAN_POINT ( 'NONE',  ( 1.500000000000035971, 6.999999999999999112, 9.886859966642587594 ) ) ;
#165755=AXIS2_PLACEMENT_3D ( 'NONE', #25742, #9505, #43104 ) ;
#165781=CARTESIAN_POINT ( 'NONE',  ( -3.285556943750000070, -3.259374999522044014, 0.000000000000000000 ) ) ;
#165811=FACE_BOUND ( 'NONE', #207427, .T. ) ;
#165847=ORIENTED_EDGE ( 'NONE', *, *, #103675, .F. ) ;
#165900=LINE ( 'NONE', #136610, #159531 ) ;
#165903=CARTESIAN_POINT ( 'NONE',  ( 0.000000000000000000, -3.499999999999999556, 3.017800438942086050 ) ) ;
#165940=ORIENTED_EDGE ( 'NONE', *, *, #94477, .T. ) ;
#165941=CARTESIAN_POINT ( 'NONE',  ( -1.737500000000000266, -3.208333333333333925, -3.009438278150923907 ) ) ;
#166003=DIRECTION ( 'NONE',  ( 2.345077562848782505E-16, 0.000000000000000000, 1.000000000000000000 ) ) ;
#166069=CARTESIAN_POINT ( 'NONE',  ( 3.285556943750000514, -1.013541666188710888, 1.896917185911906722 ) ) ;
#166102=CARTESIAN_POINT ( 'NONE',  ( 3.475000000000000533, -2.552083332377419023, -2.006292185433951047 ) ) ;
#166185=CARTESIAN_POINT ( 'NONE',  ( -1.642778471875000035, -2.617708332855375186, -2.845375778867859751 ) ) ;
#166380=CARTESIAN_POINT ( 'NONE',  ( -3.475000000000000533, -2.756249999044086074, 0.000000000000000000 ) ) ;
#166392=CARTESIAN_POINT ( 'NONE',  ( -1.642778471874998480, -3.901041666188709289, 2.845375778867863303 ) ) ;
#166412=DIRECTION ( 'NONE',  ( 0.000000000000000000, 1.000000000000000000, 0.000000000000000000 ) ) ;
#166504=AXIS2_PLACEMENT_3D ( 'NONE', #150167, #1735, #68872 ) ;
#166519=CARTESIAN_POINT ( 'NONE',  ( -1.737499999999997824, -2.041666666666667407, 3.009438278150925683 ) ) ;
#166546=CARTESIAN_POINT ( 'NONE',  ( -1.737500000000000266, -0.4083333333333334370, -3.009438278150923907 ) ) ;
#166550=B_SPLINE_CURVE_WITH_KNOTS ( 'NONE', 3,
 ( #157360, #189837, #21969, #8952, #105420, #54510, #42557, #207153, #203929, #57713, #186633, #23047 ),
 .UNSPECIFIED., .F., .F.,
 ( 4, 2, 2, 2, 2, 4 ),
 ( 0.001599105520544900991, 0.002495321489371081849, 0.002943429473784172495, 0.003391537458197263141, 0.004287753427023444433, 0.005183969395849624857 ),
 .UNSPECIFIED. ) ;
#166592=CARTESIAN_POINT ( 'NONE',  ( -3.285556943750000070, -4.046874999522040106, 0.000000000000000000 ) ) ;
#166656=CARTESIAN_POINT ( 'NONE',  ( 1.642778471875001811, -1.830208332855375097, 2.845375778867859751 ) ) ;
#166664=ORIENTED_EDGE ( 'NONE', *, *, #29015, .T. ) ;
#166700=ADVANCED_FACE ( 'NONE', ( #125320 ), #114792, .T. ) ;
#166774=CARTESIAN_POINT ( 'NONE',  ( 0.000000000000000000, 1.000000000000000888, -9.999999999999998224 ) ) ;
#166820=CARTESIAN_POINT ( 'NONE',  ( -3.381773599491823656, -0.9528023431436689616, 0.2057550699296430974 ) ) ;
#166847=CARTESIAN_POINT ( 'NONE',  ( 3.285556943750000514, -1.713541666188707735, 1.896917185911906500 ) ) ;
#166955=AXIS2_PLACEMENT_3D ( 'NONE', #190123, #80387, #141434 ) ;
#166990=CARTESIAN_POINT ( 'NONE',  ( 1.429488589276664001, -3.154214574430208806, -3.050286313710991681 ) ) ;
#167006=CARTESIAN_POINT ( 'NONE',  ( -3.424659329065677493, -0.02067678355765355941, -0.4189035560211199494 ) ) ;
#167015=CARTESIAN_POINT ( 'NONE',  ( -1.737499999999997824, -3.791666666666665186, 3.009438278150925683 ) ) ;
#167068=ORIENTED_EDGE ( 'NONE', *, *, #151730, .T. ) ;
#167078=DIRECTION ( 'NONE',  ( -1.000000000000000000, 0.000000000000000000, 2.345077562848782505E-16 ) ) ;
#167113=VERTEX_POINT ( 'NONE', #177788 ) ;
#167120=CARTESIAN_POINT ( 'NONE',  ( 3.285556943750000514, -0.7510416661887079348, 1.896917185911906500 ) ) ;
#167144=CARTESIAN_POINT ( 'NONE',  ( -0.4577034257980932552, -0.8887487162305418575, -3.253519940713586855 ) ) ;
#167175=CARTESIAN_POINT ( 'NONE',  ( 3.285556943749998737, -1.042708332855377451, -1.896917185911906500 ) ) ;
#167266=CARTESIAN_POINT ( 'NONE',  ( 3.285556943749998737, -1.305208332855376296, -1.896917185911906500 ) ) ;
#167380=VERTEX_POINT ( 'NONE', #73498 ) ;
#167464=CARTESIAN_POINT ( 'NONE',  ( 3.285556943749998737, -2.705208332855374209, -1.896917185911906500 ) ) ;
#167516=FACE_OUTER_BOUND ( 'NONE', #113388, .T. ) ;
#167602=AXIS2_PLACEMENT_3D ( 'NONE', #59131, #43974, #172904 ) ;
#167613=CARTESIAN_POINT ( 'NONE',  ( -3.285556943750000070, -3.959374999522043304, 0.000000000000000000 ) ) ;
#167654=CARTESIAN_POINT ( 'NONE',  ( -3.285556943749998737, -1.480208332855375453, 1.896917185911908499 ) ) ;
#167685=ORIENTED_EDGE ( 'NONE', *, *, #184597, .T. ) ;
#167704=CIRCLE ( 'NONE', #70872, 0.1000000000000000333 ) ;
#167712=EDGE_CURVE ( 'NONE', #141673, #70696, #31724, .T. ) ;
#167717=CARTESIAN_POINT ( 'NONE',  ( -3.285556943749998737, -1.567708332855375142, 1.896917185911908499 ) ) ;
#167760=AXIS2_PLACEMENT_3D ( 'NONE', #158040, #204610, #159087 ) ;
#167804=CARTESIAN_POINT ( 'NONE',  ( 0.4423056438102772603, -0.9742743152163436671, 3.420118577353472133 ) ) ;
#167881=EDGE_CURVE ( 'NONE', #141673, #152360, #39294, .T. ) ;
#167886=CARTESIAN_POINT ( 'NONE',  ( 1.250000000000053069, 8.500000000000000000, 15.75000000000000000 ) ) ;
#167904=ORIENTED_EDGE ( 'NONE', *, *, #109904, .T. ) ;
#167908=CARTESIAN_POINT ( 'NONE',  ( -1.642778471875000035, -2.617708332855375186, -2.845375778867859751 ) ) ;
#167940=DIRECTION ( 'NONE',  ( 0.000000000000000000, 1.000000000000000000, 0.000000000000000000 ) ) ;
#167942=CARTESIAN_POINT ( 'NONE',  ( 0.000000000000000000, -3.499999999999999556, 0.000000000000000000 ) ) ;
#168049=CARTESIAN_POINT ( 'NONE',  ( -1.347971487989957070E-14, -3.018749999044084475, 3.475000000000000089 ) ) ;
#168063=CARTESIAN_POINT ( 'NONE',  ( -3.422413393345596688, -0.02203823224375053846, -0.4176190697224198001 ) ) ;
#168075=AXIS2_PLACEMENT_3D ( 'NONE', #204920, #173545, #3512 ) ;
#168202=CARTESIAN_POINT ( 'NONE',  ( 1.642778471875001811, -1.042708332855375009, 2.845375778867859751 ) ) ;
#168236=CARTESIAN_POINT ( 'NONE',  ( -1.737499999999997824, -3.747916665710750994, 3.009438278150925683 ) ) ;
#168299=CARTESIAN_POINT ( 'NONE',  ( -1.520658191422891603, -0.9880266363068606061, 3.134631954704482748 ) ) ;
#168327=CARTESIAN_POINT ( 'NONE',  ( -1.642778471875000035, -1.567708332855376252, -2.845375778867859751 ) ) ;
#168508=DIRECTION ( 'NONE',  ( 3.706092522800016599E-15, 0.000000000000000000, 1.000000000000000000 ) ) ;
#168525=CARTESIAN_POINT ( 'NONE',  ( 2.520460663003311730, -4.091624451297095177, -2.338645729556988240 ) ) ;
#168535=ORIENTED_EDGE ( 'NONE', *, *, #68949, .F. ) ;
#168547=DIRECTION ( 'NONE',  ( -0.000000000000000000, 1.000000000000000000, -0.000000000000000000 ) ) ;
#168647=CARTESIAN_POINT ( 'NONE',  ( -3.475000000000000533, -2.100000000000000977, 0.000000000000000000 ) ) ;
#168650=CARTESIAN_POINT ( 'NONE',  ( -1.642778471875000035, -0.9552083328553742092, -2.845375778867859751 ) ) ;
#168674=CARTESIAN_POINT ( 'NONE',  ( -1.737500000000000266, -0.7583333333333330817, -3.009438278150923907 ) ) ;
#168706=FACE_OUTER_BOUND ( 'NONE', #197957, .T. ) ;
#168716=CARTESIAN_POINT ( 'NONE',  ( 3.475000000000000533, -2.945833333333332416, -2.006292185433951047 ) ) ;
#168719=CARTESIAN_POINT ( 'NONE',  ( -1.642778471874998480, -0.4010416661887096224, 2.845375778867863303 ) ) ;
#168780=CARTESIAN_POINT ( 'NONE',  ( -3.285556943749998737, -2.267708332855375986, 1.896917185911908499 ) ) ;
#168859=EDGE_CURVE ( 'NONE', #9969, #101274, #83567, .T. ) ;
#168916=CARTESIAN_POINT ( 'NONE',  ( 1.737499999999999378, -1.866666666666665808, -3.009438278150925683 ) ) ;
#168924=EDGE_CURVE ( 'NONE', #10807, #35390, #172139, .T. ) ;
#168939=CARTESIAN_POINT ( 'NONE',  ( -3.386157300525472369, -0.9633972889761682756, 0.4263094016780412665 ) ) ;
#168966=CARTESIAN_POINT ( 'NONE',  ( 3.285556943750000514, -2.763541666188707335, 1.896917185911906500 ) ) ;
#169094=DIRECTION ( 'NONE',  ( 0.000000000000000000, -0.000000000000000000, 1.000000000000000000 ) ) ;
#169119=AXIS2_PLACEMENT_3D ( 'NONE', #206387, #55880, #90535 ) ;
#169123=CARTESIAN_POINT ( 'NONE',  ( -3.418738334753848029, -0.02680128005874191088, -0.3660903872622625066 ) ) ;
#169124=CARTESIAN_POINT ( 'NONE',  ( -1.499999999999960254, 7.064371086078064188, 10.89416074946470836 ) ) ;
#169163=VERTEX_POINT ( 'NONE', #112260 ) ;
#169267=CARTESIAN_POINT ( 'NONE',  ( 0.000000000000000000, -1.946874999522044014, -3.793834371823813445 ) ) ;
#169301=CARTESIAN_POINT ( 'NONE',  ( 3.475000000000000533, -4.010416665710750728, 2.006292185433948827 ) ) ;
#169389=CARTESIAN_POINT ( 'NONE',  ( -3.285556943750000514, -2.938541666188710266, -1.896917185911906500 ) ) ;
#169418=DIRECTION ( 'NONE',  ( -0.000000000000000000, 1.000000000000000000, -0.000000000000000000 ) ) ;
#169546=DIRECTION ( 'NONE',  ( 0.000000000000000000, 0.000000000000000000, 1.000000000000000000 ) ) ;
#169593=( BOUNDED_CURVE ( )  B_SPLINE_CURVE ( 3, ( #10843, #27104, #95347, #112700 ),
 .UNSPECIFIED., .F., .T. ) 
 B_SPLINE_CURVE_WITH_KNOTS ( ( 4, 4 ),
 ( 4.837716811552755125, 4.862957253161376059 ),
 .UNSPECIFIED. ) 
 CURVE ( )  GEOMETRIC_REPRESENTATION_ITEM ( )  RATIONAL_B_SPLINE_CURVE ( ( 1.000000000000000000, 0.9999469107135832147, 0.9999469107135832147, 1.000000000000000000 ) ) 
 REPRESENTATION_ITEM ( '' )  );
#169645=CARTESIAN_POINT ( 'NONE',  ( 0.000000000000000000, 0.000000000000000000, 0.000000000000000000 ) ) ;
#169718=CARTESIAN_POINT ( 'NONE',  ( -3.285556943750000070, -0.8968749995220438587, 0.000000000000000000 ) ) ;
#169727=DIRECTION ( 'NONE',  ( 0.000000000000000000, -0.000000000000000000, 1.000000000000000000 ) ) ;
#169741=CARTESIAN_POINT ( 'NONE',  ( 2.960183410750786059, -4.109567543049581495, -1.425552035297093623 ) ) ;
#169784=CARTESIAN_POINT ( 'NONE',  ( 1.642778471875001811, -2.092708332855373943, 2.845375778867859751 ) ) ;
#169846=CARTESIAN_POINT ( 'NONE',  ( -1.642778471875000035, -2.705208332855375986, -2.845375778867859751 ) ) ;
#169931=EDGE_CURVE ( 'NONE', #12134, #94066, #34919, .T. ) ;
#169979=DIRECTION ( 'NONE',  ( 0.000000000000000000, 1.000000000000000000, 0.000000000000000000 ) ) ;
#170028=CARTESIAN_POINT ( 'NONE',  ( 3.285556943750000070, -3.434374999522042060, 0.000000000000000000 ) ) ;
#170063=CARTESIAN_POINT ( 'NONE',  ( -1.737499999999997824, -2.391666666666667052, 3.009438278150925683 ) ) ;
#170070=EDGE_CURVE ( 'NONE', #157226, #134989, #121020, .T. ) ;
#170225=FACE_BOUND ( 'NONE', #188195, .T. ) ;
#170300=CARTESIAN_POINT ( 'NONE',  ( -1.642778471875000035, -0.9552083328553742092, -2.845375778867859751 ) ) ;
#170323=CARTESIAN_POINT ( 'NONE',  ( 3.285556943750000514, -1.713541666188707735, 1.896917185911906722 ) ) ;
#170359=CARTESIAN_POINT ( 'NONE',  ( -1.737500000000000266, -4.214583332377418223, -3.009438278150923907 ) ) ;
#170363=CIRCLE ( 'NONE', #35380, 2.750000000000000444 ) ;
#170395=EDGE_CURVE ( 'NONE', #121330, #25653, #21135, .T. ) ;
#170444=EDGE_CURVE ( 'NONE', #40241, #113311, #78576, .T. ) ;
#170448=CARTESIAN_POINT ( 'NONE',  ( -1.432719062495390716, -3.042800438942089514, 3.165902886691621010 ) ) ;
#170449=CARTESIAN_POINT ( 'NONE',  ( 1.001543065824772753E-15, -2.821874999522044458, 3.793834371823811669 ) ) ;
#170556=CARTESIAN_POINT ( 'NONE',  ( -0.9311234436981496998, -1.284380368602565659, 3.475000000000000977 ) ) ;
#170645=EDGE_LOOP ( 'NONE', ( #121034, #43713, #106628, #73827 ) ) ;
#170653=CARTESIAN_POINT ( 'NONE',  ( 1.685698123273788651, -1.500000000000000000, -1.979500400907064916 ) ) ;
#170762=ORIENTED_EDGE ( 'NONE', *, *, #59714, .T. ) ;
#170787=CARTESIAN_POINT ( 'NONE',  ( 3.285556943750000514, -1.451041666188708890, 1.896917185911906722 ) ) ;
#170788=DIRECTION ( 'NONE',  ( 1.000000000000000000, 0.000000000000000000, -3.491481338843133355E-15 ) ) ;
#170851=CARTESIAN_POINT ( 'NONE',  ( 1.347111479062088405E-15, 6.999999999999999112, 11.00000000000000000 ) ) ;
#170854=CARTESIAN_POINT ( 'NONE',  ( 1.001543065824772753E-15, -0.3718749995220430038, 3.793834371823811669 ) ) ;
#170913=CARTESIAN_POINT ( 'NONE',  ( -3.285556943749998737, -3.667708332855377673, 1.896917185911908499 ) ) ;
#170914=VERTEX_POINT ( 'NONE', #34089 ) ;
#171047=CARTESIAN_POINT ( 'NONE',  ( -1.333477130265052990, 8.249568609204949610, -9.911050286642563378 ) ) ;
#171063=CARTESIAN_POINT ( 'NONE',  ( 0.000000000000000000, -0.1968749995220437643, -3.793834371823813001 ) ) ;
#171102=CARTESIAN_POINT ( 'NONE',  ( 3.475000000000000533, -0.2041666666666657748, 2.006292185433948827 ) ) ;
#171107=CARTESIAN_POINT ( 'NONE',  ( 1.737500000000001155, -1.283333333333334325, 3.009438278150922130 ) ) ;
#171190=ORIENTED_EDGE ( 'NONE', *, *, #111491, .F. ) ;
#171257=AXIS2_PLACEMENT_3D ( 'NONE', #119168, #169979, #184096 ) ;
#171287=CARTESIAN_POINT ( 'NONE',  ( 1.464175926609780964E-14, -2.493749999044085452, -3.475000000000000533 ) ) ;
#171293=EDGE_LOOP ( 'NONE', ( #11079, #165940, #155902, #139887 ) ) ;
#171353=CARTESIAN_POINT ( 'NONE',  ( -1.288108131580338211, -0.9841229182759280159, 3.227445187970915619 ) ) ;
#171373=CARTESIAN_POINT ( 'NONE',  ( 3.285556943750000514, -2.151041666188709733, 1.896917185911906500 ) ) ;
#171420=EDGE_CURVE ( 'NONE', #126440, #94296, #114281, .T. ) ;
#171435=CARTESIAN_POINT ( 'NONE',  ( -3.285556943749998737, -0.5177083328553757635, 1.896917185911908499 ) ) ;
#171475=CARTESIAN_POINT ( 'NONE',  ( 0.000000000000000000, -0.5000000000000004441, 3.599999999999999201 ) ) ;
#171490=FACE_OUTER_BOUND ( 'NONE', #181274, .T. ) ;
#171519=CARTESIAN_POINT ( 'NONE',  ( 0.000000000000000000, -2.996874999522043392, -3.793834371823813001 ) ) ;
#171525=LINE ( 'NONE', #141214, #70506 ) ;
#171552=DIRECTION ( 'NONE',  ( 0.000000000000000000, 0.000000000000000000, 1.000000000000000000 ) ) ;
#171577=EDGE_CURVE ( 'NONE', #212297, #74385, #69697, .T. ) ;
#171672=SHAPE_DEFINITION_REPRESENTATION ( #213239, #203468 ) ;
#171673=CIRCLE ( 'NONE', #5586, 3.150000000000000799 ) ;
#171721=DIRECTION ( 'NONE',  ( -0.000000000000000000, 1.000000000000000000, -0.000000000000000000 ) ) ;
#171927=CARTESIAN_POINT ( 'NONE',  ( 0.000000000000000000, -0.8968749995220406390, -3.793834371823813001 ) ) ;
#171956=( BOUNDED_CURVE ( )  B_SPLINE_CURVE ( 2, ( #13506, #76375, #161916, #128427, #95860, #111082, #142482, #78508, #159764 ),
 .UNSPECIFIED., .F., .T. ) 
 B_SPLINE_CURVE_WITH_KNOTS ( ( 3, 2, 2, 2, 3 ),
 ( 0.6458333333333333703, 0.6527777777777777901, 0.6666666666666666297, 0.6805555555555555802, 0.6875000000000000000 ),
 .UNSPECIFIED. ) 
 CURVE ( )  GEOMETRIC_REPRESENTATION_ITEM ( )  RATIONAL_B_SPLINE_CURVE ( ( 0.9330127018922192983, 0.9330127018922198534, 1.000000000000000000, 0.8660254037844387076, 1.000000000000000000, 0.8660254037844387076, 1.000000000000000000, 0.9330127018922194093, 0.9330127018922194093 ) ) 
 REPRESENTATION_ITEM ( '' )  );
#171963=ORIENTED_EDGE ( 'NONE', *, *, #103930, .T. ) ;
#171993=CARTESIAN_POINT ( 'NONE',  ( -1.642778471874998480, -3.638541666188710444, 2.845375778867863303 ) ) ;
#172010=CARTESIAN_POINT ( 'NONE',  ( 1.333477130265051214, 8.249568609204947833, 9.911050286642563378 ) ) ;
#172022=DIRECTION ( 'NONE',  ( -0.000000000000000000, -1.000000000000000000, -0.000000000000000000 ) ) ;
#172072=CIRCLE ( 'NONE', #96020, 3.150000000000000799 ) ;
#172139=( BOUNDED_CURVE ( )  B_SPLINE_CURVE ( 2, ( #103933, #85531, #41884, #8279, #74363, #107995, #25591, #80763, #61308 ),
 .UNSPECIFIED., .F., .T. ) 
 B_SPLINE_CURVE_WITH_KNOTS ( ( 3, 2, 2, 2, 3 ),
 ( 0.4375000000000000000, 0.4444444444444444198, 0.4583333333333333148, 0.4722222222222222099, 0.4791666666666666852 ),
 .UNSPECIFIED. ) 
 CURVE ( )  GEOMETRIC_REPRESENTATION_ITEM ( )  RATIONAL_B_SPLINE_CURVE ( ( 0.9330127018922194093, 0.9330127018922194093, 1.000000000000000000, 0.8660254037844387076, 1.000000000000000000, 0.8660254037844387076, 1.000000000000000000, 0.9330127018922190762, 0.9330127018922194093 ) ) 
 REPRESENTATION_ITEM ( '' )  );
#172148=CARTESIAN_POINT ( 'NONE',  ( -1.642778471875000035, -0.5177083328553738761, -2.845375778867859751 ) ) ;
#172186=CARTESIAN_POINT ( 'NONE',  ( 1.737499999999999378, -0.8166666666666668739, -3.009438278150925683 ) ) ;
#172337=CARTESIAN_POINT ( 'NONE',  ( -1.499999999999960254, 7.564371094685077068, 10.87018506808107965 ) ) ;
#172455=CARTESIAN_POINT ( 'NONE',  ( -3.285556943750000070, -1.946874999522042682, 0.000000000000000000 ) ) ;
#172508=DIRECTION ( 'NONE',  ( 0.000000000000000000, 0.000000000000000000, -1.000000000000000000 ) ) ;
#172511=CARTESIAN_POINT ( 'NONE',  ( 1.620863580070950549, -1.399999999999998579, -1.903365770102947163 ) ) ;
#172516=CARTESIAN_POINT ( 'NONE',  ( 0.000000000000000000, -3.084374999522042859, -3.793834371823813001 ) ) ;
#172568=VECTOR ( 'NONE', #17969, 1000.000000000000000 ) ;
#172591=EDGE_CURVE ( 'NONE', #213109, #167380, #138858, .T. ) ;
#172607=CARTESIAN_POINT ( 'NONE',  ( 2.520459450608881991, -4.091624429771669291, -2.338646429533238535 ) ) ;
#172671=LINE ( 'NONE', #154281, #121664 ) ;
#172718=CARTESIAN_POINT ( 'NONE',  ( 0.000000000000000000, 6.999999999999999112, 0.000000000000000000 ) ) ;
#172896=AXIS2_PLACEMENT_3D ( 'NONE', #18896, #51429, #197660 ) ;
#172904=DIRECTION ( 'NONE',  ( 0.000000000000000000, 0.000000000000000000, 1.000000000000000000 ) ) ;
#172927=ORIENTED_EDGE ( 'NONE', *, *, #46133, .T. ) ;
#172944=CARTESIAN_POINT ( 'NONE',  ( -1.642778471874998480, -1.538541666188709245, 2.845375778867863303 ) ) ;
#173009=CARTESIAN_POINT ( 'NONE',  ( 3.285556943750000070, -3.784374999522041705, 0.000000000000000000 ) ) ;
#173070=CARTESIAN_POINT ( 'NONE',  ( -3.285556943750000070, -0.1093749995220438809, 0.000000000000000000 ) ) ;
#173158=CARTESIAN_POINT ( 'NONE',  ( 2.228883261964242912, -0.9158852807988100420, -2.473645833743700173 ) ) ;
#173225=CARTESIAN_POINT ( 'NONE',  ( -3.285556943749998737, -0.4302083328553760744, 1.896917185911908499 ) ) ;
#173234=PLANE ( 'NONE',  #127571 ) ;
#173241=FACE_OUTER_BOUND ( 'NONE', #57806, .T. ) ;
#173263=CARTESIAN_POINT ( 'NONE',  ( -3.475000000000000533, -0.6999999999999992895, 0.000000000000000000 ) ) ;
#173482=DIRECTION ( 'NONE',  ( 0.000000000000000000, 1.000000000000000000, 0.000000000000000000 ) ) ;
#173542=CARTESIAN_POINT ( 'NONE',  ( 3.285556943749998737, -2.092708332855377051, -1.896917185911906500 ) ) ;
#173545=DIRECTION ( 'NONE',  ( -0.000000000000000000, 1.000000000000000000, -0.000000000000000000 ) ) ;
#173605=CARTESIAN_POINT ( 'NONE',  ( -3.285556943750000070, -2.296874999522042327, 0.000000000000000000 ) ) ;
#173645=ORIENTED_EDGE ( 'NONE', *, *, #129564, .F. ) ;
#173691=CARTESIAN_POINT ( 'NONE',  ( 0.000000000000000000, -2.187499999999998668, -4.012584370867899430 ) ) ;
#173766=CARTESIAN_POINT ( 'NONE',  ( 1.620863580070950327, 0.5000000000000004441, -1.903365770102947385 ) ) ;
#173780=CARTESIAN_POINT ( 'NONE',  ( 3.475000000000000533, -1.574999999999999956, 0.000000000000000000 ) ) ;
#173952=DIRECTION ( 'NONE',  ( 0.000000000000000000, 0.000000000000000000, -1.000000000000000000 ) ) ;
#173976=EDGE_LOOP ( 'NONE', ( #66428, #170762, #143498, #38934 ) ) ;
#174022=CARTESIAN_POINT ( 'NONE',  ( 1.737500000000001155, -1.983333333333333393, 3.009438278150922130 ) ) ;
#174025=FACE_OUTER_BOUND ( 'NONE', #181321, .T. ) ;
#174087=CARTESIAN_POINT ( 'NONE',  ( -1.642778471874998480, -2.501041666188707158, 2.845375778867863303 ) ) ;
#174150=CARTESIAN_POINT ( 'NONE',  ( 0.000000000000000000, -3.784374999522044369, -3.793834371823813001 ) ) ;
#174163=CARTESIAN_POINT ( 'NONE',  ( 0.000000000000000000, 0.4000000000000010214, 0.000000000000000000 ) ) ;
#174269=EDGE_CURVE ( 'NONE', #210464, #92865, #49173, .T. ) ;
#174296=CARTESIAN_POINT ( 'NONE',  ( -3.285556943750000514, -1.188541666188710044, -1.896917185911906500 ) ) ;
#174305=DIRECTION ( 'NONE',  ( 0.9486832980505138790, -0.3162277660168376636, -3.312310031615527152E-15 ) ) ;
#174327=VERTEX_POINT ( 'NONE', #65700 ) ;
#174332=CARTESIAN_POINT ( 'NONE',  ( 1.642778471875001811, -3.842708332855375275, 2.845375778867859751 ) ) ;
#174362=EDGE_LOOP ( 'NONE', ( #74316, #29617, #148469, #51972, #137451 ) ) ;
#174377=CARTESIAN_POINT ( 'NONE',  ( -3.475000000000000533, 0.000000000000000000, 0.000000000000000000 ) ) ;
#174516=ORIENTED_EDGE ( 'NONE', *, *, #10280, .T. ) ;
#174526=ORIENTED_EDGE ( 'NONE', *, *, #41738, .T. ) ;
#174602=EDGE_LOOP ( 'NONE', ( #34762, #159261, #29534, #86030, #8903 ) ) ;
#174608=CARTESIAN_POINT ( 'NONE',  ( 3.285556943749998737, -1.742708332855374076, -1.896917185911906500 ) ) ;
#174652=ADVANCED_FACE ( 'NONE', ( #113497 ), #97199, .T. ) ;
#174664=CARTESIAN_POINT ( 'NONE',  ( -3.285556943749998737, -1.567708332855375142, 1.896917185911908499 ) ) ;
#174674=ORIENTED_EDGE ( 'NONE', *, *, #5122, .T. ) ;
#174757=CARTESIAN_POINT ( 'NONE',  ( -3.474999999999998312, -1.370833333333331350, 2.006292185433951047 ) ) ;
#174764=CARTESIAN_POINT ( 'NONE',  ( 0.000000000000000000, 0.9000000000000014655, 0.000000000000000000 ) ) ;
#174845=CARTESIAN_POINT ( 'NONE',  ( -3.475000000000000533, -2.100000000000000977, 0.000000000000000000 ) ) ;
#174917=CARTESIAN_POINT ( 'NONE',  ( -3.475000000000000533, -1.006249999044084298, 0.000000000000000000 ) ) ;
#175001=CARTESIAN_POINT ( 'NONE',  ( 1.001543065824772753E-15, -0.3718749995220430038, 3.793834371823811669 ) ) ;
#175081=CARTESIAN_POINT ( 'NONE',  ( -3.285556943749998737, -2.617708332855374742, 1.896917185911908721 ) ) ;
#175145=CARTESIAN_POINT ( 'NONE',  ( 1.001543065824772753E-15, -3.521874999522041083, 3.793834371823811669 ) ) ;
#175209=CARTESIAN_POINT ( 'NONE',  ( 3.285556943750000070, -0.2843749995220419269, 0.000000000000000000 ) ) ;
#175293=EDGE_CURVE ( 'NONE', #130778, #24109, #60537, .T. ) ;
#175308=ORIENTED_EDGE ( 'NONE', *, *, #189945, .T. ) ;
#175315=CIRCLE ( 'NONE', #43906, 3.475000000000000089 ) ;
#175389=CARTESIAN_POINT ( 'NONE',  ( 1.001543065824772753E-15, -1.312499999999998224, 4.012584370867899430 ) ) ;
#175486=EDGE_CURVE ( 'NONE', #107993, #192999, #170363, .T. ) ;
#175544=ORIENTED_EDGE ( 'NONE', *, *, #41171, .T. ) ;
#175588=EDGE_LOOP ( 'NONE', ( #67457, #180838, #148539, #121040 ) ) ;
#175661=CARTESIAN_POINT ( 'NONE',  ( 1.642778471875000035, -3.113541666188709200, -2.845375778867859751 ) ) ;
#175703=CARTESIAN_POINT ( 'NONE',  ( -2.550000000000001155, 2.499999999999998668, -1.849324200890690717 ) ) ;
#175714=CARTESIAN_POINT ( 'NONE',  ( -3.285556943749998737, -1.917708332855377673, 1.896917185911908499 ) ) ;
#175770=DIRECTION ( 'NONE',  ( -0.6483454320283799088, 0.000000000000000000, 0.7613463080411786432 ) ) ;
#175781=( BOUNDED_CURVE ( )  B_SPLINE_CURVE ( 2, ( #3588, #132597, #83798, #33986, #16653, #118507, #84870, #149891, #36108 ),
 .UNSPECIFIED., .F., .F. ) 
 B_SPLINE_CURVE_WITH_KNOTS ( ( 3, 2, 2, 2, 3 ),
 ( 0.3541666666666666852, 0.3611111111111111049, 0.3750000000000000000, 0.3888888888888888951, 0.3958333333333333703 ),
 .UNSPECIFIED. ) 
 CURVE ( )  GEOMETRIC_REPRESENTATION_ITEM ( )  RATIONAL_B_SPLINE_CURVE ( ( 0.9330127018922194093, 0.9330127018922196314, 1.000000000000000000, 0.8660254037844387076, 1.000000000000000000, 0.8660254037844387076, 1.000000000000000000, 0.9330127018922190762, 0.9330127018922194093 ) ) 
 REPRESENTATION_ITEM ( '' )  );
#175811=CARTESIAN_POINT ( 'NONE',  ( 3.475000000000000533, -2.274999999999999467, 0.000000000000000000 ) ) ;
#175875=LINE ( 'NONE', #208337, #136825 ) ;
#175885=CARTESIAN_POINT ( 'NONE',  ( -2.900957617708239678, -3.232243495192087757, 1.542507481629952881 ) ) ;
#175903=CARTESIAN_POINT ( 'NONE',  ( 0.000000000000000000, -1.487500000000001599, -4.012584370867899430 ) ) ;
#175974=CARTESIAN_POINT ( 'NONE',  ( 0.000000000000000000, -1.443749999044082966, -4.012584370867899430 ) ) ;
#175996=AXIS2_PLACEMENT_3D ( 'NONE', #101972, #90007, #75868 ) ;
#176061=CARTESIAN_POINT ( 'NONE',  ( -3.285556943749998737, -0.7802083328553744979, 1.896917185911908499 ) ) ;
#176100=CARTESIAN_POINT ( 'NONE',  ( 4.255647627037052709E-16, 0.5000000000000004441, 3.475000000000000089 ) ) ;
#176143=CARTESIAN_POINT ( 'NONE',  ( 1.642778471875001811, -2.180208332855374742, 2.845375778867859751 ) ) ;
#176204=CARTESIAN_POINT ( 'NONE',  ( 3.285556943750000514, -3.463541666188707957, 1.896917185911906500 ) ) ;
#176226=DIRECTION ( 'NONE',  ( -0.000000000000000000, -1.000000000000000000, -0.000000000000000000 ) ) ;
#176259=VERTEX_POINT ( 'NONE', #144471 ) ;
#176266=CARTESIAN_POINT ( 'NONE',  ( -3.285556943750000514, -0.8385416661887076240, -1.896917185911906500 ) ) ;
#176288=DIRECTION ( 'NONE',  ( 0.000000000000000000, -0.000000000000000000, 1.000000000000000000 ) ) ;
#176342=CARTESIAN_POINT ( 'NONE',  ( 3.364870901607376563, -0.9372182959936623536, -0.3762680151246870497 ) ) ;
#176358=FACE_OUTER_BOUND ( 'NONE', #32797, .T. ) ;
#176409=CARTESIAN_POINT ( 'NONE',  ( 1.642778471875001811, -2.442708332855377140, 2.845375778867859751 ) ) ;
#176445=CARTESIAN_POINT ( 'NONE',  ( 0.000000000000000000, -2.887499999999999289, -4.012584370867899430 ) ) ;
#176448=DIRECTION ( 'NONE',  ( 0.000000000000000000, 0.000000000000000000, -1.000000000000000000 ) ) ;
#176507=CARTESIAN_POINT ( 'NONE',  ( -0.9596184899144685199, -3.128028181787985584, -3.256865572402548814 ) ) ;
#176534=EDGE_CURVE ( 'NONE', #102958, #212297, #77130, .T. ) ;
#176631=CYLINDRICAL_SURFACE ( 'NONE', #202490, 3.475000000000000089 ) ;
#176700=CARTESIAN_POINT ( 'NONE',  ( 0.000000000000000000, -0.8968749995220406390, -3.793834371823813001 ) ) ;
#176734=FACE_BOUND ( 'NONE', #107324, .T. ) ;
#176768=CARTESIAN_POINT ( 'NONE',  ( 1.642778471875000035, -2.413541666188709911, -2.845375778867859751 ) ) ;
#176804=ADVANCED_FACE ( 'NONE', ( #134605 ), #51190, .F. ) ;
#176818=EDGE_LOOP ( 'NONE', ( #27718, #206630, #131924, #174516, #155537, #127518, #185682 ) ) ;
#176864=PRODUCT ( 'base', 'base', '', ( #8103 ) ) ;
#176866=CARTESIAN_POINT ( 'NONE',  ( 1.737499999999999378, -0.8166666666666668739, -3.009438278150925683 ) ) ;
#176894=CARTESIAN_POINT ( 'NONE',  ( 1.394453263437886604E-15, -1.268749999044084253, 3.474999999999999645 ) ) ;
#176905=ORIENTED_EDGE ( 'NONE', *, *, #97268, .T. ) ;
#176957=CARTESIAN_POINT ( 'NONE',  ( -3.475000000000000533, -1.399999999999998579, 0.000000000000000000 ) ) ;
#176992=CARTESIAN_POINT ( 'NONE',  ( -2.550000000000000266, 1.000000000000000888, -1.849324200890692271 ) ) ;
#177029=CARTESIAN_POINT ( 'NONE',  ( 1.737500000000001155, -1.589583332377419334, 3.009438278150922130 ) ) ;
#177115=CARTESIAN_POINT ( 'NONE',  ( 1.642778471875001811, -0.6927083328553753638, 2.845375778867859751 ) ) ;
#177200=CARTESIAN_POINT ( 'NONE',  ( 3.285556943749998737, -2.442708332855375364, -1.896917185911906722 ) ) ;
#177261=DIRECTION ( 'NONE',  ( 0.000000000000000000, -0.000000000000000000, -1.000000000000000000 ) ) ;
#177263=CARTESIAN_POINT ( 'NONE',  ( -1.642778471875000035, -2.617708332855375186, -2.845375778867859751 ) ) ;
#177327=CARTESIAN_POINT ( 'NONE',  ( -3.285556943749998737, -1.830208332855373987, 1.896917185911908499 ) ) ;
#177475=CARTESIAN_POINT ( 'NONE',  ( 3.285556943750000070, -2.384374999522043126, 0.000000000000000000 ) ) ;
#177512=CARTESIAN_POINT ( 'NONE',  ( -3.474999999999998312, -2.420833333333334725, 2.006292185433951047 ) ) ;
#177579=CARTESIAN_POINT ( 'NONE',  ( -3.315919823527478716, -3.091870070317458197, -0.8826684162155652436 ) ) ;
#177604=ORIENTED_EDGE ( 'NONE', *, *, #167881, .F. ) ;
#177775=CARTESIAN_POINT ( 'NONE',  ( 3.285556943750000070, -0.6343749995220415716, 0.000000000000000000 ) ) ;
#177781=ORIENTED_EDGE ( 'NONE', *, *, #198277, .F. ) ;
#177783=CARTESIAN_POINT ( 'NONE',  ( 2.550000000000000266, -7.105553651663779391, -1.849324200890695824 ) ) ;
#177788=CARTESIAN_POINT ( 'NONE',  ( 0.000000000000000000, 0.000000000000000000, -11.00000000000000000 ) ) ;
#177808=EDGE_LOOP ( 'NONE', ( #4119, #188131, #53236, #199364 ) ) ;
#177873=ORIENTED_EDGE ( 'NONE', *, *, #194552, .F. ) ;
#177941=CARTESIAN_POINT ( 'NONE',  ( 1.001543065824772753E-15, -0.9624999999999998002, 4.012584370867899430 ) ) ;
#178002=DIRECTION ( 'NONE',  ( 0.000000000000000000, -1.000000000000000000, 0.000000000000000000 ) ) ;
#178029=CARTESIAN_POINT ( 'NONE',  ( 3.475000000000000533, -2.245833333333331350, -2.006292185433951047 ) ) ;
#178104=CARTESIAN_POINT ( 'NONE',  ( 3.475000000000000533, -1.881249999044085186, 0.000000000000000000 ) ) ;
#178113=ORIENTED_EDGE ( 'NONE', *, *, #72642, .T. ) ;
#178190=CARTESIAN_POINT ( 'NONE',  ( -3.285556943750000514, -0.1385416661887106660, -1.896917185911906500 ) ) ;
#178247=ORIENTED_EDGE ( 'NONE', *, *, #188328, .F. ) ;
#178399=CARTESIAN_POINT ( 'NONE',  ( -1.642778471875000035, -1.567708332855376252, -2.845375778867859751 ) ) ;
#178540=CARTESIAN_POINT ( 'NONE',  ( -3.285556943750000070, -2.559374999522041172, 0.000000000000000000 ) ) ;
#178581=CARTESIAN_POINT ( 'NONE',  ( -1.737499999999997824, -2.741666666666666696, 3.009438278150925683 ) ) ;
#178642=CARTESIAN_POINT ( 'NONE',  ( 0.000000000000000000, -0.02876672507444791305, 0.000000000000000000 ) ) ;
#178648=CARTESIAN_POINT ( 'NONE',  ( 1.001543065824772753E-15, -0.4593749995220425819, 3.793834371823811669 ) ) ;
#178649=CARTESIAN_POINT ( 'NONE',  ( -3.432104779031577735, -3.080473746885612485, 0.2707740179794877466 ) ) ;
#178708=DIRECTION ( 'NONE',  ( 0.000000000000000000, -1.000000000000000000, 0.000000000000000000 ) ) ;
#178773=DIRECTION ( 'NONE',  ( -0.6483454320283799088, 0.000000000000000000, 0.7613463080411786432 ) ) ;
#178794=LINE ( 'NONE', #47739, #157507 ) ;
#178849=CARTESIAN_POINT ( 'NONE',  ( -3.285556943750000070, -1.159374999522042815, 0.000000000000000000 ) ) ;
#178975=CARTESIAN_POINT ( 'NONE',  ( -3.474999999999997868, -1.720833333333333659, 2.006292185433951047 ) ) ;
#179003=CIRCLE ( 'NONE', #5917, 0.09999999999999986677 ) ;
#179066=ADVANCED_FACE ( 'NONE', ( #185529 ), #153048, .T. ) ;
#179078=CARTESIAN_POINT ( 'NONE',  ( 1.464175926609780964E-14, -2.843749999044085541, -3.475000000000000533 ) ) ;
#179095=CARTESIAN_POINT ( 'NONE',  ( 1.737500000000001155, -3.733333333333331616, 3.009438278150922130 ) ) ;
#179115=( LENGTH_UNIT ( ) NAMED_UNIT ( * ) SI_UNIT ( .MILLI., .METRE. ) );
#179135=AXIS2_PLACEMENT_3D ( 'NONE', #74107, #140200, #110935 ) ;
#179168=CARTESIAN_POINT ( 'NONE',  ( -3.475000000000000533, -2.756249999044086074, 0.000000000000000000 ) ) ;
#179193=ADVANCED_FACE ( 'NONE', ( #75002 ), #124900, .T. ) ;
#179232=EDGE_CURVE ( 'NONE', #211538, #182913, #163733, .T. ) ;
#179285=VERTEX_POINT ( 'NONE', #172511 ) ;
#179326=ORIENTED_EDGE ( 'NONE', *, *, #103372, .F. ) ;
#179463=CARTESIAN_POINT ( 'NONE',  ( -3.285556943750000070, -2.209374999522041527, 0.000000000000000000 ) ) ;
#179495=CIRCLE ( 'NONE', #16950, 0.1000000000000000333 ) ;
#179570=MECHANICAL_DESIGN_GEOMETRIC_PRESENTATION_REPRESENTATION('',(#138146),#30853);
#179604=CARTESIAN_POINT ( 'NONE',  ( 1.642778471875001811, -1.742708332855374298, 2.845375778867859751 ) ) ;
#179646=CARTESIAN_POINT ( 'NONE',  ( 3.475000000000000533, -1.195833333333332194, -2.006292185433951047 ) ) ;
#179648=CARTESIAN_POINT ( 'NONE',  ( 0.000000000000000000, -4.134374999522041350, -3.793834371823813001 ) ) ;
#179652=( NAMED_UNIT ( * ) PLANE_ANGLE_UNIT ( ) SI_UNIT ( $, .RADIAN. ) );
#179695=CARTESIAN_POINT ( 'NONE',  ( 0.000000000000000000, -0.5000000000000005551, 0.000000000000000000 ) ) ;
#179714=CARTESIAN_POINT ( 'NONE',  ( 0.000000000000000000, -0.6343749995220417937, -3.793834371823813001 ) ) ;
#179760=ADVANCED_FACE ( 'NONE', ( #43587 ), #194067, .F. ) ;
#179972=DIRECTION ( 'NONE',  ( -0.000000000000000000, 1.000000000000000000, -0.000000000000000000 ) ) ;
#179975=CARTESIAN_POINT ( 'NONE',  ( 1.642778471875001811, -3.580208332855376430, 2.845375778867859751 ) ) ;
#180031=CARTESIAN_POINT ( 'NONE',  ( -3.475000000000000533, -1.779166666666666785, -2.006292185433948827 ) ) ;
#180057=CARTESIAN_POINT ( 'NONE',  ( -3.424509409375499747, -0.02075852630553524925, -0.4189850677842354432 ) ) ;
#180066=DIRECTION ( 'NONE',  ( 0.000000000000000000, 0.000000000000000000, 1.000000000000000000 ) ) ;
#180068=CARTESIAN_POINT ( 'NONE',  ( 3.475000000000000533, -3.325000000000001510, 0.000000000000000000 ) ) ;
#180087=ORIENTED_EDGE ( 'NONE', *, *, #23742, .T. ) ;
#180137=FACE_BOUND ( 'NONE', #113872, .T. ) ;
#180156=CARTESIAN_POINT ( 'NONE',  ( 1.001543065824772753E-15, -3.062499999999998668, 4.012584370867899430 ) ) ;
#180231=CARTESIAN_POINT ( 'NONE',  ( -3.475000000000000533, -3.106249999044085275, 0.000000000000000000 ) ) ;
#180316=CARTESIAN_POINT ( 'NONE',  ( 3.285556943749998737, -2.705208332855374209, -1.896917185911906500 ) ) ;
#180401=EDGE_CURVE ( 'NONE', #51499, #176259, #46518, .T. ) ;
#180494=CONICAL_SURFACE ( 'NONE', #59413, 3.000000000000000000, 0.7853981633974523868 ) ;
#180517=CARTESIAN_POINT ( 'NONE',  ( 1.642778471875000035, -1.976041666188709689, -2.845375778867859751 ) ) ;
#180553=DIRECTION ( 'NONE',  ( 0.000000000000000000, 0.000000000000000000, 1.000000000000000000 ) ) ;
#180658=CARTESIAN_POINT ( 'NONE',  ( -1.642778471875000035, -1.917708332855375897, -2.845375778867859751 ) ) ;
#180699=CARTESIAN_POINT ( 'NONE',  ( 1.642778471875001811, -3.580208332855376430, 2.845375778867859751 ) ) ;
#180734=CARTESIAN_POINT ( 'NONE',  ( 0.000000000000000000, 0.4000000000000010214, 0.000000000000000000 ) ) ;
#180746=DIRECTION ( 'NONE',  ( -0.000000000000000000, 1.000000000000000000, -0.000000000000000000 ) ) ;
#180838=ORIENTED_EDGE ( 'NONE', *, *, #132234, .T. ) ;
#180846=TOROIDAL_SURFACE ( 'NONE', #211921, 2.349999999999999645, 0.1000000000000000056 ) ;
#180927=CARTESIAN_POINT ( 'NONE',  ( -3.317034467965191080, -0.9147500475860976810, 0.1576429056095928760 ) ) ;
#180953=CARTESIAN_POINT ( 'NONE',  ( 3.285556943749998737, -1.305208332855376296, -1.896917185911906500 ) ) ;
#181014=CARTESIAN_POINT ( 'NONE',  ( 1.042866153392195239, -3.232243495192089089, 3.126988198976878408 ) ) ;
#181029=CARTESIAN_POINT ( 'NONE',  ( 1.642778471875000035, -3.813541666188708490, -2.845375778867859751 ) ) ;
#181083=CARTESIAN_POINT ( 'NONE',  ( -0.9311234436981532525, -1.678130369558482826, 3.474999999999999201 ) ) ;
#181094=CARTESIAN_POINT ( 'NONE',  ( 1.693866981432350594, -3.230387921952247332, 2.823574758769644255 ) ) ;
#181111=CARTESIAN_POINT ( 'NONE',  ( -3.463051730202630019, -0.006534250585093354102, -0.1996569003990655289 ) ) ;
#181121=CARTESIAN_POINT ( 'NONE',  ( 0.000000000000000000, -3.587500000000000355, -4.012584370867899430 ) ) ;
#181219=CARTESIAN_POINT ( 'NONE',  ( 1.642778471875001811, -0.4302083328553765740, 2.845375778867859751 ) ) ;
#181227=( NAMED_UNIT ( * ) PLANE_ANGLE_UNIT ( ) SI_UNIT ( $, .RADIAN. ) );
#181274=EDGE_LOOP ( 'NONE', ( #99907, #57387, #136567, #55684 ) ) ;
#181278=CARTESIAN_POINT ( 'NONE',  ( 3.475000000000000533, -2.231249999044084831, 0.000000000000000000 ) ) ;
#181321=EDGE_LOOP ( 'NONE', ( #122916, #65086, #13734, #195640 ) ) ;
#181358=( BOUNDED_CURVE ( )  B_SPLINE_CURVE ( 2, ( #200388, #187354, #105069, #85589, #34702, #53090, #171107, #83454, #70379 ),
 .UNSPECIFIED., .F., .T. ) 
 B_SPLINE_CURVE_WITH_KNOTS ( ( 3, 2, 2, 2, 3 ),
 ( 0.2708333333333333703, 0.2777777777777777901, 0.2916666666666666852, 0.3055555555555555802, 0.3125000000000000000 ),
 .UNSPECIFIED. ) 
 CURVE ( )  GEOMETRIC_REPRESENTATION_ITEM ( )  RATIONAL_B_SPLINE_CURVE ( ( 0.9330127018922194093, 0.9330127018922196314, 1.000000000000000000, 0.8660254037844387076, 1.000000000000000000, 0.8660254037844387076, 1.000000000000000000, 0.9330127018922194093, 0.9330127018922194093 ) ) 
 REPRESENTATION_ITEM ( '' )  );
#181370=CARTESIAN_POINT ( 'NONE',  ( 1.001543065824772753E-15, -1.771874999522040861, 3.793834371823811669 ) ) ;
#181495=EDGE_CURVE ( 'NONE', #153986, #81793, #145623, .T. ) ;
#181566=CARTESIAN_POINT ( 'NONE',  ( 3.285556943750000070, -2.734374999522042771, 0.000000000000000000 ) ) ;
#181677=CARTESIAN_POINT ( 'NONE',  ( 0.000000000000000000, 8.500000000000000000, -9.999999999999996447 ) ) ;
#181706=CARTESIAN_POINT ( 'NONE',  ( -1.737500000000000266, -0.05833333333333384774, -3.009438278150923907 ) ) ;
#181748=CARTESIAN_POINT ( 'NONE',  ( -1.642778471875000035, -3.055208332855375630, -2.845375778867859751 ) ) ;
#181815=CARTESIAN_POINT ( 'NONE',  ( -3.285556943750000070, -1.596874999522043037, 0.000000000000000000 ) ) ;
#181816=CARTESIAN_POINT ( 'NONE',  ( 3.475000000000000533, -1.881249999044085186, 0.000000000000000000 ) ) ;
#181924=FACE_OUTER_BOUND ( 'NONE', #41578, .T. ) ;
#181937=CIRCLE ( 'NONE', #64298, 3.099999999999999201 ) ;
#181946=ORIENTED_EDGE ( 'NONE', *, *, #198939, .F. ) ;
#181960=CARTESIAN_POINT ( 'NONE',  ( 0.9311234436981579154, -2.553130369558483270, -3.474999999999996536 ) ) ;
#181968=ORIENTED_EDGE ( 'NONE', *, *, #16746, .F. ) ;
#182005=CARTESIAN_POINT ( 'NONE',  ( 1.001543065824772753E-15, -3.171874999522042327, 3.793834371823811669 ) ) ;
#182010=DIRECTION ( 'NONE',  ( 1.000000000000000000, 0.000000000000000000, -2.345077562848777574E-16 ) ) ;
#182143=CARTESIAN_POINT ( 'NONE',  ( 1.905568696376195970, -3.159541454813609374, -2.771379219291199458 ) ) ;
#182159=CARTESIAN_POINT ( 'NONE',  ( -3.441837234280166413, -0.01368419061246708458, -0.3627113057276946106 ) ) ;
#182167=EDGE_CURVE ( 'NONE', #110540, #71536, #84205, .T. ) ;
#182171=CARTESIAN_POINT ( 'NONE',  ( 3.475000000000000533, -2.595833333333334103, -2.006292185433951047 ) ) ;
#182279=DIRECTION ( 'NONE',  ( 0.000000000000000000, 0.000000000000000000, 1.000000000000000000 ) ) ;
#182328=AXIS2_PLACEMENT_3D ( 'NONE', #158060, #42180, #208898 ) ;
#182334=CARTESIAN_POINT ( 'NONE',  ( 1.001543065824772753E-15, -1.968749999044084653, 4.012584370867899430 ) ) ;
#182423=CARTESIAN_POINT ( 'NONE',  ( -1.642778471874998480, -2.501041666188707158, 2.845375778867863303 ) ) ;
#182630=CARTESIAN_POINT ( 'NONE',  ( 1.001543065824772753E-15, -2.821874999522044458, 3.793834371823811669 ) ) ;
#182712=CARTESIAN_POINT ( 'NONE',  ( 1.499999999999959588, 8.500000000000000000, -10.89724735885168805 ) ) ;
#182781=CARTESIAN_POINT ( 'NONE',  ( -3.285556943749998737, -3.230208332855375897, 1.896917185911908499 ) ) ;
#182826=CARTESIAN_POINT ( 'NONE',  ( 2.665787487727776295, -3.982249430249628297, -2.473491247225932721 ) ) ;
#182828=CARTESIAN_POINT ( 'NONE',  ( 0.000000000000000000, -3.784374999522044369, -3.793834371823813001 ) ) ;
#182892=CARTESIAN_POINT ( 'NONE',  ( -1.642778471874998480, -2.938541666188707602, 2.845375778867863303 ) ) ;
#182913=VERTEX_POINT ( 'NONE', #135549 ) ;
#182974=DIRECTION ( 'NONE',  ( 0.6483454320283799088, 0.000000000000000000, -0.7613463080411786432 ) ) ;
#183035=CARTESIAN_POINT ( 'NONE',  ( 1.464175926609780964E-14, -2.537500000000001865, -3.475000000000000533 ) ) ;
#183045=VERTEX_POINT ( 'NONE', #191730 ) ;
#183084=CARTESIAN_POINT ( 'NONE',  ( 1.642778471875001811, -2.442708332855377140, 2.845375778867859751 ) ) ;
#183120=EDGE_CURVE ( 'NONE', #88193, #94956, #169593, .T. ) ;
#183161=CARTESIAN_POINT ( 'NONE',  ( 1.620863580070950549, 0.4000000000000010214, -1.903365770102946941 ) ) ;
#183175=EDGE_LOOP ( 'NONE', ( #35362, #179326, #142067, #64236 ) ) ;
#183249=CARTESIAN_POINT ( 'NONE',  ( -3.475000000000000533, -3.879166666666665986, -2.006292185433948827 ) ) ;
#183289=DIRECTION ( 'NONE',  ( 0.000000000000000000, 1.000000000000000000, 0.000000000000000000 ) ) ;
#183341=CARTESIAN_POINT ( 'NONE',  ( -3.475000000000000533, -3.149999999999999911, 0.000000000000000000 ) ) ;
#183357=DIRECTION ( 'NONE',  ( -0.000000000000000000, 1.000000000000000000, -0.000000000000000000 ) ) ;
#183373=ORIENTED_EDGE ( 'NONE', *, *, #196923, .F. ) ;
#183378=CARTESIAN_POINT ( 'NONE',  ( 1.642778471875001811, -2.092708332855373943, 2.845375778867859751 ) ) ;
#183414=CARTESIAN_POINT ( 'NONE',  ( 1.642778471875000035, -0.3135416661887088785, -2.845375778867859751 ) ) ;
#183497=CARTESIAN_POINT ( 'NONE',  ( -3.285556943749998737, -1.830208332855373987, 1.896917185911908499 ) ) ;
#183573=CARTESIAN_POINT ( 'NONE',  ( -1.288108131580338211, -0.9841229182759280159, 3.227445187970915619 ) ) ;
#183629=ORIENTED_EDGE ( 'NONE', *, *, #46704, .F. ) ;
#183667=VECTOR ( 'NONE', #159836, 1000.000000000000000 ) ;
#183704=CARTESIAN_POINT ( 'NONE',  ( 0.000000000000000000, -2.646874999522040639, -3.793834371823813001 ) ) ;
#183725=DIRECTION ( 'NONE',  ( -0.6483454320283799088, 0.000000000000000000, 0.7613463080411786432 ) ) ;
#183828=AXIS2_PLACEMENT_3D ( 'NONE', #92762, #93829, #73264 ) ;
#183854=CARTESIAN_POINT ( 'NONE',  ( 1.642778471875000035, -3.726041666188707691, -2.845375778867859751 ) ) ;
#183897=CARTESIAN_POINT ( 'NONE',  ( 3.285556943750000070, -2.034374999522043481, 0.000000000000000000 ) ) ;
#183959=CARTESIAN_POINT ( 'NONE',  ( 3.285556943750000070, -1.771874999522041083, 0.000000000000000000 ) ) ;
#183979=( BOUNDED_CURVE ( )  B_SPLINE_CURVE ( 3, ( #68378, #121507, #134509, #39109 ),
 .UNSPECIFIED., .F., .T. ) 
 B_SPLINE_CURVE_WITH_KNOTS ( ( 4, 4 ),
 ( 4.683789229004536203, 4.706575325518645769 ),
 .UNSPECIFIED. ) 
 CURVE ( )  GEOMETRIC_REPRESENTATION_ITEM ( )  RATIONAL_B_SPLINE_CURVE ( ( 1.000000000000000000, 0.9999567332851475587, 0.9999567332851475587, 1.000000000000000000 ) ) 
 REPRESENTATION_ITEM ( '' )  );
#184096=DIRECTION ( 'NONE',  ( -0.6483454320283799088, 0.000000000000000000, 0.7613463080411786432 ) ) ;
#184141=CARTESIAN_POINT ( 'NONE',  ( -3.285556943750000514, -2.238541666188709200, -1.896917185911906500 ) ) ;
#184271=CYLINDRICAL_SURFACE ( 'NONE', #175996, 3.150000000000000799 ) ;
#184279=DIRECTION ( 'NONE',  ( -0.6483454320283799088, 0.000000000000000000, 0.7613463080411786432 ) ) ;
#184294=CARTESIAN_POINT ( 'NONE',  ( -3.423294271397314681, -0.02146400342267793318, -0.4188604460931010243 ) ) ;
#184334=VERTEX_POINT ( 'NONE', #13791 ) ;
#184436=CARTESIAN_POINT ( 'NONE',  ( 1.642778471875001811, -1.742708332855374298, 2.845375778867859751 ) ) ;
#184468=CARTESIAN_POINT ( 'NONE',  ( -3.475000000000000533, -4.156249999044084653, 0.000000000000000000 ) ) ;
#184556=CARTESIAN_POINT ( 'NONE',  ( -3.285556943750000070, -1.859374999522041882, 0.000000000000000000 ) ) ;
#184597=EDGE_CURVE ( 'NONE', #81793, #167113, #63650, .T. ) ;
#184712=DIRECTION ( 'NONE',  ( -0.9486832980505139901, -0.3162277660168373861, 3.312310031615527941E-15 ) ) ;
#184745=ORIENTED_EDGE ( 'NONE', *, *, #139330, .T. ) ;
#184753=CARTESIAN_POINT ( 'NONE',  ( 0.000000000000000000, -3.696874999522040017, -3.793834371823813001 ) ) ;
#184813=DIRECTION ( 'NONE',  ( 0.000000000000000000, 0.000000000000000000, 1.000000000000000000 ) ) ;
#184846=ADVANCED_FACE ( 'NONE', ( #91634, #208527 ), #127392, .F. ) ;
#184884=CARTESIAN_POINT ( 'NONE',  ( 3.285556943750000514, -1.101041666188710355, 1.896917185911906722 ) ) ;
#184908=CARTESIAN_POINT ( 'NONE',  ( 3.475000000000000533, -0.1458333333333326765, -2.006292185433951047 ) ) ;
#184946=CARTESIAN_POINT ( 'NONE',  ( -1.737499999999997824, -3.441666666666665986, 3.009438278150925683 ) ) ;
#184948=CARTESIAN_POINT ( 'NONE',  ( -3.285556943750000514, -0.8385416661887076240, -1.896917185911906500 ) ) ;
#184990=EDGE_CURVE ( 'NONE', #184334, #197566, #146717, .T. ) ;
#185009=DIRECTION ( 'NONE',  ( 0.000000000000000000, 0.000000000000000000, -1.000000000000000000 ) ) ;
#185012=CARTESIAN_POINT ( 'NONE',  ( 0.000000000000000000, -1.684374999522041172, -3.793834371823813001 ) ) ;
#185030=CARTESIAN_POINT ( 'NONE',  ( 0.000000000000000000, 2.499999999999998668, 0.000000000000000000 ) ) ;
#185077=EDGE_CURVE ( 'NONE', #59550, #155131, #67020, .T. ) ;
#185159=EDGE_LOOP ( 'NONE', ( #90021, #47579, #115221 ) ) ;
#185201=CARTESIAN_POINT ( 'NONE',  ( -1.642778471875000035, -2.267708332855375541, -2.845375778867859751 ) ) ;
#185296=CYLINDRICAL_SURFACE ( 'NONE', #46387, 3.475000000000000089 ) ;
#185501=CARTESIAN_POINT ( 'NONE',  ( -3.285556943750000514, -2.238541666188709200, -1.896917185911906722 ) ) ;
#185529=FACE_OUTER_BOUND ( 'NONE', #113160, .T. ) ;
#185531=ORIENTED_EDGE ( 'NONE', *, *, #182167, .F. ) ;
#185535=CARTESIAN_POINT ( 'NONE',  ( -1.642778471875000035, -1.305208332855377407, -2.845375778867859751 ) ) ;
#185592=CARTESIAN_POINT ( 'NONE',  ( 0.000000000000000000, 0.5000000000000004441, 0.000000000000000000 ) ) ;
#185622=CARTESIAN_POINT ( 'NONE',  ( 0.000000000000000000, -3.499999999999999556, 0.000000000000000000 ) ) ;
#185623=CARTESIAN_POINT ( 'NONE',  ( -1.642778471874998480, -3.201041666188710000, 2.845375778867863303 ) ) ;
#185658=CARTESIAN_POINT ( 'NONE',  ( -2.900957617708239678, -3.232243495192087757, 1.542507481629953103 ) ) ;
#185682=ORIENTED_EDGE ( 'NONE', *, *, #33285, .T. ) ;
#185687=DIRECTION ( 'NONE',  ( 0.000000000000000000, -1.000000000000000000, -0.000000000000000000 ) ) ;
#185844=CARTESIAN_POINT ( 'NONE',  ( 0.000000000000000000, -1.500000000000001332, 0.000000000000000000 ) ) ;
#185876=FACE_BOUND ( 'NONE', #147958, .T. ) ;
#185911=EDGE_LOOP ( 'NONE', ( #76204, #178113, #123076, #85615 ) ) ;
#185951=ORIENTED_EDGE ( 'NONE', *, *, #91258, .F. ) ;
#185978=CARTESIAN_POINT ( 'NONE',  ( 1.642778471875001811, -3.492708332855375630, 2.845375778867859751 ) ) ;
#185990=LINE ( 'NONE', #201163, #134465 ) ;
#186019=CARTESIAN_POINT ( 'NONE',  ( -3.285556943750000514, -1.888541666188711110, -1.896917185911906500 ) ) ;
#186087=CARTESIAN_POINT ( 'NONE',  ( -3.285556943750000514, -2.676041666188707424, -1.896917185911906500 ) ) ;
#186095=CARTESIAN_POINT ( 'NONE',  ( 0.000000000000000000, 1.000000000000000888, 0.000000000000000000 ) ) ;
#186162=EDGE_LOOP ( 'NONE', ( #37463, #15866, #194203, #51050, #188044, #114006, #139081, #47960, #192414, #63408 ) ) ;
#186258=AXIS2_PLACEMENT_3D ( 'NONE', #164863, #14328, #146518 ) ;
#186273=CARTESIAN_POINT ( 'NONE',  ( -1.737499999999997824, -0.6416666666666653862, 3.009438278150925683 ) ) ;
#186277=EDGE_CURVE ( 'NONE', #167113, #81793, #39523, .T. ) ;
#186307=CARTESIAN_POINT ( 'NONE',  ( 1.499999999999959588, 7.378742179571330162, -10.87908636427991382 ) ) ;
#186403=CARTESIAN_POINT ( 'NONE',  ( 0.000000000000000000, 6.999999999999999112, 0.000000000000000000 ) ) ;
#186492=CARTESIAN_POINT ( 'NONE',  ( 0.000000000000000000, 8.500000000000000000, 0.000000000000000000 ) ) ;
#186553=CARTESIAN_POINT ( 'NONE',  ( 1.642778471875001811, -2.180208332855374742, 2.845375778867859751 ) ) ;
#186561=TOROIDAL_SURFACE ( 'NONE', #93216, 3.399419719642636561, 0.1000000000000000056 ) ;
#186577=CARTESIAN_POINT ( 'NONE',  ( -1.642778471874998480, -1.451041666188708446, 2.845375778867863303 ) ) ;
#186611=CARTESIAN_POINT ( 'NONE',  ( -3.475000000000000533, -3.835416665710750905, -2.006292185433948827 ) ) ;
#186633=CARTESIAN_POINT ( 'NONE',  ( -2.760655612144408799, -3.232243495192088201, 1.806370170574614464 ) ) ;
#186650=DIRECTION ( 'NONE',  ( 0.000000000000000000, 0.000000000000000000, 1.000000000000000000 ) ) ;
#186695=CARTESIAN_POINT ( 'NONE',  ( 0.000000000000000000, -3.346874999522042149, -3.793834371823813001 ) ) ;
#186912=LINE ( 'NONE', #102473, #211997 ) ;
#186984=FACE_OUTER_BOUND ( 'NONE', #19538, .T. ) ;
#187007=VERTEX_POINT ( 'NONE', #181677 ) ;
#187028=CARTESIAN_POINT ( 'NONE',  ( -1.642778471874998480, -1.188541666188709600, 2.845375778867863303 ) ) ;
#187094=CARTESIAN_POINT ( 'NONE',  ( -3.285556943750000514, -0.4885416661887091450, -1.896917185911906500 ) ) ;
#187158=CARTESIAN_POINT ( 'NONE',  ( 0.000000000000000000, -3.434374999522041616, -3.793834371823813001 ) ) ;
#187190=AXIS2_PLACEMENT_3D ( 'NONE', #10041, #11098, #93461 ) ;
#187349=CARTESIAN_POINT ( 'NONE',  ( 2.520459450608881991, -4.091624429771669291, -2.338646429533238535 ) ) ;
#187354=CARTESIAN_POINT ( 'NONE',  ( 0.9311234436981545848, -1.153130369558482027, -3.474999999999999201 ) ) ;
#187501=CARTESIAN_POINT ( 'NONE',  ( -3.419936744200066325, -0.02828022925090156736, -0.3125692937056851473 ) ) ;
#187528=ORIENTED_EDGE ( 'NONE', *, *, #38982, .T. ) ;
#187541=ORIENTED_EDGE ( 'NONE', *, *, #127328, .F. ) ;
#187558=CARTESIAN_POINT ( 'NONE',  ( -1.416652131158606664, 8.000043606524071649, 10.86080395187257608 ) ) ;
#187616=CARTESIAN_POINT ( 'NONE',  ( 1.642778471875000035, -2.413541666188709911, -2.845375778867859751 ) ) ;
#187640=CARTESIAN_POINT ( 'NONE',  ( -3.285556943750000070, -1.509374999522042238, 0.000000000000000000 ) ) ;
#187646=VECTOR ( 'NONE', #49677, 1000.000000000000000 ) ;
#187672=CARTESIAN_POINT ( 'NONE',  ( 3.285556943750000070, -0.7218749995220423710, 0.000000000000000000 ) ) ;
#187761=CARTESIAN_POINT ( 'NONE',  ( 2.960183410750786059, -4.109567543049581495, -1.425552035297093623 ) ) ;
#187790=CARTESIAN_POINT ( 'NONE',  ( 0.000000000000000000, 2.999999999999999112, 0.000000000000000000 ) ) ;
#187809=CIRCLE ( 'NONE', #66719, 2.650000000000000799 ) ;
#187822=AXIS2_PLACEMENT_3D ( 'NONE', #92350, #56618, #154120 ) ;
#187867=CARTESIAN_POINT ( 'NONE',  ( 7.204675194429079505E-15, -1.443749999044083854, -3.475000000000000089 ) ) ;
#187945=STYLED_ITEM ( 'NONE', ( #144519 ), #84085 ) ;
#187973=VERTEX_POINT ( 'NONE', #57312 ) ;
#187978=FACE_BOUND ( 'NONE', #105255, .T. ) ;
#188044=ORIENTED_EDGE ( 'NONE', *, *, #88762, .T. ) ;
#188131=ORIENTED_EDGE ( 'NONE', *, *, #72841, .T. ) ;
#188163=CARTESIAN_POINT ( 'NONE',  ( -3.285556943749998737, -1.830208332855373987, 1.896917185911908499 ) ) ;
#188195=EDGE_LOOP ( 'NONE', ( #109708, #24141 ) ) ;
#188222=CARTESIAN_POINT ( 'NONE',  ( 3.285556943750000514, -0.3135416661887098777, 1.896917185911906500 ) ) ;
#188307=CARTESIAN_POINT ( 'NONE',  ( 3.251336881620926267, -0.9471318103815578038, 0.9360613127407988454 ) ) ;
#188327=CARTESIAN_POINT ( 'NONE',  ( 0.000000000000000000, 0.5000000000000004441, 0.000000000000000000 ) ) ;
#188328=EDGE_CURVE ( 'NONE', #197566, #114098, #167704, .T. ) ;
#188376=CARTESIAN_POINT ( 'NONE',  ( -3.285556943749998737, -0.7802083328553744979, 1.896917185911908499 ) ) ;
#188414=CARTESIAN_POINT ( 'NONE',  ( 3.285556943749998737, -3.755208332855373587, -1.896917185911906500 ) ) ;
#188417=ORIENTED_EDGE ( 'NONE', *, *, #118518, .T. ) ;
#188572=DIRECTION ( 'NONE',  ( -0.000000000000000000, -1.000000000000000000, -0.000000000000000000 ) ) ;
#188638=CARTESIAN_POINT ( 'NONE',  ( -3.294361253650757604, -0.1042918288308124219, 0.000000000000000000 ) ) ;
#188660=CARTESIAN_POINT ( 'NONE',  ( 0.000000000000000000, 6.999999999999999112, -9.999999999999998224 ) ) ;
#188692=CARTESIAN_POINT ( 'NONE',  ( -3.285556943749998737, -1.567708332855375142, 1.896917185911908499 ) ) ;
#188742=CARTESIAN_POINT ( 'NONE',  ( 0.000000000000000000, 5.000000000000000888, 0.000000000000000000 ) ) ;
#188747=CARTESIAN_POINT ( 'NONE',  ( 1.642778471875001811, -1.830208332855375097, 2.845375778867859751 ) ) ;
#188839=CARTESIAN_POINT ( 'NONE',  ( 0.000000000000000000, -4.046874999522043659, -3.793834371823813001 ) ) ;
#188871=VECTOR ( 'NONE', #125746, 1000.000000000000000 ) ;
#188948=CYLINDRICAL_SURFACE ( 'NONE', #33772, 11.00000000000000000 ) ;
#188990=CIRCLE ( 'NONE', #199330, 2.250000000000000444 ) ;
#189005=( BOUNDED_CURVE ( )  B_SPLINE_CURVE ( 3, ( #8877, #58704, #124854, #91227 ),
 .UNSPECIFIED., .F., .T. ) 
 B_SPLINE_CURVE_WITH_KNOTS ( ( 4, 4 ),
 ( 1.576609981660940907, 1.599396078175049807 ),
 .UNSPECIFIED. ) 
 CURVE ( )  GEOMETRIC_REPRESENTATION_ITEM ( )  RATIONAL_B_SPLINE_CURVE ( ( 1.000000000000000000, 0.9999567332851475587, 0.9999567332851475587, 1.000000000000000000 ) ) 
 REPRESENTATION_ITEM ( '' )  );
#189139=ADVANCED_FACE ( 'NONE', ( #101792 ), #38924, .T. ) ;
#189157=ORIENTED_EDGE ( 'NONE', *, *, #58497, .F. ) ;
#189222=ORIENTED_EDGE ( 'NONE', *, *, #183120, .T. ) ;
#189240=CARTESIAN_POINT ( 'NONE',  ( 3.285556943750000070, -3.434374999522042060, 0.000000000000000000 ) ) ;
#189245=EDGE_CURVE ( 'NONE', #51499, #179285, #88228, .T. ) ;
#189291=EDGE_CURVE ( 'NONE', #24541, #12413, #131445, .T. ) ;
#189298=CARTESIAN_POINT ( 'NONE',  ( 1.642778471875001811, -3.230208332855373676, 2.845375778867859751 ) ) ;
#189443=CARTESIAN_POINT ( 'NONE',  ( 0.000000000000000000, 2.499999999999998668, 0.000000000000000000 ) ) ;
#189451=CARTESIAN_POINT ( 'NONE',  ( 1.001543065824772753E-15, -0.7218749995220414828, 3.793834371823811669 ) ) ;
#189466=FACE_BOUND ( 'NONE', #11163, .T. ) ;
#189467=AXIS2_PLACEMENT_3D ( 'NONE', #56530, #6684, #190774 ) ;
#189478=CIRCLE ( 'NONE', #30408, 2.250000000000000444 ) ;
#189487=CARTESIAN_POINT ( 'NONE',  ( 1.737499999999999378, -0.1166666666666676955, -3.009438278150925683 ) ) ;
#189509=AXIS2_PLACEMENT_3D ( 'NONE', #46522, #16110, #13983 ) ;
#189637=DIRECTION ( 'NONE',  ( 0.000000000000000000, 0.000000000000000000, 1.000000000000000000 ) ) ;
#189700=DIRECTION ( 'NONE',  ( -0.000000000000000000, 1.000000000000000000, -0.000000000000000000 ) ) ;
#189731=CARTESIAN_POINT ( 'NONE',  ( 1.464175926609780964E-14, -2.187499999999999112, -3.475000000000000533 ) ) ;
#189745=EDGE_LOOP ( 'NONE', ( #26638, #206790, #141848, #30543 ) ) ;
#189751=CARTESIAN_POINT ( 'NONE',  ( -1.642778471875000035, -2.005208332855376696, -2.845375778867859751 ) ) ;
#189801=CARTESIAN_POINT ( 'NONE',  ( -1.499999999999964029, 6.999999999999999112, 9.886859966642596476 ) ) ;
#189812=CARTESIAN_POINT ( 'NONE',  ( -1.642778471875000035, -2.005208332855376696, -2.845375778867859751 ) ) ;
#189837=CARTESIAN_POINT ( 'NONE',  ( -0.2949299779344195516, -3.232243495192088201, 3.285556943750023606 ) ) ;
#189905=CARTESIAN_POINT ( 'NONE',  ( -1.642778471874998480, -3.901041666188709289, 2.845375778867863303 ) ) ;
#189945=EDGE_CURVE ( 'NONE', #49812, #13166, #105737, .T. ) ;
#189976=DIRECTION ( 'NONE',  ( 0.000000000000000000, -1.000000000000000000, -0.000000000000000000 ) ) ;
#189989=CARTESIAN_POINT ( 'NONE',  ( 1.001543065824772753E-15, -1.662500000000000533, 4.012584370867899430 ) ) ;
#190064=CARTESIAN_POINT ( 'NONE',  ( 1.001543065824772753E-15, -0.9187499990440851638, 4.012584370867899430 ) ) ;
#190109=ORIENTED_EDGE ( 'NONE', *, *, #170070, .T. ) ;
#190117=AXIS2_PLACEMENT_3D ( 'NONE', #185592, #416, #51349 ) ;
#190123=CARTESIAN_POINT ( 'NONE',  ( 0.000000000000000000, -0.5000000000000004441, 0.000000000000000000 ) ) ;
#190292=CARTESIAN_POINT ( 'NONE',  ( 1.001543065824772753E-15, -2.471874999522041705, 3.793834371823811669 ) ) ;
#190352=CARTESIAN_POINT ( 'NONE',  ( 3.285556943750000070, -3.871874999522042504, 0.000000000000000000 ) ) ;
#190384=CARTESIAN_POINT ( 'NONE',  ( 1.734723475976807094E-15, 1.000000000000000888, 0.000000000000000000 ) ) ;
#190471=ORIENTED_EDGE ( 'NONE', *, *, #196844, .T. ) ;
#190502=CARTESIAN_POINT ( 'NONE',  ( -3.285556943749998737, -1.130208332855377140, 1.896917185911908499 ) ) ;
#190541=CARTESIAN_POINT ( 'NONE',  ( -1.737500000000000266, -0.05833333333333384774, -3.009438278150923907 ) ) ;
#190654=DIRECTION ( 'NONE',  ( 0.000000000000000000, 0.000000000000000000, -1.000000000000000000 ) ) ;
#190693=CARTESIAN_POINT ( 'NONE',  ( -1.499999999999966693, 7.750000000000000000, 9.886859966642596476 ) ) ;
#190742=CARTESIAN_POINT ( 'NONE',  ( -1.718115394875207258, -1.500000000000000888, 2.017567716309124126 ) ) ;
#190774=DIRECTION ( 'NONE',  ( 1.000000000000000000, -9.486769009248179575E-16, 0.000000000000000000 ) ) ;
#190810=CARTESIAN_POINT ( 'NONE',  ( 0.000000000000000000, -1.684374999522041172, -3.793834371823813001 ) ) ;
#190868=CARTESIAN_POINT ( 'NONE',  ( 0.000000000000000000, -2.734374999522040550, -3.793834371823813001 ) ) ;
#190882=FACE_BOUND ( 'NONE', #17579, .T. ) ;
#190955=CARTESIAN_POINT ( 'NONE',  ( 3.475000000000000533, -1.574999999999999956, 0.000000000000000000 ) ) ;
#191047=CARTESIAN_POINT ( 'NONE',  ( 1.737500000000001155, -0.9333333333333346804, 3.009438278150922130 ) ) ;
#191070=DIRECTION ( 'NONE',  ( -3.491481338843133750E-15, -0.000000000000000000, -1.000000000000000000 ) ) ;
#191211=CARTESIAN_POINT ( 'NONE',  ( -3.285556943750000070, -0.8093749995220431703, 0.000000000000000000 ) ) ;
#191225=CARTESIAN_POINT ( 'NONE',  ( -2.324088772396477673E-16, -1.837499999999999245, -3.475000000000000089 ) ) ;
#191234=ORIENTED_EDGE ( 'NONE', *, *, #129593, .F. ) ;
#191286=CARTESIAN_POINT ( 'NONE',  ( -2.324088772396477673E-16, -1.837499999999999245, -3.475000000000000089 ) ) ;
#191289=CARTESIAN_POINT ( 'NONE',  ( 1.528150327639969719, -3.232243495192087757, 2.908546201585544999 ) ) ;
#191353=CARTESIAN_POINT ( 'NONE',  ( -3.285556943749998737, -3.230208332855375897, 1.896917185911908499 ) ) ;
#191417=CARTESIAN_POINT ( 'NONE',  ( -3.285556943750000514, -0.4885416661887091450, -1.896917185911906500 ) ) ;
#191428=DIRECTION ( 'NONE',  ( 0.000000000000000000, 1.000000000000000000, 0.000000000000000000 ) ) ;
#191565=CARTESIAN_POINT ( 'NONE',  ( -3.285556943750000514, -0.1385416661887106660, -1.896917185911906500 ) ) ;
#191602=CARTESIAN_POINT ( 'NONE',  ( 1.001543065824772753E-15, -2.362500000000001155, 4.012584370867899430 ) ) ;
#191730=CARTESIAN_POINT ( 'NONE',  ( 0.000000000000000000, 5.999999999999998224, 10.25000000000000000 ) ) ;
#191876=CARTESIAN_POINT ( 'NONE',  ( 1.001543065824772753E-15, -3.959374999522043304, 3.793834371823811669 ) ) ;
#191928=CARTESIAN_POINT ( 'NONE',  ( 1.001543065824772753E-15, -1.859374999522040550, 3.793834371823811669 ) ) ;
#192022=CARTESIAN_POINT ( 'NONE',  ( 1.001543065824772753E-15, -1.312499999999998224, 4.012584370867899430 ) ) ;
#192071=CARTESIAN_POINT ( 'NONE',  ( 1.737500000000001155, -2.683333333333332682, 3.009438278150922130 ) ) ;
#192113=CARTESIAN_POINT ( 'NONE',  ( 1.737499999999999378, -0.8166666666666668739, -3.009438278150925683 ) ) ;
#192133=FILL_AREA_STYLE ('',( #81599 ) ) ;
#192160=DIRECTION ( 'NONE',  ( -0.000000000000000000, -1.000000000000000000, -0.000000000000000000 ) ) ;
#192186=CARTESIAN_POINT ( 'NONE',  ( -1.737500000000000266, -1.414583332377417735, -3.009438278150923907 ) ) ;
#192349=VERTEX_POINT ( 'NONE', #133643 ) ;
#192355=CARTESIAN_POINT ( 'NONE',  ( 0.000000000000000000, 0.9000000000000014655, 0.000000000000000000 ) ) ;
#192414=ORIENTED_EDGE ( 'NONE', *, *, #118482, .T. ) ;
#192421=CARTESIAN_POINT ( 'NONE',  ( 1.642778471875001811, -3.142708332855375986, 2.845375778867859751 ) ) ;
#192484=CARTESIAN_POINT ( 'NONE',  ( -3.285556943749998737, -2.530208332855374831, 1.896917185911908499 ) ) ;
#192530=CARTESIAN_POINT ( 'NONE',  ( -0.9311234436981480345, -1.778119629485602537, -3.475000000000001421 ) ) ;
#192563=VECTOR ( 'NONE', #19487, 1000.000000000000000 ) ;
#192626=EDGE_LOOP ( 'NONE', ( #162221, #196773, #59955, #83014 ) ) ;
#192632=CARTESIAN_POINT ( 'NONE',  ( 1.642778471875001811, -1.392708332855374653, 2.845375778867859751 ) ) ;
#192641=CARTESIAN_POINT ( 'NONE',  ( 0.000000000000000000, 5.000000000000000888, 10.25000000000000000 ) ) ;
#192667=CARTESIAN_POINT ( 'NONE',  ( 1.737499999999999378, -2.216666666666665453, -3.009438278150925683 ) ) ;
#192668=EDGE_CURVE ( 'NONE', #12234, #136464, #209576, .T. ) ;
#192731=CARTESIAN_POINT ( 'NONE',  ( -3.024971404778824091, -3.100164103410550709, -1.602261151954494700 ) ) ;
#192821=DIRECTION ( 'NONE',  ( 0.000000000000000000, -1.000000000000000000, 0.000000000000000000 ) ) ;
#192858=EDGE_LOOP ( 'NONE', ( #82044, #63669 ) ) ;
#192931=FACE_OUTER_BOUND ( 'NONE', #106095, .T. ) ;
#192999=VERTEX_POINT ( 'NONE', #71805 ) ;
#193001=CARTESIAN_POINT ( 'NONE',  ( -1.642778471874998480, -3.288541666188707246, 2.845375778867863303 ) ) ;
#193054=CARTESIAN_POINT ( 'NONE',  ( -3.475000000000000533, -1.399999999999998579, 0.000000000000000000 ) ) ;
#193103=CARTESIAN_POINT ( 'NONE',  ( -3.475000000000000533, -1.429166666666668251, -2.006292185433948827 ) ) ;
#193157=VERTEX_POINT ( 'NONE', #46830 ) ;
#193166=CARTESIAN_POINT ( 'NONE',  ( 0.000000000000000000, -3.042800438942089514, 0.000000000000000000 ) ) ;
#193177=CARTESIAN_POINT ( 'NONE',  ( 3.285556943750000070, -3.084374999522042415, 0.000000000000000000 ) ) ;
#193196=CARTESIAN_POINT ( 'NONE',  ( 1.737499999999999378, -1.166666666666666519, -3.009438278150925683 ) ) ;
#193197=CARTESIAN_POINT ( 'NONE',  ( 0.000000000000000000, 6.999999999999999112, 0.000000000000000000 ) ) ;
#193270=CARTESIAN_POINT ( 'NONE',  ( 3.475000000000000533, -1.531249999044085541, 0.000000000000000000 ) ) ;
#193444=CARTESIAN_POINT ( 'NONE',  ( 3.285556943749998737, -3.142708332855375986, -1.896917185911906722 ) ) ;
#193507=CARTESIAN_POINT ( 'NONE',  ( -3.285556943750000514, -2.238541666188709200, -1.896917185911906500 ) ) ;
#193566=CARTESIAN_POINT ( 'NONE',  ( 3.285556943749998737, -1.655208332855374609, -1.896917185911906500 ) ) ;
#193613=CARTESIAN_POINT ( 'NONE',  ( 0.000000000000000000, 0.5000000000000004441, 0.000000000000000000 ) ) ;
#193706=CARTESIAN_POINT ( 'NONE',  ( -3.285556943749998737, -2.880208332855377584, 1.896917185911908499 ) ) ;
#193744=CARTESIAN_POINT ( 'NONE',  ( 0.000000000000000000, -1.487500000000001599, -4.012584370867899430 ) ) ;
#193747=FILL_AREA_STYLE ('',( #195899 ) ) ;
#193789=ORIENTED_EDGE ( 'NONE', *, *, #91258, .T. ) ;
#193805=CARTESIAN_POINT ( 'NONE',  ( 1.642778471875000035, -0.6635416661887084677, -2.845375778867859751 ) ) ;
#193806=CARTESIAN_POINT ( 'NONE',  ( -2.112474647679212225, -3.050145162711633162, 2.777154369939415002 ) ) ;
#194002=CARTESIAN_POINT ( 'NONE',  ( -1.642778471875000035, -0.8677083328553769626, -2.845375778867859751 ) ) ;
#194067=PLANE ( 'NONE',  #74188 ) ;
#194119=EDGE_CURVE ( 'NONE', #211538, #183045, #57468, .T. ) ;
#194128=B_SPLINE_CURVE_WITH_KNOTS ( 'NONE', 3,
 ( #174, #134515, #30599, #65189, #146499, #14307, #166990, #133451, #182143, #199456, #80402, #130300, #1250, #117224, #114047, #213567, #97740, #115098, #197338, #196288, #33774, #131343, #212516, #15375, #17500, #66241, #83587, #149669, #48979, #132390, #200519, #64158, #181094, #32711 ),
 .UNSPECIFIED., .F., .F.,
 ( 4, 2, 2, 2, 2, 2, 2, 2, 2, 2, 2, 2, 2, 2, 2, 2, 4 ),
 ( 0.009372056057571971632, 0.009929098612377838459, 0.01048614116718370702, 0.01104318372198957385, 0.01160022627679544241, 0.01215726883160131097, 0.01271431138640717953, 0.01327135394121304636, 0.01382839649601891319, 0.01438543905082478175, 0.01494248160563065031, 0.01549952416043651714, 0.01605656671524238396, 0.01661360927004825253, 0.01717065182485411762, 0.01772769437965998618, 0.01828473693446585127 ),
 .UNSPECIFIED. ) ;
#194173=CARTESIAN_POINT ( 'NONE',  ( 3.475000000000000533, -0.8750000000000007772, 0.000000000000000000 ) ) ;
#194203=ORIENTED_EDGE ( 'NONE', *, *, #71672, .F. ) ;
#194245=CARTESIAN_POINT ( 'NONE',  ( -3.285556943750000514, -2.588541666188707513, -1.896917185911906722 ) ) ;
#194263=CARTESIAN_POINT ( 'NONE',  ( -1.737499999999997824, -2.041666666666667407, 3.009438278150925683 ) ) ;
#194338=CARTESIAN_POINT ( 'NONE',  ( 3.475000000000000533, -1.852083332377418401, -2.006292185433951047 ) ) ;
#194500=DIRECTION ( 'NONE',  ( 0.000000000000000000, -1.000000000000000000, -0.000000000000000000 ) ) ;
#194552=EDGE_CURVE ( 'NONE', #71536, #192349, #40838, .T. ) ;
#194627=CARTESIAN_POINT ( 'NONE',  ( 3.285556943750000514, -1.363541666188709423, 1.896917185911906500 ) ) ;
#194731=AXIS2_PLACEMENT_3D ( 'NONE', #201866, #119648, #151034 ) ;
#194774=CARTESIAN_POINT ( 'NONE',  ( 1.642778471875000035, -2.326041666188709112, -2.845375778867859751 ) ) ;
#194813=CARTESIAN_POINT ( 'NONE',  ( 3.475000000000000533, -2.624999999999998668, 0.000000000000000000 ) ) ;
#194881=CARTESIAN_POINT ( 'NONE',  ( -2.821163330806889746, -3.104354205566886460, -1.931348577005352674 ) ) ;
#195004=DIRECTION ( 'NONE',  ( 0.000000000000000000, 0.000000000000000000, -1.000000000000000000 ) ) ;
#195027=CARTESIAN_POINT ( 'NONE',  ( 0.000000000000000000, 6.999999999999999112, 0.000000000000000000 ) ) ;
#195082=CARTESIAN_POINT ( 'NONE',  ( 1.642778471875000035, -0.9260416661887073131, -2.845375778867859751 ) ) ;
#195117=CARTESIAN_POINT ( 'NONE',  ( 0.000000000000000000, 1.000000000000000888, 0.000000000000000000 ) ) ;
#195249=CARTESIAN_POINT ( 'NONE',  ( -3.284816854459712054, -0.1112512837626866702, -0.08051823526699090905 ) ) ;
#195252=CARTESIAN_POINT ( 'NONE',  ( -3.475000000000000533, -2.129166666666665542, -2.006292185433948827 ) ) ;
#195284=ORIENTED_EDGE ( 'NONE', *, *, #151772, .F. ) ;
#195341=CARTESIAN_POINT ( 'NONE',  ( -3.474999999999998312, -3.120833333333331350, 2.006292185433951047 ) ) ;
#195418=CARTESIAN_POINT ( 'NONE',  ( 1.737500000000001155, -2.639583332377418046, 3.009438278150922130 ) ) ;
#195475=CARTESIAN_POINT ( 'NONE',  ( -1.500000000000035971, 8.500000000000000000, -9.886859966642585817 ) ) ;
#195603=ORIENTED_EDGE ( 'NONE', *, *, #85587, .T. ) ;
#195640=ORIENTED_EDGE ( 'NONE', *, *, #13231, .F. ) ;
#195644=DIRECTION ( 'NONE',  ( 0.000000000000000000, -1.000000000000000000, 0.000000000000000000 ) ) ;
#195709=CARTESIAN_POINT ( 'NONE',  ( -1.642778471874998480, -1.801041666188708090, 2.845375778867863303 ) ) ;
#195776=EDGE_LOOP ( 'NONE', ( #154053, #175544, #165847, #33717 ) ) ;
#195851=CARTESIAN_POINT ( 'NONE',  ( -3.285556943750000514, -2.938541666188710266, -1.896917185911906500 ) ) ;
#195890=CARTESIAN_POINT ( 'NONE',  ( -3.475000000000000533, -2.100000000000000977, 0.000000000000000000 ) ) ;
#195892=CARTESIAN_POINT ( 'NONE',  ( 0.000000000000000000, -0.1968749995220437643, -3.793834371823813001 ) ) ;
#195899=FILL_AREA_STYLE_COLOUR ( '', #3115 ) ;
#195909=ADVANCED_FACE ( 'NONE', ( #151934 ), #125797, .T. ) ;
#195935=CARTESIAN_POINT ( 'NONE',  ( 7.204675194429079505E-15, -1.793749999044084831, -3.475000000000000089 ) ) ;
#195961=CARTESIAN_POINT ( 'NONE',  ( -3.285556943750000514, -0.5760416661887087786, -1.896917185911906500 ) ) ;
#195973=DIRECTION ( 'NONE',  ( -0.6483454320283800199, 0.000000000000000000, 0.7613463080411787542 ) ) ;
#196018=CARTESIAN_POINT ( 'NONE',  ( -2.041582876286177406, -0.8887487162373145511, -2.583516629109316121 ) ) ;
#196117=LINE ( 'NONE', #47754, #43619 ) ;
#196148=CARTESIAN_POINT ( 'NONE',  ( 1.255262969126037241E-15, 5.999999999999998224, -10.25000000000000000 ) ) ;
#196154=CARTESIAN_POINT ( 'NONE',  ( -1.642778471875000035, -0.1677083328553742592, -2.845375778867859751 ) ) ;
#196214=CARTESIAN_POINT ( 'NONE',  ( 1.292131300536165872, -3.232243495192088201, 3.032550610867861707 ) ) ;
#196219=DIRECTION ( 'NONE',  ( 0.9486832980505138790, -0.3162277660168376636, -3.312310031615527152E-15 ) ) ;
#196238=CARTESIAN_POINT ( 'NONE',  ( 0.000000000000000000, -0.5000000000000004441, 0.000000000000000000 ) ) ;
#196288=CARTESIAN_POINT ( 'NONE',  ( 3.328416922175579273, -3.193033774422709303, -0.09933519640907825798 ) ) ;
#196305=CYLINDRICAL_SURFACE ( 'NONE', #34283, 11.00000000000000000 ) ;
#196307=PLANE ( 'NONE',  #186258 ) ;
#196315=FACE_OUTER_BOUND ( 'NONE', #4088, .T. ) ;
#196353=CARTESIAN_POINT ( 'NONE',  ( 1.500000000000039524, 6.999999999999999112, 10.89724735885167561 ) ) ;
#196405=CARTESIAN_POINT ( 'NONE',  ( -1.737499999999997824, -3.091666666666666341, 3.009438278150925683 ) ) ;
#196431=AXIS2_PLACEMENT_3D ( 'NONE', #80240, #13091, #197180 ) ;
#196479=CARTESIAN_POINT ( 'NONE',  ( -1.737500000000000266, -3.514583332377418934, -3.009438278150923907 ) ) ;
#196562=ADVANCED_FACE ( 'NONE', ( #2725 ), #150090, .F. ) ;
#196564=CARTESIAN_POINT ( 'NONE',  ( 1.642778471875001811, -2.442708332855377140, 2.845375778867859751 ) ) ;
#196601=CARTESIAN_POINT ( 'NONE',  ( -1.523611765266693174, 0.5999999999999998668, 1.789163823896770200 ) ) ;
#196660=ORIENTED_EDGE ( 'NONE', *, *, #202477, .T. ) ;
#196751=ADVANCED_FACE ( 'NONE', ( #90424 ), #140263, .T. ) ;
#196767=CARTESIAN_POINT ( 'NONE',  ( 3.285556943750000514, -2.413541666188708579, 1.896917185911906500 ) ) ;
#196773=ORIENTED_EDGE ( 'NONE', *, *, #59598, .T. ) ;
#196844=EDGE_CURVE ( 'NONE', #130259, #85478, #10219, .T. ) ;
#196871=AXIS2_PLACEMENT_3D ( 'NONE', #177783, #182010, #33641 ) ;
#196906=CARTESIAN_POINT ( 'NONE',  ( -1.642778471875000035, -1.567708332855376252, -2.845375778867859751 ) ) ;
#196923=EDGE_CURVE ( 'NONE', #198335, #155131, #68081, .T. ) ;
#196946=CARTESIAN_POINT ( 'NONE',  ( -3.475000000000000533, -3.149999999999999911, 0.000000000000000000 ) ) ;
#196948=CARTESIAN_POINT ( 'NONE',  ( -3.285556943750000070, -3.346874999522041261, 0.000000000000000000 ) ) ;
#196990=AXIS2_PLACEMENT_3D ( 'NONE', #11768, #28034, #159099 ) ;
#197014=CARTESIAN_POINT ( 'NONE',  ( -1.642778471875000035, -0.6052083328553746755, -2.845375778867859751 ) ) ;
#197029=CARTESIAN_POINT ( 'NONE',  ( 0.000000000000000000, 5.000000000000000888, 0.000000000000000000 ) ) ;
#197033=ORIENTED_EDGE ( 'NONE', *, *, #205891, .T. ) ;
#197065=CARTESIAN_POINT ( 'NONE',  ( -1.867619373655151183, -0.8887487162373142180, -2.711732807817992974 ) ) ;
#197127=DIRECTION ( 'NONE',  ( -0.6483454320283799088, 0.000000000000000000, 0.7613463080411786432 ) ) ;
#197164=ORIENTED_EDGE ( 'NONE', *, *, #181495, .T. ) ;
#197166=ORIENTED_EDGE ( 'NONE', *, *, #149738, .T. ) ;
#197176=CARTESIAN_POINT ( 'NONE',  ( -3.336159340019098973, -0.9254121791666594099, 0.08595556041762617006 ) ) ;
#197180=DIRECTION ( 'NONE',  ( 0.000000000000000000, 0.000000000000000000, 1.000000000000000000 ) ) ;
#197196=ORIENTED_EDGE ( 'NONE', *, *, #159826, .T. ) ;
#197200=CARTESIAN_POINT ( 'NONE',  ( -3.285556943749998737, -1.130208332855377140, 1.896917185911908499 ) ) ;
#197270=CARTESIAN_POINT ( 'NONE',  ( 3.285556943750000070, -3.521874999522042859, 0.000000000000000000 ) ) ;
#197279=ORIENTED_EDGE ( 'NONE', *, *, #168859, .F. ) ;
#197338=CARTESIAN_POINT ( 'NONE',  ( 3.300611021875788698, -3.189313111690857294, -0.4679188877521224255 ) ) ;
#197366=CARTESIAN_POINT ( 'NONE',  ( 0.000000000000000000, -2.537500000000000977, -4.012584370867899430 ) ) ;
#197383=CARTESIAN_POINT ( 'NONE',  ( -1.458777222063855072, 1.000000000000000888, 1.713029193092652669 ) ) ;
#197454=CARTESIAN_POINT ( 'NONE',  ( 0.000000000000000000, -3.587500000000000355, -4.012584370867899430 ) ) ;
#197459=ORIENTED_EDGE ( 'NONE', *, *, #211412, .T. ) ;
#197525=CARTESIAN_POINT ( 'NONE',  ( 3.475000000000000533, -2.202083332377417157, -2.006292185433951047 ) ) ;
#197566=VERTEX_POINT ( 'NONE', #84498 ) ;
#197611=CARTESIAN_POINT ( 'NONE',  ( 1.001543065824772753E-15, -1.421874999522042327, 3.793834371823811669 ) ) ;
#197651=EDGE_CURVE ( 'NONE', #70696, #12842, #18424, .T. ) ;
#197660=DIRECTION ( 'NONE',  ( 1.000000000000000000, 0.000000000000000000, -3.491481338843133355E-15 ) ) ;
#197709=ORIENTED_EDGE ( 'NONE', *, *, #33285, .F. ) ;
#197820=CARTESIAN_POINT ( 'NONE',  ( 1.642778471875000035, -4.076041666188710444, -2.845375778867859751 ) ) ;
#197916=VERTEX_POINT ( 'NONE', #65820 ) ;
#197922=EDGE_LOOP ( 'NONE', ( #106047, #44211, #204939, #81517 ) ) ;
#197957=EDGE_LOOP ( 'NONE', ( #139713, #113717, #1991, #89345 ) ) ;
#197963=CARTESIAN_POINT ( 'NONE',  ( -3.285556943749998737, -3.930208332855377407, 1.896917185911908499 ) ) ;
#198007=CARTESIAN_POINT ( 'NONE',  ( 3.285556943750000514, -3.201041666188709112, 1.896917185911906500 ) ) ;
#198068=DIRECTION ( 'NONE',  ( 0.000000000000000000, 0.000000000000000000, -1.000000000000000000 ) ) ;
#198072=CARTESIAN_POINT ( 'NONE',  ( 3.285556943749998737, -1.042708332855377451, -1.896917185911906500 ) ) ;
#198255=CARTESIAN_POINT ( 'NONE',  ( -3.285556943750000070, -2.909374999522040817, 0.000000000000000000 ) ) ;
#198260=DIRECTION ( 'NONE',  ( 0.000000000000000000, -1.000000000000000000, -0.000000000000000000 ) ) ;
#198273=CARTESIAN_POINT ( 'NONE',  ( -1.500000000000039524, 7.750000000000000000, -10.86128356754322688 ) ) ;
#198277=EDGE_CURVE ( 'NONE', #176259, #132336, #40604, .T. ) ;
#198294=CIRCLE ( 'NONE', #52976, 3.475000000000000089 ) ;
#198335=VERTEX_POINT ( 'NONE', #115534 ) ;
#198339=CARTESIAN_POINT ( 'NONE',  ( 3.475000000000000533, -1.210416665710750683, 2.006292185433948827 ) ) ;
#198388=AXIS2_PLACEMENT_3D ( 'NONE', #137767, #40259, #138834 ) ;
#198419=CARTESIAN_POINT ( 'NONE',  ( 0.000000000000000000, -3.937499999999998224, -4.012584370867899430 ) ) ;
#198460=AXIS2_PLACEMENT_3D ( 'NONE', #118827, #4976, #184813 ) ;
#198470=EDGE_CURVE ( 'NONE', #136464, #22324, #161687, .T. ) ;
#198507=CARTESIAN_POINT ( 'NONE',  ( 1.737500000000001155, -2.683333333333332682, 3.009438278150922130 ) ) ;
#198519=CARTESIAN_POINT ( 'NONE',  ( 3.285556943749998737, -0.6927083328553748087, -1.896917185911906500 ) ) ;
#198527=( NAMED_UNIT ( * ) SI_UNIT ( $, .STERADIAN. ) SOLID_ANGLE_UNIT ( ) );
#198544=DIRECTION ( 'NONE',  ( -0.000000000000000000, 1.000000000000000000, -0.000000000000000000 ) ) ;
#198577=CARTESIAN_POINT ( 'NONE',  ( -1.737499999999997824, -3.397916665710751349, 3.009438278150925683 ) ) ;
#198602=CIRCLE ( 'NONE', #84359, 2.500000000000000888 ) ;
#198664=CARTESIAN_POINT ( 'NONE',  ( -1.642778471875000035, -2.267708332855375541, -2.845375778867859751 ) ) ;
#198866=CARTESIAN_POINT ( 'NONE',  ( 1.642778471875001811, -2.792708332855376785, 2.845375778867859751 ) ) ;
#198939=EDGE_CURVE ( 'NONE', #153475, #5754, #16288, .T. ) ;
#198985=CARTESIAN_POINT ( 'NONE',  ( -6.042630808230841359E-15, -2.012500000000000178, 3.474999999999999645 ) ) ;
#199013=CARTESIAN_POINT ( 'NONE',  ( 3.475000000000000533, -0.2041666666666657748, 2.006292185433948827 ) ) ;
#199054=CARTESIAN_POINT ( 'NONE',  ( 3.475000000000000533, -3.325000000000001510, 0.000000000000000000 ) ) ;
#199056=CARTESIAN_POINT ( 'NONE',  ( -3.285556943749998737, -3.317708332855375808, 1.896917185911908499 ) ) ;
#199120=CARTESIAN_POINT ( 'NONE',  ( 1.001543065824772753E-15, -2.209374999522042859, 3.793834371823811669 ) ) ;
#199174=CARTESIAN_POINT ( 'NONE',  ( -0.6744113354752461209, -0.8887487162305419686, -3.223033589173039282 ) ) ;
#199204=CARTESIAN_POINT ( 'NONE',  ( 0.000000000000000000, 0.5000000000000004441, 0.000000000000000000 ) ) ;
#199269=VECTOR ( 'NONE', #32876, 1000.000000000000000 ) ;
#199271=CARTESIAN_POINT ( 'NONE',  ( -1.416814887940473167, 7.999555336178689302, -9.899480522462164700 ) ) ;
#199278=ORIENTED_EDGE ( 'NONE', *, *, #13474, .F. ) ;
#199315=CARTESIAN_POINT ( 'NONE',  ( 3.285556943750000070, -1.684374999522043836, 0.000000000000000000 ) ) ;
#199330=AXIS2_PLACEMENT_3D ( 'NONE', #79629, #28755, #145748 ) ;
#199364=ORIENTED_EDGE ( 'NONE', *, *, #19444, .F. ) ;
#199400=CARTESIAN_POINT ( 'NONE',  ( -1.523611765266693174, 0.5000000000000001110, 1.789163823896770200 ) ) ;
#199401=VECTOR ( 'NONE', #84706, 1000.000000000000000 ) ;
#199456=CARTESIAN_POINT ( 'NONE',  ( 2.194551752856947591, -3.163290167409173570, -2.543720345301475838 ) ) ;
#199472=CARTESIAN_POINT ( 'NONE',  ( -3.469473121595833653, -0.004037186406451471338, -0.1333067274223260212 ) ) ;
#199480=DIRECTION ( 'NONE',  ( -0.000000000000000000, 1.000000000000000000, -0.000000000000000000 ) ) ;
#199482=CARTESIAN_POINT ( 'NONE',  ( 3.475000000000000533, -2.974999999999998312, 0.000000000000000000 ) ) ;
#199503=EDGE_CURVE ( 'NONE', #63041, #213109, #179003, .T. ) ;
#199523=CARTESIAN_POINT ( 'NONE',  ( 1.500000000000039524, 7.193113254731344774, 10.88798745763943465 ) ) ;
#199576=CARTESIAN_POINT ( 'NONE',  ( 1.737500000000001155, -3.033333333333332327, 3.009438278150922130 ) ) ;
#199613=CARTESIAN_POINT ( 'NONE',  ( 3.285556943750000514, -2.063541666188710266, 1.896917185911906722 ) ) ;
#199645=CARTESIAN_POINT ( 'NONE',  ( -3.474999999999998312, -3.777083332377418223, 2.006292185433951047 ) ) ;
#199738=CARTESIAN_POINT ( 'NONE',  ( 3.285556943750000514, -2.063541666188710266, 1.896917185911906500 ) ) ;
#199941=CARTESIAN_POINT ( 'NONE',  ( -3.285556943750000514, -3.988541666188710089, -1.896917185911906500 ) ) ;
#199995=DIRECTION ( 'NONE',  ( 0.000000000000000000, -0.000000000000000000, 1.000000000000000000 ) ) ;
#200084=ORIENTED_EDGE ( 'NONE', *, *, #121881, .T. ) ;
#200090=CARTESIAN_POINT ( 'NONE',  ( -1.642778471874998480, -3.201041666188710000, 2.845375778867863303 ) ) ;
#200134=CARTESIAN_POINT ( 'NONE',  ( -3.285556943750000070, -0.4593749995220435256, 0.000000000000000000 ) ) ;
#200189=DIRECTION ( 'NONE',  ( -0.000000000000000000, -1.000000000000000000, -0.000000000000000000 ) ) ;
#200193=CARTESIAN_POINT ( 'NONE',  ( 3.285556943750000514, -1.801041666188707424, 1.896917185911906500 ) ) ;
#200195=CARTESIAN_POINT ( 'NONE',  ( 3.475000000000000533, -1.910416665710751749, 2.006292185433948827 ) ) ;
#200269=ORIENTED_EDGE ( 'NONE', *, *, #184597, .F. ) ;
#200308=CIRCLE ( 'NONE', #127759, 2.650000000000000799 ) ;
#200309=CARTESIAN_POINT ( 'NONE',  ( 0.000000000000000000, 6.999999999999999112, -11.00000000000000000 ) ) ;
#200321=EDGE_LOOP ( 'NONE', ( #60637, #79355, #82344, #61408, #62389, #67558, #114028, #140702, #60579, #69339, #187541, #22475, #155054, #68365, #58871, #4926, #121023 ) ) ;
#200383=CARTESIAN_POINT ( 'NONE',  ( -1.642778471875000035, -1.567708332855376252, -2.845375778867859751 ) ) ;
#200388=CARTESIAN_POINT ( 'NONE',  ( 7.204675194429079505E-15, -1.137499999999999512, -3.475000000000000089 ) ) ;
#200392=CARTESIAN_POINT ( 'NONE',  ( -1.499999999999966693, 7.750000000000000000, 9.886859966642596476 ) ) ;
#200407=AXIS2_PLACEMENT_3D ( 'NONE', #95216, #132002, #161266 ) ;
#200519=CARTESIAN_POINT ( 'NONE',  ( 2.148112680227530102, -3.224741275562422960, 2.502858284989965210 ) ) ;
#200536=CARTESIAN_POINT ( 'NONE',  ( -3.446831259402118430, -0.01219589716538043052, -0.3300872410877821461 ) ) ;
#200546=CARTESIAN_POINT ( 'NONE',  ( -1.737499999999997824, -2.391666666666667052, 3.009438278150925683 ) ) ;
#200565=LINE ( 'NONE', #197383, #199401 ) ;
#200569=ORIENTED_EDGE ( 'NONE', *, *, #167712, .T. ) ;
#200594=EDGE_CURVE ( 'NONE', #101274, #201966, #87106, .T. ) ;
#200610=AXIS2_PLACEMENT_3D ( 'NONE', #193613, #32184, #164317 ) ;
#200670=CARTESIAN_POINT ( 'NONE',  ( 3.285556943750000070, -1.334374999522040861, 0.000000000000000000 ) ) ;
#200705=CARTESIAN_POINT ( 'NONE',  ( 3.285556943750000070, -0.3718749995220427262, 0.000000000000000000 ) ) ;
#200793=CARTESIAN_POINT ( 'NONE',  ( -3.285556943750000514, -1.888541666188711110, -1.896917185911906500 ) ) ;
#200871=EDGE_CURVE ( 'NONE', #192999, #107993, #23407, .T. ) ;
#200917=( GEOMETRIC_REPRESENTATION_CONTEXT ( 3 ) GLOBAL_UNCERTAINTY_ASSIGNED_CONTEXT ( ( #160207 ) ) GLOBAL_UNIT_ASSIGNED_CONTEXT ( ( #179115, #181227, #198527 ) ) REPRESENTATION_CONTEXT ( 'NONE', 'WORKASPACE' ) );
#200924=DIRECTION ( 'NONE',  ( 0.000000000000000000, -0.000000000000000000, 1.000000000000000000 ) ) ;
#200939=CARTESIAN_POINT ( 'NONE',  ( 4.255647627037042355E-16, -6.776263578034402713E-18, 3.474999999999992095 ) ) ;
#200995=CARTESIAN_POINT ( 'NONE',  ( 3.285556943750000070, -3.084374999522042415, 0.000000000000000000 ) ) ;
#201016=( BOUNDED_CURVE ( )  B_SPLINE_CURVE ( 3, ( #53987, #136317, #172010, #23602 ),
 .UNSPECIFIED., .F., .T. ) 
 B_SPLINE_CURVE_WITH_KNOTS ( ( 4, 4 ),
 ( 1.420228054018210617, 1.445468495626831329 ),
 .UNSPECIFIED. ) 
 CURVE ( )  GEOMETRIC_REPRESENTATION_ITEM ( )  RATIONAL_B_SPLINE_CURVE ( ( 1.000000000000000000, 0.9999469107135832147, 0.9999469107135832147, 1.000000000000000000 ) ) 
 REPRESENTATION_ITEM ( '' )  );
#201039=CARTESIAN_POINT ( 'NONE',  ( 0.000000000000000000, 0.5000000000000004441, -3.475000000000000089 ) ) ;
#201069=ORIENTED_EDGE ( 'NONE', *, *, #185077, .F. ) ;
#201081=CARTESIAN_POINT ( 'NONE',  ( 1.734723475976807094E-15, -7.105553651663779391, 3.150000000000000799 ) ) ;
#201106=ORIENTED_EDGE ( 'NONE', *, *, #75988, .T. ) ;
#201125=CARTESIAN_POINT ( 'NONE',  ( -3.475000000000000533, -2.129166666666665542, -2.006292185433948827 ) ) ;
#201151=CARTESIAN_POINT ( 'NONE',  ( 1.001543065824772753E-15, -3.171874999522042327, 3.793834371823811669 ) ) ;
#201163=CARTESIAN_POINT ( 'NONE',  ( 1.500000000000053291, 7.750000000000000000, 15.74999999999999289 ) ) ;
#201194=CARTESIAN_POINT ( 'NONE',  ( 3.285556943750000070, -0.6343749995220415716, 0.000000000000000000 ) ) ;
#201252=FACE_OUTER_BOUND ( 'NONE', #105828, .T. ) ;
#201256=CARTESIAN_POINT ( 'NONE',  ( 1.001543065824772753E-15, -1.859374999522040550, 3.793834371823811669 ) ) ;
#201383=DIRECTION ( 'NONE',  ( 0.000000000000000000, 0.000000000000000000, 1.000000000000000000 ) ) ;
#201414=CARTESIAN_POINT ( 'NONE',  ( -3.338938632592583833, -0.9270362344595499682, 0.07568478739854733739 ) ) ;
#201442=CARTESIAN_POINT ( 'NONE',  ( 3.285556943749998737, -2.705208332855374209, -1.896917185911906500 ) ) ;
#201534=CARTESIAN_POINT ( 'NONE',  ( 0.000000000000000000, 6.999999999999999112, 0.000000000000000000 ) ) ;
#201598=CARTESIAN_POINT ( 'NONE',  ( -1.499999999999960476, 6.999999999999999112, 10.89724735885168982 ) ) ;
#201632=FACE_OUTER_BOUND ( 'NONE', #13492, .T. ) ;
#201637=CARTESIAN_POINT ( 'NONE',  ( 0.000000000000000000, -1.399999999999998579, 0.000000000000000000 ) ) ;
#201715=CARTESIAN_POINT ( 'NONE',  ( 3.285556943750000070, -0.3718749995220427262, 0.000000000000000000 ) ) ;
#201739=CARTESIAN_POINT ( 'NONE',  ( -1.642778471874998480, -2.501041666188707158, 2.845375778867863303 ) ) ;
#201772=CARTESIAN_POINT ( 'NONE',  ( -3.475000000000000533, -4.185416665710754103, -2.006292185433948827 ) ) ;
#201859=CARTESIAN_POINT ( 'NONE',  ( -1.642778471875000035, -4.017708332855376874, -2.845375778867859751 ) ) ;
#201866=CARTESIAN_POINT ( 'NONE',  ( 0.000000000000000000, 2.000000000000001776, 0.000000000000000000 ) ) ;
#201966=VERTEX_POINT ( 'NONE', #164711 ) ;
#202037=AXIS2_PLACEMENT_3D ( 'NONE', #142748, #126545, #44158 ) ;
#202051=CARTESIAN_POINT ( 'NONE',  ( 3.285556943749998737, -3.055208332855376518, -1.896917185911906500 ) ) ;
#202055=ORIENTED_EDGE ( 'NONE', *, *, #207484, .T. ) ;
#202075=CARTESIAN_POINT ( 'NONE',  ( 3.475000000000000533, -1.531249999044085541, 0.000000000000000000 ) ) ;
#202105=DIRECTION ( 'NONE',  ( -0.6483454320283800199, 0.000000000000000000, 0.7613463080411787542 ) ) ;
#202214=CARTESIAN_POINT ( 'NONE',  ( -3.285556943750000070, -3.259374999522044014, 0.000000000000000000 ) ) ;
#202246=DIRECTION ( 'NONE',  ( 0.000000000000000000, -1.000000000000000000, 0.000000000000000000 ) ) ;
#202259=CARTESIAN_POINT ( 'NONE',  ( 3.285556943749998737, -0.6052083328553753416, -1.896917185911906500 ) ) ;
#202322=CARTESIAN_POINT ( 'NONE',  ( 3.285556943750000514, -2.501041666188708046, 1.896917185911906500 ) ) ;
#202354=CARTESIAN_POINT ( 'NONE',  ( 5.510910596163088569E-16, 2.499999999999998668, 4.500000000000000000 ) ) ;
#202456=CARTESIAN_POINT ( 'NONE',  ( -6.042630808230841359E-15, -2.012500000000000178, 3.474999999999999645 ) ) ;
#202477=EDGE_CURVE ( 'NONE', #5559, #46791, #158419, .T. ) ;
#202490=AXIS2_PLACEMENT_3D ( 'NONE', #164637, #96472, #195004 ) ;
#202511=CARTESIAN_POINT ( 'NONE',  ( -3.285556943750000514, -1.888541666188711110, -1.896917185911906500 ) ) ;
#202630=EDGE_CURVE ( 'NONE', #197916, #167380, #141145, .T. ) ;
#202684=CARTESIAN_POINT ( 'NONE',  ( -1.500000000000039524, 7.064371086078061523, -10.89416074946469770 ) ) ;
#202696=ORIENTED_EDGE ( 'NONE', *, *, #18997, .F. ) ;
#202778=ORIENTED_EDGE ( 'NONE', *, *, #139330, .F. ) ;
#202808=CARTESIAN_POINT ( 'NONE',  ( -1.642778471874998480, -1.101041666188708801, 2.845375778867863303 ) ) ;
#202837=B_SPLINE_CURVE_WITH_KNOTS ( 'NONE', 3,
 ( #183573, #101255, #15732, #151100, #86079, #16791 ),
 .UNSPECIFIED., .F., .F.,
 ( 4, 2, 4 ),
 ( 0.000000000000000000, 0.0006594656818133617666, 0.001318931363626723533 ),
 .UNSPECIFIED. ) ;
#202840=CARTESIAN_POINT ( 'NONE',  ( 3.285556943749998737, -1.392708332855375764, -1.896917185911906500 ) ) ;
#202916=VECTOR ( 'NONE', #39020, 1000.000000000000114 ) ;
#202931=CARTESIAN_POINT ( 'NONE',  ( -3.285556943750000070, -2.909374999522040817, 0.000000000000000000 ) ) ;
#202980=VERTEX_POINT ( 'NONE', #196148 ) ;
#203158=CARTESIAN_POINT ( 'NONE',  ( 0.000000000000000000, 0.5999999999999998668, 0.000000000000000000 ) ) ;
#203190=DIRECTION ( 'NONE',  ( 0.000000000000000000, 1.000000000000000000, 0.000000000000000000 ) ) ;
#203247=ORIENTED_EDGE ( 'NONE', *, *, #86107, .T. ) ;
#203326=CARTESIAN_POINT ( 'NONE',  ( 0.000000000000000000, -1.946874999522044014, -3.793834371823813001 ) ) ;
#203372=AXIS2_PLACEMENT_3D ( 'NONE', #105066, #92020, #87724 ) ;
#203387=CARTESIAN_POINT ( 'NONE',  ( 1.001543065824772753E-15, -2.909374999522043925, 3.793834371823811669 ) ) ;
#203468=SHAPE_REPRESENTATION ( 'base', ( #200407 ), #13653 ) ;
#203470=CARTESIAN_POINT ( 'NONE',  ( 2.218196896764117909, -0.9619707940356122533, 2.597613648450887158 ) ) ;
#203533=ORIENTED_EDGE ( 'NONE', *, *, #69586, .T. ) ;
#203577=CARTESIAN_POINT ( 'NONE',  ( 3.475000000000000533, -0.8750000000000007772, 0.000000000000000000 ) ) ;
#203580=DIRECTION ( 'NONE',  ( 0.000000000000000000, -1.000000000000000000, 0.000000000000000000 ) ) ;
#203589=ORIENTED_EDGE ( 'NONE', *, *, #197651, .T. ) ;
#203610=CARTESIAN_POINT ( 'NONE',  ( -3.475000000000000533, -2.479166666666667851, -2.006292185433948827 ) ) ;
#203770=ORIENTED_EDGE ( 'NONE', *, *, #43314, .F. ) ;
#203776=CARTESIAN_POINT ( 'NONE',  ( 0.000000000000000000, 2.000000000000001776, -11.00000000000000000 ) ) ;
#203828=CARTESIAN_POINT ( 'NONE',  ( 3.475000000000000533, -2.304166666666668473, 2.006292185433948827 ) ) ;
#203850=CARTESIAN_POINT ( 'NONE',  ( 1.642778471875001811, -1.130208332855375808, 2.845375778867859751 ) ) ;
#203875=CARTESIAN_POINT ( 'NONE',  ( 1.642778471875000035, -1.976041666188709689, -2.845375778867859751 ) ) ;
#203905=ORIENTED_EDGE ( 'NONE', *, *, #80012, .F. ) ;
#203908=CARTESIAN_POINT ( 'NONE',  ( -3.285556943750000070, -0.5468749995220407722, 0.000000000000000000 ) ) ;
#203929=CARTESIAN_POINT ( 'NONE',  ( -2.176944501978025137, -3.232243495192087313, 2.478859588741756603 ) ) ;
#203989=CARTESIAN_POINT ( 'NONE',  ( 1.642778471875000035, -3.026041666188708401, -2.845375778867859751 ) ) ;
#204320=CARTESIAN_POINT ( 'NONE',  ( 0.000000000000000000, -1.684374999522041394, -3.793834371823813445 ) ) ;
#204322=AXIS2_PLACEMENT_3D ( 'NONE', #57684, #25167, #107561 ) ;
#204390=CARTESIAN_POINT ( 'NONE',  ( 3.285556943750000514, -1.013541666188710888, 1.896917185911906500 ) ) ;
#204453=CARTESIAN_POINT ( 'NONE',  ( -3.285556943750000514, -0.1385416661887106660, -1.896917185911906500 ) ) ;
#204466=DIRECTION ( 'NONE',  ( -0.6483454320283799088, 0.000000000000000000, 0.7613463080411786432 ) ) ;
#204485=DIRECTION ( 'NONE',  ( 0.000000000000000000, 0.000000000000000000, 1.000000000000000000 ) ) ;
#204486=AXIS2_PLACEMENT_3D ( 'NONE', #6568, #105184, #190654 ) ;
#204508=LINE ( 'NONE', #138486, #83379 ) ;
#204541=CARTESIAN_POINT ( 'NONE',  ( 1.496383747040779033, -0.9083167890128959199, -2.962306210641313164 ) ) ;
#204566=EDGE_CURVE ( 'NONE', #88062, #164595, #101010, .T. ) ;
#204575=AXIS2_PLACEMENT_3D ( 'NONE', #148671, #86862, #136693 ) ;
#204581=CYLINDRICAL_SURFACE ( 'NONE', #76582, 2.750000000000000444 ) ;
#204603=VERTEX_POINT ( 'NONE', #199400 ) ;
#204610=DIRECTION ( 'NONE',  ( -0.000000000000000000, 1.000000000000000000, -0.000000000000000000 ) ) ;
#204644=CARTESIAN_POINT ( 'NONE',  ( 1.001543065824772753E-15, -3.521874999522041083, 3.793834371823811669 ) ) ;
#204796=CARTESIAN_POINT ( 'NONE',  ( -3.420250508247430155, -0.02876672507465954931, -0.2938434605158617985 ) ) ;
#204850=CARTESIAN_POINT ( 'NONE',  ( 3.475000000000000533, -2.610416665710752593, 2.006292185433948827 ) ) ;
#204883=DIRECTION ( 'NONE',  ( 0.000000000000000000, -1.000000000000000000, 0.000000000000000000 ) ) ;
#204917=CARTESIAN_POINT ( 'NONE',  ( 3.285556943750000514, -1.101041666188710355, 1.896917185911906500 ) ) ;
#204920=CARTESIAN_POINT ( 'NONE',  ( 0.000000000000000000, 2.000000000000001776, 0.000000000000000000 ) ) ;
#204939=ORIENTED_EDGE ( 'NONE', *, *, #202630, .T. ) ;
#204972=DIRECTION ( 'NONE',  ( 0.000000000000000000, 0.000000000000000000, 1.000000000000000000 ) ) ;
#204978=CARTESIAN_POINT ( 'NONE',  ( 1.001543065824772753E-15, -2.909374999522043925, 3.793834371823811669 ) ) ;
#204992=ADVANCED_FACE ( 'NONE', ( #167516, #185876 ), #19113, .F. ) ;
#205069=DIRECTION ( 'NONE',  ( 0.000000000000000000, 0.000000000000000000, -1.000000000000000000 ) ) ;
#205070=CARTESIAN_POINT ( 'NONE',  ( 3.475000000000000533, -0.1750000000000015432, 0.000000000000000000 ) ) ;
#205126=VERTEX_POINT ( 'NONE', #150213 ) ;
#205284=DIRECTION ( 'NONE',  ( -0.000000000000000000, -1.000000000000000000, -0.000000000000000000 ) ) ;
#205296=DIRECTION ( 'NONE',  ( -0.6483454320283800199, 0.000000000000000000, 0.7613463080411787542 ) ) ;
#205334=DIRECTION ( 'NONE',  ( -0.6483454320283799088, 0.000000000000000000, 0.7613463080411786432 ) ) ;
#205359=EDGE_LOOP ( 'NONE', ( #100465, #18325, #134570, #183629 ) ) ;
#205406=CARTESIAN_POINT ( 'NONE',  ( 3.285556943750000070, -2.121874999522044281, 0.000000000000000000 ) ) ;
#205477=CARTESIAN_POINT ( 'NONE',  ( 3.285556943749998737, -3.055208332855376518, -1.896917185911906500 ) ) ;
#205535=CARTESIAN_POINT ( 'NONE',  ( 1.642778471875000035, -4.163541666188708135, -2.845375778867859751 ) ) ;
#205556=ORIENTED_EDGE ( 'NONE', *, *, #7000, .T. ) ;
#205567=AXIS2_PLACEMENT_3D ( 'NONE', #91185, #142084, #110685 ) ;
#205725=CARTESIAN_POINT ( 'NONE',  ( 3.285556943750000514, -3.813541666188710710, 1.896917185911906500 ) ) ;
#205891=EDGE_CURVE ( 'NONE', #152360, #130259, #13655, .T. ) ;
#205918=DIRECTION ( 'NONE',  ( 0.000000000000000000, 0.000000000000000000, 1.000000000000000000 ) ) ;
#205921=CIRCLE ( 'NONE', #57196, 2.350000000000000533 ) ;
#205939=CARTESIAN_POINT ( 'NONE',  ( 1.394453263437886604E-15, -2.668749999044085275, 3.474999999999999645 ) ) ;
#205949=CARTESIAN_POINT ( 'NONE',  ( 1.394453263437886604E-15, -1.618749999044085230, 3.474999999999999645 ) ) ;
#205964=CARTESIAN_POINT ( 'NONE',  ( 0.000000000000000000, 2.499999999999998668, 0.000000000000000000 ) ) ;
#205998=CARTESIAN_POINT ( 'NONE',  ( 1.642778471875001811, -1.480208332855375453, 2.845375778867859751 ) ) ;
#206034=AXIS2_PLACEMENT_3D ( 'NONE', #178642, #6774, #95274 ) ;
#206044=DIRECTION ( 'NONE',  ( 0.000000000000000000, 0.000000000000000000, -1.000000000000000000 ) ) ;
#206057=CARTESIAN_POINT ( 'NONE',  ( 3.285556943750000514, -2.151041666188709733, 1.896917185911906500 ) ) ;
#206117=ORIENTED_EDGE ( 'NONE', *, *, #48694, .F. ) ;
#206148=CARTESIAN_POINT ( 'NONE',  ( -1.737499999999997824, -0.2916666666666657415, 3.009438278150925683 ) ) ;
#206171=CARTESIAN_POINT ( 'NONE',  ( 1.734723475976807094E-15, 1.000000000000000888, 0.000000000000000000 ) ) ;
#206199=VERTEX_POINT ( 'NONE', #3761 ) ;
#206234=CARTESIAN_POINT ( 'NONE',  ( -1.737500000000000266, -1.108333333333332726, -3.009438278150923907 ) ) ;
#206257=CARTESIAN_POINT ( 'NONE',  ( 1.394453263437886604E-15, -1.268749999044084253, 3.474999999999999645 ) ) ;
#206297=CARTESIAN_POINT ( 'NONE',  ( 1.499999999999959588, 6.999999999999999112, -10.89724735885168805 ) ) ;
#206312=CARTESIAN_POINT ( 'NONE',  ( -3.475000000000000533, -1.706249999044083587, 0.000000000000000000 ) ) ;
#206333=AXIS2_PLACEMENT_3D ( 'NONE', #97490, #192821, #146250 ) ;
#206387=CARTESIAN_POINT ( 'NONE',  ( 0.000000000000000000, 6.999999999999999112, 0.000000000000000000 ) ) ;
#206481=CARTESIAN_POINT ( 'NONE',  ( -3.285556943749998737, -1.917708332855377673, 1.896917185911908721 ) ) ;
#206532=ADVANCED_FACE ( 'NONE', ( #51495 ), #44629, .T. ) ;
#206544=CARTESIAN_POINT ( 'NONE',  ( 0.000000000000000000, -4.046874999522043659, -3.793834371823813001 ) ) ;
#206608=CARTESIAN_POINT ( 'NONE',  ( 3.285556943750000514, -3.201041666188709112, 1.896917185911906500 ) ) ;
#206630=ORIENTED_EDGE ( 'NONE', *, *, #169931, .T. ) ;
#206779=EDGE_CURVE ( 'NONE', #94956, #155561, #207335, .T. ) ;
#206790=ORIENTED_EDGE ( 'NONE', *, *, #19444, .T. ) ;
#206795=CARTESIAN_POINT ( 'NONE',  ( 0.000000000000000000, -4.046874999522043659, -3.793834371823813001 ) ) ;
#206979=CARTESIAN_POINT ( 'NONE',  ( -0.9311234436981447038, -2.478119629485602715, -3.475000000000004086 ) ) ;
#206999=DIRECTION ( 'NONE',  ( -0.000000000000000000, -1.000000000000000000, -0.000000000000000000 ) ) ;
#207066=CARTESIAN_POINT ( 'NONE',  ( -3.285556943750000070, -1.596874999522043037, 0.000000000000000000 ) ) ;
#207090=ADVANCED_FACE ( 'NONE', ( #127251 ), #188948, .T. ) ;
#207127=CARTESIAN_POINT ( 'NONE',  ( -1.642778471875000035, -1.655208332855377051, -2.845375778867859751 ) ) ;
#207135=TOROIDAL_SURFACE ( 'NONE', #96471, 2.400000000000000355, 0.1000000000000000056 ) ;
#207142=CARTESIAN_POINT ( 'NONE',  ( 1.467252801262404871, -3.037869857053148603, 3.165465571089816521 ) ) ;
#207153=CARTESIAN_POINT ( 'NONE',  ( -1.945698667645833879, -3.232243495192120619, 2.663941817279478208 ) ) ;
#207218=CARTESIAN_POINT ( 'NONE',  ( 1.001543065824772753E-15, -2.012499999999999289, 4.012584370867899430 ) ) ;
#207251=CARTESIAN_POINT ( 'NONE',  ( -0.5999334525453070555, -3.113692707265594439, 3.364453219699692355 ) ) ;
#207255=EDGE_LOOP ( 'NONE', ( #26134, #102939, #94773, #36372 ) ) ;
#207270=ORIENTED_EDGE ( 'NONE', *, *, #171420, .F. ) ;
#207279=TOROIDAL_SURFACE ( 'NONE', #113985, 2.600000000000000089, 0.1000000000000000056 ) ;
#207289=CARTESIAN_POINT ( 'NONE',  ( -2.458659901369638412, -3.215527211319108680, 2.374326415922315636 ) ) ;
#207308=CARTESIAN_POINT ( 'NONE',  ( 3.475000000000000533, -0.8458333333333335480, -2.006292185433951047 ) ) ;
#207335=LINE ( 'NONE', #76271, #44160 ) ;
#207383=CARTESIAN_POINT ( 'NONE',  ( 1.737499999999999378, -0.7729166657107523486, -3.009438278150925683 ) ) ;
#207427=EDGE_LOOP ( 'NONE', ( #177781, #62082 ) ) ;
#207484=EDGE_CURVE ( 'NONE', #74385, #192349, #104890, .T. ) ;
#207545=ORIENTED_EDGE ( 'NONE', *, *, #72642, .F. ) ;
#207583=CARTESIAN_POINT ( 'NONE',  ( 0.000000000000000000, -3.042800438942089514, 3.475000000000000089 ) ) ;
#207610=CARTESIAN_POINT ( 'NONE',  ( 3.285556943750000070, -2.384374999522043126, 0.000000000000000000 ) ) ;
#207677=CARTESIAN_POINT ( 'NONE',  ( -3.285556943750000070, -0.4593749995220435256, 0.000000000000000000 ) ) ;
#207808=CARTESIAN_POINT ( 'NONE',  ( 7.204675194429079505E-15, -1.487500000000000044, -3.475000000000000089 ) ) ;
#207858=CARTESIAN_POINT ( 'NONE',  ( 0.000000000000000000, -0.08749999999999961975, -4.012584370867899430 ) ) ;
#207901=CIRCLE ( 'NONE', #187190, 0.09999999999999982514 ) ;
#208061=VECTOR ( 'NONE', #65679, 1000.000000000000000 ) ;
#208065=CARTESIAN_POINT ( 'NONE',  ( 1.464175926609780964E-14, -2.493749999044085452, -3.475000000000000533 ) ) ;
#208128=CARTESIAN_POINT ( 'NONE',  ( -1.642778471874998480, -1.188541666188709600, 2.845375778867863303 ) ) ;
#208184=CARTESIAN_POINT ( 'NONE',  ( 1.642778471875000035, -1.713541666188707291, -2.845375778867859751 ) ) ;
#208194=ORIENTED_EDGE ( 'NONE', *, *, #2302, .F. ) ;
#208273=CARTESIAN_POINT ( 'NONE',  ( 3.475000000000000533, -1.254166666666665098, 2.006292185433948827 ) ) ;
#208337=CARTESIAN_POINT ( 'NONE',  ( 0.000000000000000000, 0.5000000000000004441, -3.475000000000000089 ) ) ;
#208366=CARTESIAN_POINT ( 'NONE',  ( -1.737500000000000266, -2.508333333333334636, -3.009438278150923907 ) ) ;
#208435=CARTESIAN_POINT ( 'NONE',  ( 1.001543065824772753E-15, -1.268749999044083587, 4.012584370867899430 ) ) ;
#208527=FACE_OUTER_BOUND ( 'NONE', #165079, .T. ) ;
#208598=EDGE_LOOP ( 'NONE', ( #124365, #161905, #189157 ) ) ;
#208668=CARTESIAN_POINT ( 'NONE',  ( 3.285556943750000070, -2.734374999522042771, 0.000000000000000000 ) ) ;
#208733=CARTESIAN_POINT ( 'NONE',  ( 3.285556943750000514, -1.013541666188710888, 1.896917185911906500 ) ) ;
#208779=CARTESIAN_POINT ( 'NONE',  ( -3.475000000000000533, -1.706249999044083587, 0.000000000000000000 ) ) ;
#208898=DIRECTION ( 'NONE',  ( 0.000000000000000000, 0.000000000000000000, 1.000000000000000000 ) ) ;
#208914=CARTESIAN_POINT ( 'NONE',  ( -3.475000000000000533, -1.429166666666668251, -2.006292185433948827 ) ) ;
#208932=EDGE_CURVE ( 'NONE', #104308, #142643, #71930, .T. ) ;
#208977=CARTESIAN_POINT ( 'NONE',  ( -3.422965436091124136, -3.085995815972477629, -0.3132428434422417918 ) ) ;
#209026=EDGE_CURVE ( 'NONE', #169163, #211199, #150841, .T. ) ;
#209226=CARTESIAN_POINT ( 'NONE',  ( 1.250000000000033973, 8.500000000000000000, 9.921567416492207414 ) ) ;
#209238=CARTESIAN_POINT ( 'NONE',  ( 3.285556943749998737, -1.742708332855374076, -1.896917185911906500 ) ) ;
#209330=CARTESIAN_POINT ( 'NONE',  ( 1.737500000000001155, -1.283333333333334325, 3.009438278150922130 ) ) ;
#209423=CARTESIAN_POINT ( 'NONE',  ( 1.737499999999999378, -2.216666666666665453, -3.009438278150925683 ) ) ;
#209455=ORIENTED_EDGE ( 'NONE', *, *, #176534, .T. ) ;
#209498=CARTESIAN_POINT ( 'NONE',  ( 1.737499999999999378, -1.472916665710751527, -3.009438278150925683 ) ) ;
#209570=VECTOR ( 'NONE', #142435, 1000.000000000000000 ) ;
#209576=CIRCLE ( 'NONE', #206034, 3.432849766368862632 ) ;
#209595=EDGE_CURVE ( 'NONE', #155131, #108029, #23551, .T. ) ;
#209669=CARTESIAN_POINT ( 'NONE',  ( 3.285556943750000070, -2.821874999522043570, 0.000000000000000000 ) ) ;
#209734=CARTESIAN_POINT ( 'NONE',  ( 1.642778471875000035, -3.726041666188707691, -2.845375778867859751 ) ) ;
#209784=EDGE_CURVE ( 'NONE', #897, #145305, #96117, .T. ) ;
#209798=CARTESIAN_POINT ( 'NONE',  ( -1.642778471874998480, -1.101041666188708801, 2.845375778867863303 ) ) ;
#209911=ORIENTED_EDGE ( 'NONE', *, *, #2058, .T. ) ;
#209943=CARTESIAN_POINT ( 'NONE',  ( 1.642778471875001811, -2.792708332855376785, 2.845375778867859751 ) ) ;
#209978=CARTESIAN_POINT ( 'NONE',  ( -1.737500000000000266, -1.458333333333332371, -3.009438278150923907 ) ) ;
#210240=ORIENTED_EDGE ( 'NONE', *, *, #189291, .T. ) ;
#210244=ORIENTED_EDGE ( 'NONE', *, *, #31849, .T. ) ;
#210246=CARTESIAN_POINT ( 'NONE',  ( 1.001543065824772753E-15, -0.7218749995220414828, 3.793834371823811669 ) ) ;
#210296=EDGE_CURVE ( 'NONE', #16835, #160077, #106501, .T. ) ;
#210319=CARTESIAN_POINT ( 'NONE',  ( 2.520459579114900261, -4.179124432053225036, -2.338646355340254779 ) ) ;
#210403=CARTESIAN_POINT ( 'NONE',  ( 1.347111479062088405E-15, 5.999999999999998224, 11.00000000000000000 ) ) ;
#210414=CARTESIAN_POINT ( 'NONE',  ( 3.475000000000000533, -0.4958333333333350690, -2.006292185433951047 ) ) ;
#210430=CARTESIAN_POINT ( 'NONE',  ( -3.380278471875000523, -0.05468749976102194044, 0.000000000000000000 ) ) ;
#210433=DIRECTION ( 'NONE',  ( 0.000000000000000000, 0.000000000000000000, 1.000000000000000000 ) ) ;
#210464=VERTEX_POINT ( 'NONE', #151647 ) ;
#210468=ORIENTED_EDGE ( 'NONE', *, *, #58497, .T. ) ;
#210506=CARTESIAN_POINT ( 'NONE',  ( 3.475000000000000533, -1.895833333333332815, -2.006292185433951047 ) ) ;
#210583=CARTESIAN_POINT ( 'NONE',  ( 1.737499999999999378, -1.822916665710751172, -3.009438278150925683 ) ) ;
#210750=CARTESIAN_POINT ( 'NONE',  ( 1.642778471875000035, -2.413541666188709911, -2.845375778867859751 ) ) ;
#210808=CARTESIAN_POINT ( 'NONE',  ( 1.528150327639969719, -3.232243495192087757, 2.908546201585544999 ) ) ;
#210863=DIRECTION ( 'NONE',  ( -3.491481338843133355E-15, 0.000000000000000000, -1.000000000000000000 ) ) ;
#210871=CARTESIAN_POINT ( 'NONE',  ( -1.642778471875000035, -0.8677083328553769626, -2.845375778867859751 ) ) ;
#210892=DIRECTION ( 'NONE',  ( 0.000000000000000000, 1.000000000000000000, 0.000000000000000000 ) ) ;
#211011=CARTESIAN_POINT ( 'NONE',  ( 3.285556943750000514, -2.063541666188710266, 1.896917185911906500 ) ) ;
#211046=CARTESIAN_POINT ( 'NONE',  ( 0.000000000000000000, -2.537500000000000977, -4.012584370867899430 ) ) ;
#211115=CARTESIAN_POINT ( 'NONE',  ( 3.285556943750000514, -0.7510416661887079348, 1.896917185911906500 ) ) ;
#211172=CARTESIAN_POINT ( 'NONE',  ( -0.4577034257980932552, -0.8887487162305418575, -3.253519940713586855 ) ) ;
#211199=VERTEX_POINT ( 'NONE', #58399 ) ;
#211233=ORIENTED_EDGE ( 'NONE', *, *, #41850, .F. ) ;
#211385=CARTESIAN_POINT ( 'NONE',  ( 1.642778471875001811, -3.930208332855376074, 2.845375778867859751 ) ) ;
#211401=CARTESIAN_POINT ( 'NONE',  ( 0.9311234436981512541, -2.903130369558482027, -3.475000000000000977 ) ) ;
#211410=ADVANCED_FACE ( 'NONE', ( #41103 ), #173234, .F. ) ;
#211412=EDGE_CURVE ( 'NONE', #73220, #36604, #88780, .T. ) ;
#211450=CARTESIAN_POINT ( 'NONE',  ( 1.464175926609780964E-14, -2.843749999044085097, -3.475000000000000533 ) ) ;
#211477=CARTESIAN_POINT ( 'NONE',  ( 1.737499999999999378, -1.516666666666666163, -3.009438278150925683 ) ) ;
#211498=ORIENTED_EDGE ( 'NONE', *, *, #12527, .T. ) ;
#211538=VERTEX_POINT ( 'NONE', #192641 ) ;
#211539=DIRECTION ( 'NONE',  ( 0.000000000000000000, -1.000000000000000000, 0.000000000000000000 ) ) ;
#211547=CARTESIAN_POINT ( 'NONE',  ( 3.285556943750000070, -2.734374999522042771, 0.000000000000000000 ) ) ;
#211565=CARTESIAN_POINT ( 'NONE',  ( -1.737500000000000266, -2.858333333333334281, -3.009438278150923907 ) ) ;
#211637=CARTESIAN_POINT ( 'NONE',  ( -3.475000000000000533, -2.406249999044082877, 0.000000000000000000 ) ) ;
#211811=EDGE_CURVE ( 'NONE', #160528, #22347, #185990, .T. ) ;
#211849=DIRECTION ( 'NONE',  ( -3.491481338843133750E-15, -0.000000000000000000, -1.000000000000000000 ) ) ;
#211921=AXIS2_PLACEMENT_3D ( 'NONE', #203158, #139266, #205296 ) ;
#211934=CARTESIAN_POINT ( 'NONE',  ( 3.285556943750000070, -2.034374999522043481, 0.000000000000000000 ) ) ;
#211978=CARTESIAN_POINT ( 'NONE',  ( 0.000000000000000000, -6.776263578034402713E-18, -3.474999999999992095 ) ) ;
#211997=VECTOR ( 'NONE', #54793, 1000.000000000000000 ) ;
#212042=CARTESIAN_POINT ( 'NONE',  ( -0.7684286640458091178, -3.130108765795259984, -3.305065527396989111 ) ) ;
#212071=CARTESIAN_POINT ( 'NONE',  ( 3.285556943750000070, -2.034374999522043481, 0.000000000000000000 ) ) ;
#212110=CARTESIAN_POINT ( 'NONE',  ( 1.737500000000001155, -1.283333333333334325, 3.009438278150922130 ) ) ;
#212112=CARTESIAN_POINT ( 'NONE',  ( -1.642778471875000035, -2.705208332855375986, -2.845375778867859751 ) ) ;
#212239=CARTESIAN_POINT ( 'NONE',  ( -1.297773248481477681, -0.8887487162373152172, -3.026232207781772932 ) ) ;
#212297=VERTEX_POINT ( 'NONE', #207583 ) ;
#212405=DIRECTION ( 'NONE',  ( 0.000000000000000000, -0.000000000000000000, 1.000000000000000000 ) ) ;
#212446=CARTESIAN_POINT ( 'NONE',  ( -1.642778471875000035, -4.105208332855374564, -2.845375778867859751 ) ) ;
#212477=CLOSED_SHELL ( 'NONE', ( #141608, #21309, #166700, #23096, #93822, #112396, #107230, #51380, #27090, #196751, #25658, #24122, #65866, #40884, #125225, #140427, #118259, #162144, #48968, #58788, #140141, #213677, #9776, #26863, #21863, #93777, #109063, #36562, #207090, #101902, #33748, #32, #73321, #86398, #14431, #119076, #34794, #88204, #131899, #125142, #89993, #92234, #48825, #158043, #155738, #211410, #62399, #179760, #189139, #82814, #107080, #204992, #147918, #109112, #24668, #117650, #53541, #176804, #90848, #213872, #115175, #45090, #152515, #174652, #154198, #52177, #142856, #179193, #10817, #206532, #48386, #24021, #20972, #109780, #8500, #155916, #184846, #15215, #18415, #161237, #196562, #71855, #110157, #131853, #114753, #97734, #62572, #195909, #142295, #179066, #73870 ) ) ;
#212516=CARTESIAN_POINT ( 'NONE',  ( 3.261441746617202764, -3.200405687979760216, 0.6342848732913847210 ) ) ;
#212544=CYLINDRICAL_SURFACE ( 'NONE', #25240, 3.150000000000000799 ) ;
#212546=CARTESIAN_POINT ( 'NONE',  ( -3.474999999999998312, -3.470833333333334103, 2.006292185433951047 ) ) ;
#212632=CARTESIAN_POINT ( 'NONE',  ( 1.001543065824772753E-15, -2.712499999999999911, 4.012584370867899430 ) ) ;
#212666=CARTESIAN_POINT ( 'NONE',  ( -1.737500000000000266, -1.064583332377418090, -3.009438278150923907 ) ) ;
#212705=CARTESIAN_POINT ( 'NONE',  ( -3.475000000000000533, -3.456249999044084920, 0.000000000000000000 ) ) ;
#212792=CARTESIAN_POINT ( 'NONE',  ( 3.285556943750000514, -1.013541666188710888, 1.896917185911906500 ) ) ;
#212910=CARTESIAN_POINT ( 'NONE',  ( 1.556029036868112669, 0.5000000000000007772, -1.827231139298829410 ) ) ;
#212996=CARTESIAN_POINT ( 'NONE',  ( -3.285556943750000514, -1.538541666188708357, -1.896917185911906500 ) ) ;
#213006=CARTESIAN_POINT ( 'NONE',  ( 1.500000000000032641, 7.750000000000000000, 9.886859966642587594 ) ) ;
#213094=ORIENTED_EDGE ( 'NONE', *, *, #174269, .F. ) ;
#213109=VERTEX_POINT ( 'NONE', #212910 ) ;
#213128=CARTESIAN_POINT ( 'NONE',  ( 1.500000000000035971, 7.750000000000000000, 10.86128356754324109 ) ) ;
#213142=CARTESIAN_POINT ( 'NONE',  ( -1.642778471874998480, -1.801041666188708090, 2.845375778867863303 ) ) ;
#213180=CARTESIAN_POINT ( 'NONE',  ( -1.737499999999997824, -2.391666666666667052, 3.009438278150925683 ) ) ;
#213182=CARTESIAN_POINT ( 'NONE',  ( 3.285556943749998737, -2.792708332855373676, -1.896917185911906500 ) ) ;
#213205=CARTESIAN_POINT ( 'NONE',  ( -3.410126044457033156, -0.03745499569612897872, 0.000000000000000000 ) ) ;
#213228=ORIENTED_EDGE ( 'NONE', *, *, #161705, .T. ) ;
#213239=PRODUCT_DEFINITION_SHAPE ( 'NONE', 'NONE',  #160678 ) ;
#213246=CARTESIAN_POINT ( 'NONE',  ( -2.658506526196446007, -3.058169421092554963, 2.222368686088465939 ) ) ;
#213378=DIRECTION ( 'NONE',  ( -3.706092522800016599E-15, 0.000000000000000000, -1.000000000000000000 ) ) ;
#213437=VERTEX_POINT ( 'NONE', #37357 ) ;
#213504=CARTESIAN_POINT ( 'NONE',  ( -3.285556943750000070, -3.696874999522044458, 0.000000000000000000 ) ) ;
#213567=CARTESIAN_POINT ( 'NONE',  ( 3.124804640640014064, -3.181435245600519046, -1.183652705699159924 ) ) ;
#213583=CARTESIAN_POINT ( 'NONE',  ( -3.424799127523457276, -0.02060169327834648900, -0.4188067397860005814 ) ) ;
#213593=CARTESIAN_POINT ( 'NONE',  ( 1.737500000000001155, -3.033333333333332327, 3.009438278150922130 ) ) ;
#213677=ADVANCED_FACE ( 'NONE', ( #97609 ), #114961, .F. ) ;
#213753=CARTESIAN_POINT ( 'NONE',  ( 3.475000000000000533, -3.602083332377418401, -2.006292185433951047 ) ) ;
#213809=CARTESIAN_POINT ( 'NONE',  ( -1.500000000000035971, 7.750000000000000000, -9.886859966642584041 ) ) ;
#213842=CARTESIAN_POINT ( 'NONE',  ( -3.285556943749998737, -1.480208332855375453, 1.896917185911908499 ) ) ;
#213872=ADVANCED_FACE ( 'NONE', ( #130169 ), #64023, .F. ) ;
#213949=AXIS2_PLACEMENT_3D ( 'NONE', #48985, #101983, #134520 ) ;
#214035=ORIENTED_EDGE ( 'NONE', *, *, #33740, .T. ) ;
#214038=CARTESIAN_POINT ( 'NONE',  ( 1.642778471875001811, -3.842708332855375275, 2.845375778867859751 ) ) ;
#214105=EDGE_LOOP ( 'NONE', ( #18945, #88990, #25941 ) ) ;
#214118=EDGE_CURVE ( 'NONE', #56290, #213437, #181358, .T. ) ;
#214166=DIRECTION ( 'NONE',  ( 0.7613463080411785322, -0.000000000000000000, 0.6483454320283801309 ) ) ;
#214167=EDGE_CURVE ( 'NONE', #197916, #63041, #51709, .T. ) ;
#214178=CARTESIAN_POINT ( 'NONE',  ( -1.642778471874998480, -3.901041666188709289, 2.845375778867863303 ) ) ;
#214218=CARTESIAN_POINT ( 'NONE',  ( 1.737499999999999378, -3.616666666666667140, -3.009438278150925683 ) ) ;
#214220=CARTESIAN_POINT ( 'NONE',  ( 2.960184520039609524, -4.197067588314596698, -1.425549731837409961 ) ) ;
#214283=CARTESIAN_POINT ( 'NONE',  ( 7.204675194429079505E-15, -1.793749999044084831, -3.475000000000000089 ) ) ;
#214334=CARTESIAN_POINT ( 'NONE',  ( -3.291865441634294509, -0.8887487162373572946, 0.07338535974613247248 ) ) ;
#214401=CARTESIAN_POINT ( 'NONE',  ( 0.000000000000000000, 8.500000000000000000, 0.000000000000000000 ) ) ;
ENDSEC;
END-ISO-10303-21;
